ISO-10303-21;
HEADER;
FILE_DESCRIPTION (('STEP AP214'),
    '1' );
FILE_NAME ('straight miter gear_iso_ISO - Straight miter gear 1.5M20T 20PA 2FW ---20O5H16.576MD5.0N.step',
    '2026-09-24T10:15:42',
    ( '' ),
    ( '' ),
    'SwSTEP 2.0',
    'SolidWorks 2026',
    '' );
FILE_SCHEMA (( 'AUTOMOTIVE_DESIGN' ));
ENDSEC;

DATA;
#3=VERTEX_POINT ( 'NONE', #8497 ) ;
#4=ORIENTED_EDGE ( 'NONE', *, *, #17500, .T. ) ;
#5=B_SPLINE_CURVE_WITH_KNOTS ( 'NONE', 3,
 ( #7725, #1687, #4752, #9340, #164, #3200, #16319, #9048, #7824, #13639, #557, #15165, #451 ),
 .UNSPECIFIED., .F., .F.,
 ( 4, 3, 3, 3, 4 ),
 ( 1.788933584601082316E-18, 0.0002299804304191483382, 0.0004599608082120253344, 0.0006467586077648016917, 0.0008336169836825988323 ),
 .UNSPECIFIED. ) ;
#6=CARTESIAN_POINT ( 'NONE',  ( 3.950837973638668288, 0.000000000000000000, 0.000000000000000000 ) ) ;
#7=CARTESIAN_POINT ( 'NONE',  ( 1.254009781011409919, 5.487405433548389055, 13.61532727684416955 ) ) ;
#8=ORIENTED_EDGE ( 'NONE', *, *, #17820, .T. ) ;
#9=CARTESIAN_POINT ( 'NONE',  ( 8.438534575730034959, 3.845978796786118981, -5.688336279099003079 ) ) ;
#11=ORIENTED_EDGE ( 'NONE', *, *, #5609, .T. ) ;
#18=CARTESIAN_POINT ( 'NONE',  ( 0.4862570985993235340, -13.89016912371018186, 0.7479633556561964269 ) ) ;
#19=ADVANCED_FACE ( 'NONE', ( #12879 ), #13081, .T. ) ;
#24=FACE_OUTER_BOUND ( 'NONE', #1681, .T. ) ;
#25=CARTESIAN_POINT ( 'NONE',  ( 0.4862570985993252548, 11.67702470553365401, 7.559321496869467971 ) ) ;
#27=ORIENTED_EDGE ( 'NONE', *, *, #8314, .T. ) ;
#30=ORIENTED_EDGE ( 'NONE', *, *, #17968, .F. ) ;
#31=VERTEX_POINT ( 'NONE', #18279 ) ;
#35=CARTESIAN_POINT ( 'NONE',  ( 0.4862570985993252548, 11.67702470553365401, 7.559321496869467971 ) ) ;
#37=CARTESIAN_POINT ( 'NONE',  ( 16.56822296793089322, -0.007741272030791128758, 0.006547366384936715959 ) ) ;
#38=CARTESIAN_POINT ( 'NONE',  ( 0.8740779401507028368, 12.04241618260048696, 7.708543377337672808 ) ) ;
#40=CARTESIAN_POINT ( 'NONE',  ( 2.747332970342022840, -7.555624153089539163, -14.49942876448600693 ) ) ;
#49=ADVANCED_FACE ( 'NONE', ( #15133 ), #3233, .F. ) ;
#52=EDGE_LOOP ( 'NONE', ( #9471, #1055, #7657, #12818 ) ) ;
#55=ORIENTED_EDGE ( 'NONE', *, *, #1230, .F. ) ;
#56=EDGE_CURVE ( 'NONE', #18903, #4935, #3396, .T. ) ;
#59=ORIENTED_EDGE ( 'NONE', *, *, #10784, .F. ) ;
#60=CARTESIAN_POINT ( 'NONE',  ( 1.918921323896324083, -12.08297777410667173, 3.258415356426475729 ) ) ;
#69=FACE_OUTER_BOUND ( 'NONE', #6354, .T. ) ;
#79=B_SPLINE_CURVE_WITH_KNOTS ( 'NONE', 3,
 ( #11643, #13256, #14690, #17565, #11836, #14888, #1601, #176, #17673, #5998, #1801, #7447, #16432 ),
 .UNSPECIFIED., .F., .F.,
 ( 4, 3, 3, 3, 4 ),
 ( 2.453269466693398698E-18, 0.0002299780670421062274, 0.0004599561239687902829, 0.0006896788984287884972, 0.0009194956271626412558 ),
 .UNSPECIFIED. ) ;
#86=EDGE_LOOP ( 'NONE', ( #14741, #12706, #5227, #3702 ) ) ;
#89=FACE_OUTER_BOUND ( 'NONE', #1635, .T. ) ;
#98=CARTESIAN_POINT ( 'NONE',  ( 0.3939822652208159193, 8.678192463540325363, -10.75310269629511950 ) ) ;
#108=CARTESIAN_POINT ( 'NONE',  ( 0.4862570985993235340, -5.003653737315397976, -12.97920246947884770 ) ) ;
#109=EDGE_CURVE ( 'NONE', #2481, #6541, #2281, .T. ) ;
#110=ORIENTED_EDGE ( 'NONE', *, *, #15625, .F. ) ;
#111=CARTESIAN_POINT ( 'NONE',  ( 2.002547531651519996, -11.75462648437105173, 4.532360870844282630 ) ) ;
#116=B_SPLINE_CURVE_WITH_KNOTS ( 'NONE', 3,
 ( #18756, #7109, #8540, #9966, #5749, #14281 ),
 .UNSPECIFIED., .F., .F.,
 ( 4, 2, 4 ),
 ( 1.939479807224432123E-18, 0.001657017934710795738, 0.003314035869421589307 ),
 .UNSPECIFIED. ) ;
#117=CARTESIAN_POINT ( 'NONE',  ( 0.3939875929385652231, -10.75308190953749410, 8.678227324501083473 ) ) ;
#118=CARTESIAN_POINT ( 'NONE',  ( 2.123976203522053741, 14.31368049382978569, -6.261444813538409981 ) ) ;
#124=CARTESIAN_POINT ( 'NONE',  ( 3.950837973638668288, 14.41405733518061716, 1.958075594453843493 ) ) ;
#131=ADVANCED_FACE ( 'NONE', ( #5565 ), #15082, .F. ) ;
#133=CARTESIAN_POINT ( 'NONE',  ( 0.3170788640506440603, -8.200855617524609897, 11.02668139258439162 ) ) ;
#136=CARTESIAN_POINT ( 'NONE',  ( 2.123976203522053297, 11.67822624909925544, 10.37815841598495936 ) ) ;
#137=VERTEX_POINT ( 'NONE', #11515 ) ;
#138=CARTESIAN_POINT ( 'NONE',  ( 0.4862570985993235340, -0.7479633556561480212, -13.89016912371018186 ) ) ;
#140=CARTESIAN_POINT ( 'NONE',  ( 0.3145729642390374670, 4.535980493005085989, 12.96842777670208768 ) ) ;
#144=( BOUNDED_SURFACE ( )  B_SPLINE_SURFACE ( 3, 1, ( 
 ( #4726, #10659 ),
 ( #8827, #16291 ),
 ( #14654, #136 ),
 ( #10557, #2981 ) ),
 .UNSPECIFIED., .F., .F., .T. ) 
 B_SPLINE_SURFACE_WITH_KNOTS ( ( 4, 4 ),
 ( 2, 2 ),
 ( 0.000000000000000000, 1.000000000000000000 ),
 ( 0.000000000000000000, 1.000000000000000000 ),
 .UNSPECIFIED. ) 
 GEOMETRIC_REPRESENTATION_ITEM ( )  RATIONAL_B_SPLINE_SURFACE ( (
 ( 1.000000000000000000, 1.000000000000000000),
 ( 0.7792777138730160313, 0.9689936506012927220),
 ( 0.7792777138730160313, 0.9689936506012927220),
 ( 1.000000000000000000, 1.000000000000000000) ) ) 
 REPRESENTATION_ITEM ( '' )  SURFACE ( )  );
#151=CARTESIAN_POINT ( 'NONE',  ( 3.377929128793397684, -9.234024516648242198, -10.50432311212913028 ) ) ;
#152=B_SPLINE_CURVE_WITH_KNOTS ( 'NONE', 3,
 ( #10208, #11842, #17680, #7551, #14410, #10117 ),
 .UNSPECIFIED., .F., .F.,
 ( 4, 2, 4 ),
 ( 8.940560153363745023E-19, 0.0001828790815881870750, 0.0003657581631763732284 ),
 .UNSPECIFIED. ) ;
#153=CARTESIAN_POINT ( 'NONE',  ( 1.846524061778021419, -11.93805390544203426, 3.506196582971057740 ) ) ;
#157=ORIENTED_EDGE ( 'NONE', *, *, #6144, .T. ) ;
#163=VECTOR ( 'NONE', #1770, 1000.000000000000227 ) ;
#164=CARTESIAN_POINT ( 'NONE',  ( 1.847380140988739150, -12.44273713935591097, 0.1101766933248207875 ) ) ;
#176=CARTESIAN_POINT ( 'NONE',  ( 0.3151926232592474619, -8.137833541809298410, -11.07013665200804198 ) ) ;
#177=ORIENTED_EDGE ( 'NONE', *, *, #14523, .F. ) ;
#180=ORIENTED_EDGE ( 'NONE', *, *, #12954, .F. ) ;
#181=VERTEX_POINT ( 'NONE', #6446 ) ;
#184=CARTESIAN_POINT ( 'NONE',  ( 1.846955891736117517, 11.91257079808168839, 3.593597880662386945 ) ) ;
#185=CARTESIAN_POINT ( 'NONE',  ( 16.57778382496167424, -0.002851818597093896349, 0.01466529584256787665 ) ) ;
#201=CARTESIAN_POINT ( 'NONE',  ( 0.3145734862173252266, 8.321353293018990627, -10.93207848441423913 ) ) ;
#203=CARTESIAN_POINT ( 'NONE',  ( 0.3170788640506441158, 7.952793437297734691, -11.20690911610894958 ) ) ;
#212=CARTESIAN_POINT ( 'NONE',  ( 3.950837973638676281, -1.958075594453890789, 14.41405733518059940 ) ) ;
#223=CARTESIAN_POINT ( 'NONE',  ( 16.56753206892534891, -0.004368917149004301892, 0.008432171035096367243 ) ) ;
#224=CARTESIAN_POINT ( 'NONE',  ( 3.950837973638675393, -10.05648675950118509, -10.51028938476228980 ) ) ;
#231=AXIS2_PLACEMENT_3D ( 'NONE', #2781, #14645, #1752 ) ;
#236=ORIENTED_EDGE ( 'NONE', *, *, #1230, .T. ) ;
#241=VECTOR ( 'NONE', #2260, 1000.000000000000000 ) ;
#243=CARTESIAN_POINT ( 'NONE',  ( 1.254255976358384705, 12.44256109021893941, -7.789651112956954115 ) ) ;
#247=CARTESIAN_POINT ( 'NONE',  ( 2.002547531651519996, 3.242439124566821818, -12.17374746633574745 ) ) ;
#249=CARTESIAN_POINT ( 'NONE',  ( 0.3137051932979792457, 13.73004976592202198, 0.4596302728640249136 ) ) ;
#250=B_SPLINE_CURVE_WITH_KNOTS ( 'NONE', 3,
 ( #14214, #9455, #845, #15278, #18327, #2190 ),
 .UNSPECIFIED., .F., .F.,
 ( 4, 2, 4 ),
 ( 2.790109556687801058E-18, 0.0002017457492448093974, 0.0004034914984896159759 ),
 .UNSPECIFIED. ) ;
#259=CARTESIAN_POINT ( 'NONE',  ( 3.074695600507442172, 6.754521329824937581, 14.01296402267882435 ) ) ;
#260=CARTESIAN_POINT ( 'NONE',  ( 3.353306896162455697, -12.78841260990234119, -5.573563251762232440 ) ) ;
#266=CARTESIAN_POINT ( 'NONE',  ( 16.56753206892534891, -0.001549402974393209202, 0.009369540855502124857 ) ) ;
#271=CARTESIAN_POINT ( 'NONE',  ( 2.636624412717099908, 15.80357026013547816, -2.862162146981609201 ) ) ;
#280=ORIENTED_EDGE ( 'NONE', *, *, #17255, .F. ) ;
#283=CARTESIAN_POINT ( 'NONE',  ( 0.4862570985993235340, -11.67702470553359539, -7.559321496869553236 ) ) ;
#284=CARTESIAN_POINT ( 'NONE',  ( 1.847412631396506022, 11.82061107079964124, 3.886120457021434493 ) ) ;
#285=CIRCLE ( 'NONE', #10975, 16.06066017081991149 ) ;
#291=FACE_OUTER_BOUND ( 'NONE', #18282, .T. ) ;
#292=CARTESIAN_POINT ( 'NONE',  ( 2.747332970342022840, 16.17136872824898575, 2.409922051470737348 ) ) ;
#299=B_SPLINE_CURVE_WITH_KNOTS ( 'NONE', 3,
 ( #4256, #2705, #10076, #18865, #9879, #5572, #15994, #2887, #18769, #12755, #6839, #14374, #14094 ),
 .UNSPECIFIED., .F., .F.,
 ( 4, 3, 3, 3, 4 ),
 ( 2.453269466693398698E-18, 0.0002299804304191474167, 0.0004599608082120242502, 0.0006467586077648022338, 0.0008336169836825977481 ),
 .UNSPECIFIED. ) ;
#305=CARTESIAN_POINT ( 'NONE',  ( 0.3939822652208148646, -4.930560016699156556, 12.90851734139305229 ) ) ;
#306=VERTEX_POINT ( 'NONE', #15315 ) ;
#309=EDGE_LOOP ( 'NONE', ( #5566, #18701, #10116, #9842 ) ) ;
#312=CARTESIAN_POINT ( 'NONE',  ( 0.3137051932979792457, -10.83767969834809008, 8.442169467526815296 ) ) ;
#321=B_SPLINE_CURVE_WITH_KNOTS ( 'NONE', 3,
 ( #17192, #9823, #5805, #5438 ),
 .UNSPECIFIED., .F., .F.,
 ( 4, 4 ),
 ( 0.000000000000000000, 0.002004993803842603211 ),
 .UNSPECIFIED. ) ;
#323=CARTESIAN_POINT ( 'NONE',  ( 0.3150686449036046444, -4.099563462784746370, 13.11344473514187037 ) ) ;
#324=CARTESIAN_POINT ( 'NONE',  ( 0.3170788640506440603, 4.100430649997962362, 13.11595226728159425 ) ) ;
#325=ORIENTED_EDGE ( 'NONE', *, *, #17573, .T. ) ;
#326=AXIS2_PLACEMENT_3D ( 'NONE', #1638, #13202, #16171 ) ;
#336=CARTESIAN_POINT ( 'NONE',  ( 0.3148213771069390265, 4.026433757158980775, 13.13560149728601978 ) ) ;
#341=CARTESIAN_POINT ( 'NONE',  ( 3.950837973638675393, -14.31366178983251380, -2.591948120961955926 ) ) ;
#345=CARTESIAN_POINT ( 'NONE',  ( 1.847168016377982669, -11.77471791462001782, 4.022276579849913603 ) ) ;
#346=CARTESIAN_POINT ( 'NONE',  ( 16.56753206892534891, 0.008432171035096448775, -0.004368917149005361808 ) ) ;
#349=VERTEX_POINT ( 'NONE', #8162 ) ;
#351=EDGE_CURVE ( 'NONE', #4935, #7190, #5754, .T. ) ;
#352=CARTESIAN_POINT ( 'NONE',  ( 0.3148208552358962575, 0.2299193288887468323, 13.73693263646118190 ) ) ;
#354=CARTESIAN_POINT ( 'NONE',  ( 1.861628059977342264, -3.332996951203546665, -12.00316790821105073 ) ) ;
#357=B_SPLINE_CURVE_WITH_KNOTS ( 'NONE', 3,
 ( #10765, #14764, #7622, #345, #8933, #1676, #3489, #9329, #7716, #7424, #13338, #153, #5976 ),
 .UNSPECIFIED., .F., .F.,
 ( 4, 3, 3, 3, 4 ),
 ( 1.734723475976807094E-18, 0.0002299804304191486635, 0.0004599608082120272860, 0.0006467586077648025591, 0.0008336169836825982902 ),
 .UNSPECIFIED. ) ;
#359=CARTESIAN_POINT ( 'NONE',  ( 0.4754618798421162973, 0.7484603771386368898, -13.89949764182681768 ) ) ;
#363=CARTESIAN_POINT ( 'NONE',  ( 3.512766787571010241, 14.81029789862133583, -2.682019731918177996 ) ) ;
#371=ORIENTED_EDGE ( 'NONE', *, *, #9707, .F. ) ;
#381=VERTEX_POINT ( 'NONE', #5276 ) ;
#382=CARTESIAN_POINT ( 'NONE',  ( 8.522092701127531811, -4.388629235579537102, -5.397361180353192012 ) ) ;
#385=FACE_OUTER_BOUND ( 'NONE', #17996, .T. ) ;
#386=CARTESIAN_POINT ( 'NONE',  ( 3.377929128793394575, 5.536064832134161229, 12.84367544717937548 ) ) ;
#387=PRESENTATION_STYLE_ASSIGNMENT (( #6024 ) ) ;
#391=CARTESIAN_POINT ( 'NONE',  ( 2.636624412714242194, 14.46769361191244485, 6.973567714906650394 ) ) ;
#392=CARTESIAN_POINT ( 'NONE',  ( 2.636624412714763555, 6.973567714907159321, 14.46769361191226722 ) ) ;
#397=ORIENTED_EDGE ( 'NONE', *, *, #3733, .F. ) ;
#404=EDGE_CURVE ( 'NONE', #17773, #6765, #13791, .T. ) ;
#406=CARTESIAN_POINT ( 'NONE',  ( 1.846138399168762989, -4.238866729160486457, 11.69739621335920710 ) ) ;
#408=EDGE_CURVE ( 'NONE', #9965, #18537, #2403, .T. ) ;
#410=( NAMED_UNIT ( * ) PLANE_ANGLE_UNIT ( ) SI_UNIT ( $, .RADIAN. ) );
#413=CARTESIAN_POINT ( 'NONE',  ( 2.636624412717099908, 14.46769361191384817, -6.973567714910368309 ) ) ;
#416=CARTESIAN_POINT ( 'NONE',  ( 2.123976203522053297, -11.67822624909917550, -10.37815841598504107 ) ) ;
#418=CARTESIAN_POINT ( 'NONE',  ( 0.3142014840576498602, -8.382000553815529997, 10.88517824918540278 ) ) ;
#419=CARTESIAN_POINT ( 'NONE',  ( 1.254255976357772751, -11.25336128106935263, -9.426444230097215993 ) ) ;
#420=ORIENTED_EDGE ( 'NONE', *, *, #6109, .F. ) ;
#424=CARTESIAN_POINT ( 'NONE',  ( 1.846138399168762989, 3.446241763652997836, 11.95493567637851839 ) ) ;
#430=CARTESIAN_POINT ( 'NONE',  ( 0.3939875929385635023, 13.80036004410494499, -0.7003304234513649806 ) ) ;
#431=CARTESIAN_POINT ( 'NONE',  ( 16.57210152137263393, 0.01361613799508961699, -0.005118120558001958316 ) ) ;
#432=CARTESIAN_POINT ( 'NONE',  ( 0.3939822652208138098, 12.90851734139308071, 4.930560016699109482 ) ) ;
#434=EDGE_CURVE ( 'NONE', #181, #4199, #9675, .T. ) ;
#436=CARTESIAN_POINT ( 'NONE',  ( 16.58200780006414732, -0.01080144354108868512, -0.002844973367391535370 ) ) ;
#438=CARTESIAN_POINT ( 'NONE',  ( 0.3151928476913540278, 8.075884471919755114, 11.11514699826553176 ) ) ;
#443=LINE ( 'NONE', #12103, #11221 ) ;
#444=FACE_OUTER_BOUND ( 'NONE', #3964, .T. ) ;
#445=ORIENTED_EDGE ( 'NONE', *, *, #10810, .T. ) ;
#447=VERTEX_POINT ( 'NONE', #5372 ) ;
#448=ORIENTED_EDGE ( 'NONE', *, *, #10596, .T. ) ;
#450=CARTESIAN_POINT ( 'NONE',  ( 0.3939822652208129217, -13.80035637018650974, -0.7002900021919380436 ) ) ;
#451=CARTESIAN_POINT ( 'NONE',  ( 1.846138399168762101, -12.43476674860266229, -0.4167076046096845898 ) ) ;
#457=CARTESIAN_POINT ( 'NONE',  ( 3.950837973638675393, -13.10350451991845055, 6.316429227969417859 ) ) ;
#462=EDGE_CURVE ( 'NONE', #17659, #3664, #17402, .T. ) ;
#470=ORIENTED_EDGE ( 'NONE', *, *, #8782, .T. ) ;
#472=AXIS2_PLACEMENT_3D ( 'NONE', #5716, #17109, #4302 ) ;
#473=VERTEX_POINT ( 'NONE', #7191 ) ;
#477=CARTESIAN_POINT ( 'NONE',  ( 16.56782317627811096, 0.003357783021327236019, -0.009228812961909608689 ) ) ;
#487=CARTESIAN_POINT ( 'NONE',  ( 0.3151930723728407768, 13.09040889075576608, -4.172946285306434078 ) ) ;
#488=AXIS2_PLACEMENT_3D ( 'NONE', #18155, #7953, #2196 ) ;
#489=EDGE_CURVE ( 'NONE', #17676, #8500, #10336, .T. ) ;
#491=EDGE_CURVE ( 'NONE', #2529, #913, #989, .T. ) ;
#492=VERTEX_POINT ( 'NONE', #16064 ) ;
#497=B_SPLINE_CURVE_WITH_KNOTS ( 'NONE', 3,
 ( #14879, #16600, #17753, #3500, #1982, #14773 ),
 .UNSPECIFIED., .F., .F.,
 ( 4, 2, 4 ),
 ( 3.499941646806256644E-17, 0.0001825746017570581273, 0.0003651492035140812891 ),
 .UNSPECIFIED. ) ;
#498=CARTESIAN_POINT ( 'NONE',  ( 2.320520222536476496, 15.64520721754621491, 1.795797593768047262 ) ) ;
#504=EDGE_LOOP ( 'NONE', ( #8548, #8022, #110, #17428 ) ) ;
#505=FACE_OUTER_BOUND ( 'NONE', #4433, .T. ) ;
#508=CARTESIAN_POINT ( 'NONE',  ( 3.074695600507255655, -6.754521329824886955, 14.01296402267885988 ) ) ;
#509=EDGE_CURVE ( 'NONE', #7915, #137, #6486, .T. ) ;
#510=EDGE_CURVE ( 'NONE', #16993, #1072, #2856, .T. ) ;
#513=EDGE_CURVE ( 'NONE', #10109, #4171, #7612, .T. ) ;
#519=CARTESIAN_POINT ( 'NONE',  ( 2.353870697619111052, 12.05847592522643907, 4.720869121224175124 ) ) ;
#524=AXIS2_PLACEMENT_3D ( 'NONE', #18729, #5363, #1342 ) ;
#534=CARTESIAN_POINT ( 'NONE',  ( 0.4862570985993235340, 13.89016912371017476, -0.7479633556562934604 ) ) ;
#535=CARTESIAN_POINT ( 'NONE',  ( 3.950837973638668288, 0.000000000000000000, 0.000000000000000000 ) ) ;
#537=PRODUCT ( 'straight miter gear_iso_ISO - Straight miter gear 1.5M20T 20PA 2FW ---20O5H16.576MD5.0N', 'straight miter gear_iso_ISO - Straight miter gear 1.5M20T 20PA 2FW ---20O5H16.576MD5.0N', '', ( #18470 ) ) ;
#539=DIRECTION ( 'NONE',  ( -0.7635533937278216055, -0.3620487483322522015, 0.5347026451755926280 ) ) ;
#545=CARTESIAN_POINT ( 'NONE',  ( 0.4384471787762829753, 8.732395932355681012, 10.76632603192789617 ) ) ;
#550=ORIENTED_EDGE ( 'NONE', *, *, #3093, .T. ) ;
#555=CARTESIAN_POINT ( 'NONE',  ( 2.636624412714242194, 14.46769361191244485, 6.973567714906650394 ) ) ;
#556=ADVANCED_BREP_SHAPE_REPRESENTATION ( '', ( #10437, #2030 ), #15178 ) ;
#557=CARTESIAN_POINT ( 'NONE',  ( 1.846822687350019754, -12.43915556955403545, -0.2922081769261452022 ) ) ;
#563=LINE ( 'NONE', #12218, #6284 ) ;
#564=CARTESIAN_POINT ( 'NONE',  ( 0.3132635586635977853, 12.89236642382228126, -4.743936529203109487 ) ) ;
#580=CARTESIAN_POINT ( 'NONE',  ( 0.3939875929385661668, 3.598491969338414531, -13.34133634968951831 ) ) ;
#584=CARTESIAN_POINT ( 'NONE',  ( 1.846138399168762989, 11.69739621335922308, 4.238866729160444713 ) ) ;
#589=( BOUNDED_SURFACE ( )  B_SPLINE_SURFACE ( 3, 1, ( 
 ( #17899, #13586 ),
 ( #9192, #12166 ),
 ( #14923, #3353 ),
 ( #1842, #1548 ) ),
 .UNSPECIFIED., .F., .F., .T. ) 
 B_SPLINE_SURFACE_WITH_KNOTS ( ( 4, 4 ),
 ( 2, 2 ),
 ( 0.000000000000000000, 1.000000000000000000 ),
 ( 0.000000000000000000, 1.000000000000000000 ),
 .UNSPECIFIED. ) 
 GEOMETRIC_REPRESENTATION_ITEM ( )  RATIONAL_B_SPLINE_SURFACE ( (
 ( 1.000000000000000000, 1.000000000000000000),
 ( 0.9593108457356467333, 0.9995965569486454649),
 ( 0.9593108457356467333, 0.9995965569486454649),
 ( 1.000000000000000000, 1.000000000000000000) ) ) 
 REPRESENTATION_ITEM ( '' )  SURFACE ( )  );
#592=DIRECTION ( 'NONE',  ( 1.000000000000000000, 0.000000000000000000, 0.000000000000000000 ) ) ;
#594=EDGE_LOOP ( 'NONE', ( #10018, #5497, #2207, #4575 ) ) ;
#595=CARTESIAN_POINT ( 'NONE',  ( 1.846138399168762101, 11.69739621335927815, -4.238866729160283064 ) ) ;
#599=EDGE_LOOP ( 'NONE', ( #4795, #7309, #27, #8867 ) ) ;
#600=CARTESIAN_POINT ( 'NONE',  ( 16.56679352167444819, -0.009190982326619374226, 0.001390132774595425865 ) ) ;
#602=CARTESIAN_POINT ( 'NONE',  ( 0.4862570985993235340, 12.97920246947886191, -5.003653737315353567 ) ) ;
#616=CARTESIAN_POINT ( 'NONE',  ( 8.438534575730034959, 1.899950616255281055, -6.598402093327859319 ) ) ;
#618=VERTEX_POINT ( 'NONE', #13291 ) ;
#623=EDGE_CURVE ( 'NONE', #15645, #13108, #16050, .T. ) ;
#625=EDGE_CURVE ( 'NONE', #6956, #6611, #15112, .T. ) ;
#628=CARTESIAN_POINT ( 'NONE',  ( 0.3137051932979792457, -3.805684345189695783, -13.20008686438109891 ) ) ;
#629=CARTESIAN_POINT ( 'NONE',  ( 3.074695600507183268, 7.366518011946177502, -13.70113613813200537 ) ) ;
#631=FACE_OUTER_BOUND ( 'NONE', #11718, .T. ) ;
#638=ORIENTED_EDGE ( 'NONE', *, *, #5134, .T. ) ;
#640=ORIENTED_EDGE ( 'NONE', *, *, #8910, .T. ) ;
#644=CARTESIAN_POINT ( 'NONE',  ( 1.845756295923353996, 9.776763338604718356, -7.694561132136850112 ) ) ;
#646=CARTESIAN_POINT ( 'NONE',  ( 8.522092701127531811, -2.505958102592576342, -6.489356537178215589 ) ) ;
#651=DIRECTION ( 'NONE',  ( 0.000000000000000000, 0.000000000000000000, 1.000000000000000000 ) ) ;
#652=CARTESIAN_POINT ( 'NONE',  ( 3.664313757352978485, 12.42002390572636372, -7.012524439851359759 ) ) ;
#660=CARTESIAN_POINT ( 'NONE',  ( 3.353306896162455697, -1.348936822032921423, 13.88482890973696016 ) ) ;
#662=CARTESIAN_POINT ( 'NONE',  ( 1.847247051441588184, -7.177495230324629105, -10.16425585218608951 ) ) ;
#663=CARTESIAN_POINT ( 'NONE',  ( 3.664313757352974932, -5.926151963190458893, 12.97355833021538096 ) ) ;
#664=EDGE_CURVE ( 'NONE', #10558, #9813, #10583, .T. ) ;
#666=VERTEX_POINT ( 'NONE', #13954 ) ;
#667=CARTESIAN_POINT ( 'NONE',  ( 2.002547531651519996, -0.6781519942172617998, 12.57989064830759318 ) ) ;
#668=CARTESIAN_POINT ( 'NONE',  ( 1.847034903785825577, -11.76058231742742777, -4.063013886994832013 ) ) ;
#670=ADVANCED_FACE ( 'NONE', ( #3543 ), #3340, .T. ) ;
#674=CARTESIAN_POINT ( 'NONE',  ( 2.636624412714236865, 0.000000000000000000, 0.000000000000000000 ) ) ;
#675=CARTESIAN_POINT ( 'NONE',  ( 0.3137051932979809665, 13.20008686438111312, -3.805684345189650042 ) ) ;
#677=CARTESIAN_POINT ( 'NONE',  ( 8.438534575730034959, -4.221456476902702981, 5.415535776177505589 ) ) ;
#679=CARTESIAN_POINT ( 'NONE',  ( 2.705023505549862595, -13.27418276223636795, 0.8488853074252508124 ) ) ;
#683=CARTESIAN_POINT ( 'NONE',  ( 1.847372867223029846, -3.744745203533896394, -11.86627781945711924 ) ) ;
#687=CARTESIAN_POINT ( 'NONE',  ( 2.353870697619111496, 8.216087327473076130, -10.00946331859655203 ) ) ;
#689=CARTESIAN_POINT ( 'NONE',  ( 1.959212340397945562, -11.71715421693495074, -4.509090217468642692 ) ) ;
#690=( BOUNDED_SURFACE ( )  B_SPLINE_SURFACE ( 3, 1, ( 
 ( #16837, #9567 ),
 ( #4019, #966 ),
 ( #12441, #17029 ),
 ( #12716, #12808 ) ),
 .UNSPECIFIED., .F., .F., .T. ) 
 B_SPLINE_SURFACE_WITH_KNOTS ( ( 4, 4 ),
 ( 2, 2 ),
 ( 0.000000000000000000, 1.000000000000000000 ),
 ( 0.000000000000000000, 1.000000000000000000 ),
 .UNSPECIFIED. ) 
 GEOMETRIC_REPRESENTATION_ITEM ( )  RATIONAL_B_SPLINE_SURFACE ( (
 ( 1.000000000000000000, 1.000000000000000000),
 ( 0.7792777138730158093, 0.9689936506012928330),
 ( 0.7792777138730158093, 0.9689936506012928330),
 ( 1.000000000000000000, 1.000000000000000000) ) ) 
 REPRESENTATION_ITEM ( '' )  SURFACE ( )  );
#695=EDGE_CURVE ( 'NONE', #306, #15917, #9432, .T. ) ;
#699=CARTESIAN_POINT ( 'NONE',  ( 3.377929128793395019, 9.234024516648318581, 10.50432311212905923 ) ) ;
#700=EDGE_CURVE ( 'NONE', #6674, #10089, #4653, .T. ) ;
#701=DIRECTION ( 'NONE',  ( -1.000000000000000000, -0.000000000000000000, -0.000000000000000000 ) ) ;
#703=CARTESIAN_POINT ( 'NONE',  ( 1.977436885026283564, -11.52792723756319582, -10.21547824869606202 ) ) ;
#706=DIRECTION ( 'NONE',  ( 0.7561779333270775005, -0.6534392409364819798, -0.03481510524965015368 ) ) ;
#711=PLANE ( 'NONE',  #11015 ) ;
#712=CARTESIAN_POINT ( 'NONE',  ( 8.522092701127531811, 4.388629235579655230, -5.397361180353095200 ) ) ;
#715=B_SPLINE_CURVE_WITH_KNOTS ( 'NONE', 3,
 ( #8013, #2176, #9524, #5223 ),
 .UNSPECIFIED., .F., .F.,
 ( 4, 4 ),
 ( 2.076240083260000355E-17, 0.003005512676784849197 ),
 .UNSPECIFIED. ) ;
#717=DIRECTION ( 'NONE',  ( -0.7561779333270775005, 0.5081796452863305280, -0.4122479608995649469 ) ) ;
#721=EDGE_CURVE ( 'NONE', #17138, #1603, #13761, .T. ) ;
#730=EDGE_LOOP ( 'NONE', ( #17623, #5630, #1085, #177 ) ) ;
#736=CARTESIAN_POINT ( 'NONE',  ( 2.636624412715137922, -14.46769361191291559, 6.973567714907789927 ) ) ;
#737=CARTESIAN_POINT ( 'NONE',  ( 16.56753206892534891, -0.009389754735541561842, 0.001421777558676752366 ) ) ;
#739=CARTESIAN_POINT ( 'NONE',  ( 1.918921323896325415, -7.860085869556248994, 9.738309537478970768 ) ) ;
#747=EDGE_CURVE ( 'NONE', #1603, #10624, #8981, .T. ) ;
#750=CARTESIAN_POINT ( 'NONE',  ( 1.846138399168762101, 4.238866729160568170, -11.69739621335917690 ) ) ;
#757=ADVANCED_FACE ( 'NONE', ( #11008 ), #16924, .F. ) ;
#760=CARTESIAN_POINT ( 'NONE',  ( 0.8740764193769885448, -7.708542792189400750, -12.04241474978016058 ) ) ;
#775=ORIENTED_EDGE ( 'NONE', *, *, #8349, .F. ) ;
#779=CARTESIAN_POINT ( 'NONE',  ( 1.847380140988742925, -7.224522571381399416, 10.13114603776194045 ) ) ;
#780=CARTESIAN_POINT ( 'NONE',  ( 0.3308579732647023430, -13.25341063505878481, 3.680601586799824076 ) ) ;
#786=CARTESIAN_POINT ( 'NONE',  ( 0.3720661004400040439, 0.7231997263364806638, 13.79610186261030158 ) ) ;
#791=CARTESIAN_POINT ( 'NONE',  ( 3.950837973638668288, 0.000000000000000000, 0.000000000000000000 ) ) ;
#792=CARTESIAN_POINT ( 'NONE',  ( 0.3148213771069329203, -10.97836617636219181, -8.260246460850838801 ) ) ;
#796=VERTEX_POINT ( 'NONE', #15942 ) ;
#798=CARTESIAN_POINT ( 'NONE',  ( 3.950837973638676281, -6.888253895133199300, -12.81214529934982949 ) ) ;
#803=FACE_OUTER_BOUND ( 'NONE', #16659, .T. ) ;
#804=CARTESIAN_POINT ( 'NONE',  ( 1.977436885025821267, -1.488549889121935976, 15.33079650480412326 ) ) ;
#810=B_SPLINE_CURVE_WITH_KNOTS ( 'NONE', 3,
 ( #16439, #7455, #17969, #16342, #8967, #13458 ),
 .UNSPECIFIED., .F., .F.,
 ( 4, 2, 4 ),
 ( 2.168404344971008868E-18, 0.001500839035891550922, 0.003001678071783099675 ),
 .UNSPECIFIED. ) ;
#813=CARTESIAN_POINT ( 'NONE',  ( 3.512766787570694493, 2.025881399556607843, -14.91422000116826041 ) ) ;
#816=ORIENTED_EDGE ( 'NONE', *, *, #6223, .T. ) ;
#817=CONICAL_SURFACE ( 'NONE', #14250, 14.54644660717763927, 0.8559913436420816257 ) ;
#824=EDGE_CURVE ( 'NONE', #1293, #8134, #321, .T. ) ;
#826=APPLICATION_CONTEXT ( 'automotive_design' ) ;
#832=CARTESIAN_POINT ( 'NONE',  ( 0.3058872367615230181, 10.75034008168928068, -8.562166468153600718 ) ) ;
#834=CLOSED_SHELL ( 'NONE', ( #1353, #12116, #18745, #2158, #7258, #14492, #670, #7285, #7540, #16676, #8621, #13198, #16078, #15978, #14844, #4782, #15344, #6030, #16370, #19, #9913, #896, #16768, #16256, #9026, #12362, #10248, #7370, #18298, #3790, #3520, #8034, #9734, #4930, #9876, #2998, #1892, #1119, #7178, #757, #8644, #16920, #1136, #9988, #15975, #7884, #9819, #14781, #12613, #3497, #3154, #16279, #17386, #4390, #12523, #17725, #13690, #3020, #16226, #6733, #11254, #16175, #6172, #11125, #10141, #8520, #131, #5640, #11541, #12593, #1046, #12070, #11650, #14730, #12238, #7929, #6377, #18616, #49, #16677, #2908, #16030, #11593, #16028, #12458, #14143, #7723, #16173, #15476, #10731, #11016, #15599, #11998, #2570, #2108, #4236, #11894, #11236, #16624, #13067, #10236, #8250, #6292, #12047, #12440, #17515, #10077, #9159, #10235, #15790, #17839, #11761, #1734, #12021, #11256, #2177, #6511, #16100, #1146, #10830, #6605, #5029, #9480, #4853, #17963, #13008, #1691, #8975 ) ) ;
#835=CARTESIAN_POINT ( 'NONE',  ( 16.56679352167444819, 0.006618561353600086947, 0.006526964904752371663 ) ) ;
#838=ORIENTED_EDGE ( 'NONE', *, *, #16170, .F. ) ;
#845=CARTESIAN_POINT ( 'NONE',  ( 0.3307726912345202441, 13.25328329128666205, 3.680742887039352151 ) ) ;
#850=CARTESIAN_POINT ( 'NONE',  ( 0.3137051932979792457, 11.37800749014142276, -7.698472063774345564 ) ) ;
#853=CARTESIAN_POINT ( 'NONE',  ( 0.4862570985993235340, -13.89016912371018186, 0.7479633556561964269 ) ) ;
#855=DIRECTION ( 'NONE',  ( 0.000000000000000000, 0.000000000000000000, 1.000000000000000000 ) ) ;
#857=CARTESIAN_POINT ( 'NONE',  ( 1.254255976357841584, 1.011593778944668731, -14.64488542023482331 ) ) ;
#866=CARTESIAN_POINT ( 'NONE',  ( 3.950837973638677170, 6.316429227969654114, -13.10350451991833687 ) ) ;
#872=CARTESIAN_POINT ( 'NONE',  ( 3.512766787570764215, -6.535475144497081779, 13.55823433651946175 ) ) ;
#877=CARTESIAN_POINT ( 'NONE',  ( 16.56753206892534891, 0.009389754735541551434, -0.001421777558676823056 ) ) ;
#883=CARTESIAN_POINT ( 'NONE',  ( 0.3142011359265305392, -4.608101617236689762, -12.94258167753017297 ) ) ;
#888=CARTESIAN_POINT ( 'NONE',  ( 2.002547531651519996, -0.6781519942170860515, -12.57989064830760206 ) ) ;
#889=CARTESIAN_POINT ( 'NONE',  ( 1.918918678667045130, 6.832809802519163256, -10.48466773720554279 ) ) ;
#894=CARTESIAN_POINT ( 'NONE',  ( 1.959212340397961327, 12.53706137681889743, 0.6675998551412224424 ) ) ;
#895=DIRECTION ( 'NONE',  ( -1.000000000000000000, -0.000000000000000000, -0.000000000000000000 ) ) ;
#896=ADVANCED_FACE ( 'NONE', ( #11558 ), #16489, .T. ) ;
#897=CARTESIAN_POINT ( 'NONE',  ( 1.977228804422058728, -14.12033626431055211, 6.152949558601312319 ) ) ;
#907=CARTESIAN_POINT ( 'NONE',  ( 0.3095370825347224519, -4.681152801286251552, 12.91933430393606486 ) ) ;
#909=EDGE_CURVE ( 'NONE', #12106, #1319, #1522, .T. ) ;
#913=VERTEX_POINT ( 'NONE', #1138 ) ;
#914=CARTESIAN_POINT ( 'NONE',  ( 2.636624412716045196, 11.10302021257998994, -11.60464335004042447 ) ) ;
#917=CARTESIAN_POINT ( 'NONE',  ( 1.254009781011619307, -7.789615163754444183, 12.44229282923071445 ) ) ;
#923=CARTESIAN_POINT ( 'NONE',  ( 1.342453679581834924, -14.34050741580209198, 3.649820028552675844 ) ) ;
#925=ORIENTED_EDGE ( 'NONE', *, *, #8906, .T. ) ;
#926=EDGE_CURVE ( 'NONE', #14041, #17093, #6983, .T. ) ;
#928=ORIENTED_EDGE ( 'NONE', *, *, #4691, .F. ) ;
#930=CARTESIAN_POINT ( 'NONE',  ( 1.342453679581834924, 12.51077660954466353, 7.902645620902494450 ) ) ;
#933=CARTESIAN_POINT ( 'NONE',  ( 0.3095370825347234511, -8.444334731364085300, 10.84046130709055333 ) ) ;
#935=ORIENTED_EDGE ( 'NONE', *, *, #13033, .T. ) ;
#937=CARTESIAN_POINT ( 'NONE',  ( 8.522092701127531811, -6.946128462138593029, -0.3779863304871954321 ) ) ;
#939=CARTESIAN_POINT ( 'NONE',  ( 1.846138399168762101, -11.95493567637848109, -3.446241763653124401 ) ) ;
#943=B_SPLINE_CURVE_WITH_KNOTS ( 'NONE', 3,
 ( #16001, #4262, #13232, #5970, #8747, #11615 ),
 .UNSPECIFIED., .F., .F.,
 ( 4, 2, 4 ),
 ( 4.027530160694267299E-17, 0.0002014099069817290827, 0.0004028198139634178872 ),
 .UNSPECIFIED. ) ;
#948=CARTESIAN_POINT ( 'NONE',  ( 16.56872352241294521, 0.009207754980064196751, -0.004907101719995712874 ) ) ;
#950=EDGE_CURVE ( 'NONE', #9697, #3395, #3249, .T. ) ;
#955=CARTESIAN_POINT ( 'NONE',  ( 0.3058872367615230181, 11.46514199369357989, 7.578326039752647958 ) ) ;
#956=B_SPLINE_CURVE_WITH_KNOTS ( 'NONE', 3,
 ( #2833, #10120, #14163, #5806, #11653, #17478 ),
 .UNSPECIFIED., .F., .F.,
 ( 4, 2, 4 ),
 ( 8.673617379884035472E-19, 0.001500839035891551789, 0.003001678071783102711 ),
 .UNSPECIFIED. ) ;
#957=LINE ( 'NONE', #18435, #5032 ) ;
#958=ORIENTED_EDGE ( 'NONE', *, *, #8263, .F. ) ;
#961=CARTESIAN_POINT ( 'NONE',  ( 0.3307726912345201886, -8.558645027434195640, -10.76786801061216714 ) ) ;
#966=CARTESIAN_POINT ( 'NONE',  ( 2.123976203522053741, -14.31368049382974483, 6.261444813538503240 ) ) ;
#967=CARTESIAN_POINT ( 'NONE',  ( 0.3058872367615230181, -10.75034008168922206, 8.562166468153680654 ) ) ;
#970=CARTESIAN_POINT ( 'NONE',  ( 16.56679352167444819, 0.008311568981097982450, 0.004162264567718830001 ) ) ;
#974=ORIENTED_EDGE ( 'NONE', *, *, #1070, .T. ) ;
#982=DIRECTION ( 'NONE',  ( -0.7561779333270775005, 0.5491072561318340872, 0.3559159372837335522 ) ) ;
#987=CARTESIAN_POINT ( 'NONE',  ( 0.3095370825347233956, 7.700448427572036181, -11.38092634279620263 ) ) ;
#989=B_SPLINE_CURVE_WITH_KNOTS ( 'NONE', 3,
 ( #17211, #10142, #15779, #11770, #8804, #17501, #5542, #15966, #2579, #2957, #11393, #8425, #12910 ),
 .UNSPECIFIED., .F., .F.,
 ( 4, 3, 3, 3, 4 ),
 ( 4.670885906470169154E-18, 0.0002299780670421063087, 0.0004599561239687901203, 0.0006896788984287873046, 0.0009194956271626388705 ),
 .UNSPECIFIED. ) ;
#1001=EDGE_CURVE ( 'NONE', #1902, #7915, #810, .T. ) ;
#1004=EDGE_CURVE ( 'NONE', #2340, #1302, #7798, .T. ) ;
#1005=CARTESIAN_POINT ( 'NONE',  ( 0.3095370825347234511, -10.84046130709052314, -8.444334731364126156 ) ) ;
#1007=CARTESIAN_POINT ( 'NONE',  ( 0.4754618798421167414, 0.7484603771386338922, -13.89949764182681768 ) ) ;
#1008=CARTESIAN_POINT ( 'NONE',  ( 16.57210152137263393, 0.01214401161737518019, -0.008007331252332923130 ) ) ;
#1012=VERTEX_POINT ( 'NONE', #12034 ) ;
#1014=CARTESIAN_POINT ( 'NONE',  ( 1.847412631396506022, 3.886120457021560171, -11.82061107079959861 ) ) ;
#1018=CARTESIAN_POINT ( 'NONE',  ( 1.342453679581834924, -3.649820028552632767, -14.34050741580210619 ) ) ;
#1021=CARTESIAN_POINT ( 'NONE',  ( 1.846955891736118849, -11.91257079808165820, -3.593597880662470878 ) ) ;
#1029=CARTESIAN_POINT ( 'NONE',  ( 1.846524061778020531, -4.180439405448407975, 11.71897913237548039 ) ) ;
#1030=ORIENTED_EDGE ( 'NONE', *, *, #3955, .F. ) ;
#1032=ORIENTED_EDGE ( 'NONE', *, *, #11354, .T. ) ;
#1033=CARTESIAN_POINT ( 'NONE',  ( 16.57778382496167424, 0.002851818597093999999, -0.01466529584256785410 ) ) ;
#1036=VERTEX_POINT ( 'NONE', #9164 ) ;
#1037=CARTESIAN_POINT ( 'NONE',  ( 2.002547531651519996, 12.57989064830759496, -0.6781519942172177240 ) ) ;
#1042=DIRECTION ( 'NONE',  ( -1.000000000000000000, -0.000000000000000000, -0.000000000000000000 ) ) ;
#1045=AXIS2_PLACEMENT_3D ( 'NONE', #18602, #5505, #11353 ) ;
#1046=ADVANCED_FACE ( 'NONE', ( #3123 ), #9224, .F. ) ;
#1048=EDGE_CURVE ( 'NONE', #8831, #8605, #1481, .T. ) ;
#1050=FILL_AREA_STYLE ('',( #5450 ) ) ;
#1051=DIRECTION ( 'NONE',  ( -0.7635533937278214944, -0.1790966170213966202, 0.6204116510013472086 ) ) ;
#1052=B_SPLINE_CURVE_WITH_KNOTS ( 'NONE', 3,
 ( #4893, #6326, #3442, #7765, #17986, #9278 ),
 .UNSPECIFIED., .F., .F.,
 ( 4, 2, 4 ),
 ( 3.903127820947815962E-18, 0.0002017457492448081235, 0.0004034914984896123438 ),
 .UNSPECIFIED. ) ;
#1055=ORIENTED_EDGE ( 'NONE', *, *, #4349, .F. ) ;
#1058=CARTESIAN_POINT ( 'NONE',  ( 0.3151928476913619104, -4.245853234426296474, -13.06671852871093265 ) ) ;
#1059=ORIENTED_EDGE ( 'NONE', *, *, #6680, .F. ) ;
#1061=CARTESIAN_POINT ( 'NONE',  ( 3.512766787570756222, -14.81029789862160762, 2.682019731918325878 ) ) ;
#1063=ORIENTED_EDGE ( 'NONE', *, *, #56, .F. ) ;
#1068=CARTESIAN_POINT ( 'NONE',  ( 1.846138399168762101, 7.646096044340033870, -9.815003036200328879 ) ) ;
#1070=EDGE_CURVE ( 'NONE', #17590, #5950, #14707, .T. ) ;
#1072=VERTEX_POINT ( 'NONE', #12228 ) ;
#1075=CARTESIAN_POINT ( 'NONE',  ( 0.3307726912345229087, -13.25328329128663007, -3.680742887039447631 ) ) ;
#1076=CARTESIAN_POINT ( 'NONE',  ( 2.002547531651519996, -3.242439124566566910, -12.17374746633581495 ) ) ;
#1079=CARTESIAN_POINT ( 'NONE',  ( 1.846955891736119293, 4.094751675596701723, 11.74973605926565767 ) ) ;
#1081=ORIENTED_EDGE ( 'NONE', *, *, #10539, .F. ) ;
#1085=ORIENTED_EDGE ( 'NONE', *, *, #8263, .T. ) ;
#1092=VECTOR ( 'NONE', #2228, 1000.000000000000114 ) ;
#1094=CARTESIAN_POINT ( 'NONE',  ( 2.747332970342022840, 7.555624153089646633, 14.49942876448594831 ) ) ;
#1095=CARTESIAN_POINT ( 'NONE',  ( 2.636624412715362631, -15.80357026013197519, 2.862162146984090327 ) ) ;
#1100=CARTESIAN_POINT ( 'NONE',  ( 2.002547531651519996, -12.57989064830760206, 0.6781519942171299054 ) ) ;
#1103=VERTEX_POINT ( 'NONE', #750 ) ;
#1104=ORIENTED_EDGE ( 'NONE', *, *, #11705, .T. ) ;
#1107=B_SPLINE_CURVE_WITH_KNOTS ( 'NONE', 3,
 ( #17995, #872, #508, #12167 ),
 .UNSPECIFIED., .F., .F.,
 ( 4, 4 ),
 ( 0.000000000000000000, 0.002004993803842710330 ),
 .UNSPECIFIED. ) ;
#1109=CARTESIAN_POINT ( 'NONE',  ( 2.353870697619111496, 12.53036919722789477, -3.268530966681500782 ) ) ;
#1113=CARTESIAN_POINT ( 'NONE',  ( 0.3720661004400037664, 8.694226082900744501, -10.73619472937692620 ) ) ;
#1118=MECHANICAL_DESIGN_GEOMETRIC_PRESENTATION_REPRESENTATION('',(#6327),#6934);
#1119=ADVANCED_FACE ( 'NONE', ( #3523 ), #7277, .F. ) ;
#1125=EDGE_CURVE ( 'NONE', #447, #4102, #18800, .T. ) ;
#1129=ORIENTED_EDGE ( 'NONE', *, *, #12774, .F. ) ;
#1132=ORIENTED_EDGE ( 'NONE', *, *, #3811, .T. ) ;
#1133=CARTESIAN_POINT ( 'NONE',  ( 16.56872352241294521, 0.001821578298043785094, -0.01027347319884367241 ) ) ;
#1135=CARTESIAN_POINT ( 'NONE',  ( 0.8740764193766140666, 14.27348595579769253, 0.8420116711621705718 ) ) ;
#1136=ADVANCED_FACE ( 'NONE', ( #12314 ), #18869, .F. ) ;
#1138=CARTESIAN_POINT ( 'NONE',  ( 0.3137051932979775248, 3.805684345189972895, -13.20008686438101719 ) ) ;
#1141=( BOUNDED_SURFACE ( )  B_SPLINE_SURFACE ( 3, 1, ( 
 ( #8181, #15158 ),
 ( #5206, #3771 ),
 ( #6462, #9595 ),
 ( #5020, #907 ) ),
 .UNSPECIFIED., .F., .F., .T. ) 
 B_SPLINE_SURFACE_WITH_KNOTS ( ( 4, 4 ),
 ( 2, 2 ),
 ( 0.000000000000000000, 1.000000000000000000 ),
 ( 0.000000000000000000, 1.000000000000000000 ),
 .UNSPECIFIED. ) 
 GEOMETRIC_REPRESENTATION_ITEM ( )  RATIONAL_B_SPLINE_SURFACE ( (
 ( 1.000000000000000000, 1.000000000000000000),
 ( 0.9593108457356467333, 0.9995965569486454649),
 ( 0.9593108457356467333, 0.9995965569486454649),
 ( 1.000000000000000000, 1.000000000000000000) ) ) 
 REPRESENTATION_ITEM ( '' )  SURFACE ( )  );
#1145=AXIS2_PLACEMENT_3D ( 'NONE', #3509, #15177, #651 ) ;
#1146=ADVANCED_FACE ( 'NONE', ( #16985 ), #12295, .F. ) ;
#1147=CARTESIAN_POINT ( 'NONE',  ( 3.950837973638668288, 0.000000000000000000, 0.000000000000000000 ) ) ;
#1148=CARTESIAN_POINT ( 'NONE',  ( 3.950837973638676281, -10.05648675950133963, 10.51028938476214059 ) ) ;
#1152=CARTESIAN_POINT ( 'NONE',  ( 1.342453679581834924, -14.34050741580204402, -3.649820028552883233 ) ) ;
#1153=CARTESIAN_POINT ( 'NONE',  ( 2.747332970342022840, 2.705255688517843371, 16.12459247543627683 ) ) ;
#1154=CARTESIAN_POINT ( 'NONE',  ( 8.522092701127531811, -6.489356537178172957, -2.505958102592690473 ) ) ;
#1155=ORIENTED_EDGE ( 'NONE', *, *, #5662, .F. ) ;
#1159=B_SPLINE_CURVE_WITH_KNOTS ( 'NONE', 3,
 ( #17224, #15420, #1075, #12739, #5471, #11318 ),
 .UNSPECIFIED., .F., .F.,
 ( 4, 2, 4 ),
 ( 3.144186300207962859E-18, 0.0002017457492448081777, 0.0004034914984896132112 ),
 .UNSPECIFIED. ) ;
#1163=CARTESIAN_POINT ( 'NONE',  ( 3.950837973638677170, -14.31366178983255466, 2.591948120961746760 ) ) ;
#1165=ORIENTED_EDGE ( 'NONE', *, *, #14548, .F. ) ;
#1168=CARTESIAN_POINT ( 'NONE',  ( 0.3939822652208163078, 3.598529276937260324, 13.34132036472938410 ) ) ;
#1176=CARTESIAN_POINT ( 'NONE',  ( 3.950837973638676281, 1.958075594453990487, -14.41405733518058341 ) ) ;
#1178=( BOUNDED_SURFACE ( )  B_SPLINE_SURFACE ( 3, 1, ( 
 ( #14213, #2533 ),
 ( #8736, #17731 ),
 ( #37, #13319 ),
 ( #1476, #8382 ) ),
 .UNSPECIFIED., .F., .F., .T. ) 
 B_SPLINE_SURFACE_WITH_KNOTS ( ( 4, 4 ),
 ( 2, 2 ),
 ( 0.000000000000000000, 1.000000000000000000 ),
 ( 0.000000000000000000, 1.000000000000000000 ),
 .UNSPECIFIED. ) 
 GEOMETRIC_REPRESENTATION_ITEM ( )  RATIONAL_B_SPLINE_SURFACE ( (
 ( 1.000000000000000000, 1.000000000000000000),
 ( 0.9933953342250436691, 0.8357391271907733676),
 ( 0.9933953342250436691, 0.8357391271907733676),
 ( 1.000000000000000000, 1.000000000000000000) ) ) 
 REPRESENTATION_ITEM ( '' )  SURFACE ( )  );
#1184=VERTEX_POINT ( 'NONE', #8204 ) ;
#1185=EDGE_CURVE ( 'NONE', #17332, #1103, #11737, .T. ) ;
#1188=ORIENTED_EDGE ( 'NONE', *, *, #2248, .T. ) ;
#1189=DIRECTION ( 'NONE',  ( -1.000000000000000000, -0.000000000000000000, -0.000000000000000000 ) ) ;
#1191=CARTESIAN_POINT ( 'NONE',  ( 1.846138399168762101, 12.43476674860266584, -0.4167076046095982700 ) ) ;
#1192=CARTESIAN_POINT ( 'NONE',  ( 0.000000000000000000, 0.000000000000000000, 2.500000000000000000 ) ) ;
#1193=CARTESIAN_POINT ( 'NONE',  ( 0.3058872367615226295, 4.821066432589507400, -12.87003593440623206 ) ) ;
#1197=VECTOR ( 'NONE', #8771, 1000.000000000000114 ) ;
#1200=ORIENTED_EDGE ( 'NONE', *, *, #12873, .F. ) ;
#1201=ORIENTED_EDGE ( 'NONE', *, *, #10324, .F. ) ;
#1207=FACE_OUTER_BOUND ( 'NONE', #3846, .T. ) ;
#1210=DIRECTION ( 'NONE',  ( -1.000000000000000000, -0.000000000000000000, -0.000000000000000000 ) ) ;
#1212=CARTESIAN_POINT ( 'NONE',  ( 0.3148213771069364175, -11.24846294176317407, 7.888490156175182122 ) ) ;
#1220=CARTESIAN_POINT ( 'NONE',  ( 1.342453679581834924, 11.38190519890867236, -9.456403821038676938 ) ) ;
#1228=B_SPLINE_CURVE_WITH_KNOTS ( 'NONE', 3,
 ( #4633, #4434, #7410, #16296 ),
 .UNSPECIFIED., .F., .F.,
 ( 4, 4 ),
 ( 2.211347213673310975E-17, 0.003005512676784851799 ),
 .UNSPECIFIED. ) ;
#1230=EDGE_CURVE ( 'NONE', #18002, #13478, #8565, .T. ) ;
#1233=CARTESIAN_POINT ( 'NONE',  ( 1.846955891736116184, -0.2634721419534329923, -12.44001089941741611 ) ) ;
#1234=ORIENTED_EDGE ( 'NONE', *, *, #4931, .F. ) ;
#1235=CARTESIAN_POINT ( 'NONE',  ( 2.697797270744668019, 7.053988368581864066, 11.26906156738829168 ) ) ;
#1236=DIRECTION ( 'NONE',  ( 0.7071067818211358436, 8.659560554583467185E-17, 0.7071067805519591909 ) ) ;
#1239=CARTESIAN_POINT ( 'NONE',  ( 0.4385251269669960816, -8.732456510146150208, 10.76637725024249193 ) ) ;
#1242=CARTESIAN_POINT ( 'NONE',  ( 2.636624412716913390, 14.14563173255587536, -7.605649742760633991 ) ) ;
#1249=( BOUNDED_SURFACE ( )  B_SPLINE_SURFACE ( 3, 1, ( 
 ( #12346, #18183 ),
 ( #3653, #9484 ),
 ( #12809, #967 ),
 ( #877, #8418 ) ),
 .UNSPECIFIED., .F., .F., .T. ) 
 B_SPLINE_SURFACE_WITH_KNOTS ( ( 4, 4 ),
 ( 2, 2 ),
 ( 0.000000000000000000, 1.000000000000000000 ),
 ( 0.000000000000000000, 1.000000000000000000 ),
 .UNSPECIFIED. ) 
 GEOMETRIC_REPRESENTATION_ITEM ( )  RATIONAL_B_SPLINE_SURFACE ( (
 ( 1.000000000000000000, 1.000000000000000000),
 ( 0.9933953342250438912, 0.8357391271907739227),
 ( 0.9933953342250438912, 0.8357391271907739227),
 ( 1.000000000000000000, 1.000000000000000000) ) ) 
 REPRESENTATION_ITEM ( '' )  SURFACE ( )  );
#1251=CARTESIAN_POINT ( 'NONE',  ( 1.846138399168762989, 9.815003036200414144, 7.646096044339929954 ) ) ;
#1252=CARTESIAN_POINT ( 'NONE',  ( 1.254009781011992342, -5.487405433548717681, -13.61532727684465982 ) ) ;
#1256=B_SPLINE_CURVE_WITH_KNOTS ( 'NONE', 3,
 ( #12154, #13570, #6696, #3342, #6507, #17982, #16732, #15105, #8043, #3633, #2021, #9468, #7860 ),
 .UNSPECIFIED., .F., .F.,
 ( 4, 3, 3, 3, 4 ),
 ( 1.734723475976806902E-18, 0.0002299804304191488261, 0.0004599608082120263644, 0.0006467586077648019086, 0.0008336169836826000249 ),
 .UNSPECIFIED. ) ;
#1261=ORIENTED_EDGE ( 'NONE', *, *, #6767, .F. ) ;
#1262=EDGE_CURVE ( 'NONE', #7136, #7670, #2721, .T. ) ;
#1264=EDGE_CURVE ( 'NONE', #3, #15917, #15366, .T. ) ;
#1270=DIRECTION ( 'NONE',  ( -1.000000000000000000, -0.000000000000000000, -0.000000000000000000 ) ) ;
#1271=FACE_OUTER_BOUND ( 'NONE', #2673, .T. ) ;
#1275=ORIENTED_EDGE ( 'NONE', *, *, #909, .T. ) ;
#1277=AXIS2_PLACEMENT_3D ( 'NONE', #16062, #13389, #11959 ) ;
#1278=ORIENTED_EDGE ( 'NONE', *, *, #18035, .T. ) ;
#1281=FACE_OUTER_BOUND ( 'NONE', #599, .T. ) ;
#1282=( BOUNDED_SURFACE ( )  B_SPLINE_SURFACE ( 3, 1, ( 
 ( #12044, #16349 ),
 ( #3332, #3229 ),
 ( #17584, #17484 ),
 ( #16048, #10322 ) ),
 .UNSPECIFIED., .F., .F., .T. ) 
 B_SPLINE_SURFACE_WITH_KNOTS ( ( 4, 4 ),
 ( 2, 2 ),
 ( 0.000000000000000000, 1.000000000000000000 ),
 ( 0.000000000000000000, 1.000000000000000000 ),
 .UNSPECIFIED. ) 
 GEOMETRIC_REPRESENTATION_ITEM ( )  RATIONAL_B_SPLINE_SURFACE ( (
 ( 1.000000000000000000, 1.000000000000000000),
 ( 0.7792777138730158093, 0.9689936506012928330),
 ( 0.7792777138730158093, 0.9689936506012928330),
 ( 1.000000000000000000, 1.000000000000000000) ) ) 
 REPRESENTATION_ITEM ( '' )  SURFACE ( )  );
#1283=CARTESIAN_POINT ( 'NONE',  ( 0.3095370825347224519, 0.4597470195092092093, -13.73357284481724250 ) ) ;
#1284=( BOUNDED_SURFACE ( )  B_SPLINE_SURFACE ( 3, 1, ( 
 ( #2638, #16020 ),
 ( #14586, #4367 ),
 ( #15833, #11356 ),
 ( #14396, #10192 ) ),
 .UNSPECIFIED., .F., .F., .T. ) 
 B_SPLINE_SURFACE_WITH_KNOTS ( ( 4, 4 ),
 ( 2, 2 ),
 ( 0.000000000000000000, 1.000000000000000000 ),
 ( 0.000000000000000000, 1.000000000000000000 ),
 .UNSPECIFIED. ) 
 GEOMETRIC_REPRESENTATION_ITEM ( )  RATIONAL_B_SPLINE_SURFACE ( (
 ( 1.000000000000000000, 1.000000000000000000),
 ( 0.7792777138730160313, 0.9689936506012927220),
 ( 0.7792777138730160313, 0.9689936506012927220),
 ( 1.000000000000000000, 1.000000000000000000) ) ) 
 REPRESENTATION_ITEM ( '' )  SURFACE ( )  );
#1293=VERTEX_POINT ( 'NONE', #2810 ) ;
#1294=ORIENTED_EDGE ( 'NONE', *, *, #5885, .F. ) ;
#1295=VECTOR ( 'NONE', #18044, 1000.000000000000114 ) ;
#1298=ORIENTED_EDGE ( 'NONE', *, *, #13046, .T. ) ;
#1300=CARTESIAN_POINT ( 'NONE',  ( 16.56679352167444819, -0.009170718284672552470, -0.001518074900130618379 ) ) ;
#1302=VERTEX_POINT ( 'NONE', #9898 ) ;
#1303=CARTESIAN_POINT ( 'NONE',  ( 0.3095370825347233956, -8.444334731363927204, -10.84046130709067590 ) ) ;
#1319=VERTEX_POINT ( 'NONE', #5985 ) ;
#1330=CARTESIAN_POINT ( 'NONE',  ( 1.959283090834841090, -10.53516775895155000, -6.829027319138364582 ) ) ;
#1339=CIRCLE ( 'NONE', #6236, 16.06066017081991149 ) ;
#1341=DIRECTION ( 'NONE',  ( 0.000000000000000000, 0.000000000000000000, 1.000000000000000000 ) ) ;
#1342=DIRECTION ( 'NONE',  ( 0.000000000000000000, 0.000000000000000000, 1.000000000000000000 ) ) ;
#1344=CARTESIAN_POINT ( 'NONE',  ( 16.56872352241294521, -0.009382111268606286789, 0.004564908236400187953 ) ) ;
#1352=B_SPLINE_CURVE_WITH_KNOTS ( 'NONE', 3,
 ( #13112, #3152, #9003, #17609, #14830, #18 ),
 .UNSPECIFIED., .F., .F.,
 ( 4, 2, 4 ),
 ( 2.017461075144244397E-18, 0.0002017457492448097769, 0.0004034914984896175480 ),
 .UNSPECIFIED. ) ;
#1353=ADVANCED_FACE ( 'NONE', ( #1587 ), #8852, .F. ) ;
#1354=CARTESIAN_POINT ( 'NONE',  ( 8.522092701127531811, 5.841710761610186431, -3.777034505568459100 ) ) ;
#1362=( BOUNDED_SURFACE ( )  B_SPLINE_SURFACE ( 3, 1, ( 
 ( #11523, #11804 ),
 ( #17639, #10466 ),
 ( #16301, #7125 ),
 ( #17342, #4259 ) ),
 .UNSPECIFIED., .F., .F., .T. ) 
 B_SPLINE_SURFACE_WITH_KNOTS ( ( 4, 4 ),
 ( 2, 2 ),
 ( 0.000000000000000000, 1.000000000000000000 ),
 ( 0.000000000000000000, 1.000000000000000000 ),
 .UNSPECIFIED. ) 
 GEOMETRIC_REPRESENTATION_ITEM ( )  RATIONAL_B_SPLINE_SURFACE ( (
 ( 1.000000000000000000, 1.000000000000000000),
 ( 0.9933953342250438912, 0.8357391271907739227),
 ( 0.9933953342250438912, 0.8357391271907739227),
 ( 1.000000000000000000, 1.000000000000000000) ) ) 
 REPRESENTATION_ITEM ( '' )  SURFACE ( )  );
#1364=CARTESIAN_POINT ( 'NONE',  ( 3.512766787570723803, -13.25664064834472100, -7.127386085302978458 ) ) ;
#1369=VECTOR ( 'NONE', #13910, 1000.000000000000000 ) ;
#1373=ORIENTED_EDGE ( 'NONE', *, *, #18131, .T. ) ;
#1374=CARTESIAN_POINT ( 'NONE',  ( 1.254255976357440572, -14.24071337840763363, 3.563435620217590749 ) ) ;
#1376=DIRECTION ( 'NONE',  ( 0.7561779333270775005, 0.03481510524965243658, -0.6534392409364818688 ) ) ;
#1380=EDGE_CURVE ( 'NONE', #9425, #7190, #8549, .T. ) ;
#1383=CARTESIAN_POINT ( 'NONE',  ( 16.56679352167444819, -0.001518074900130714439, 0.009170718284672536857 ) ) ;
#1386=CARTESIAN_POINT ( 'NONE',  ( 0.3137051932979792457, -3.805684345189695783, -13.20008686438109891 ) ) ;
#1395=ORIENTED_EDGE ( 'NONE', *, *, #16139, .T. ) ;
#1399=CARTESIAN_POINT ( 'NONE',  ( 2.636624412714236865, 1.966863607038798701E-15, 16.06066017081991149 ) ) ;
#1400=CARTESIAN_POINT ( 'NONE',  ( 0.3170788640506440603, 13.74111462631963576, 0.1533108587036622894 ) ) ;
#1401=CARTESIAN_POINT ( 'NONE',  ( 16.56782317627811096, -0.009814734722107087972, -0.0003415813796005906337 ) ) ;
#1402=ORIENTED_EDGE ( 'NONE', *, *, #14672, .T. ) ;
#1406=CARTESIAN_POINT ( 'NONE',  ( 3.950837973638675393, 10.51028938476217967, 10.05648675950130233 ) ) ;
#1409=CARTESIAN_POINT ( 'NONE',  ( 2.002547531651519996, -9.778737580845639599, -7.942910686618280813 ) ) ;
#1411=AXIS2_PLACEMENT_3D ( 'NONE', #6939, #15993, #5664 ) ;
#1412=CARTESIAN_POINT ( 'NONE',  ( 1.846822687350026193, -4.121816957446279517, 11.74004266906802663 ) ) ;
#1416=ORIENTED_EDGE ( 'NONE', *, *, #14728, .F. ) ;
#1420=EDGE_CURVE ( 'NONE', #13478, #12877, #1720, .T. ) ;
#1421=ORIENTED_EDGE ( 'NONE', *, *, #17693, .F. ) ;
#1425=CARTESIAN_POINT ( 'NONE',  ( 1.846613052777652975, 11.93415846513961753, 3.520031056876344433 ) ) ;
#1428=LINE ( 'NONE', #1613, #8402 ) ;
#1430=CARTESIAN_POINT ( 'NONE',  ( 2.002547531651519996, -9.778737580845639599, -7.942910686618280813 ) ) ;
#1434=CARTESIAN_POINT ( 'NONE',  ( 0.3145734862173260593, -13.73540602248380615, -0.3064017202076792512 ) ) ;
#1435=FACE_OUTER_BOUND ( 'NONE', #7651, .T. ) ;
#1437=CARTESIAN_POINT ( 'NONE',  ( 1.846613052777650976, 7.585914669018171352, 9.862487290071024759 ) ) ;
#1443=CARTESIAN_POINT ( 'NONE',  ( 2.320520222537238553, -13.71278186123262799, 7.743191299717230969 ) ) ;
#1446=CARTESIAN_POINT ( 'NONE',  ( 0.4754618798421162973, 3.583352865732857495, -13.45049478164055756 ) ) ;
#1451=EDGE_LOOP ( 'NONE', ( #10350, #9045, #13529, #7763 ) ) ;
#1453=B_SPLINE_CURVE_WITH_KNOTS ( 'NONE', 3,
 ( #2355, #4689, #10976, #12048 ),
 .UNSPECIFIED., .F., .F.,
 ( 4, 4 ),
 ( 0.000000000000000000, 0.002004993803842541195 ),
 .UNSPECIFIED. ) ;
#1463=CARTESIAN_POINT ( 'NONE',  ( 0.3058872367615230181, -0.6080468242579999405, -13.72992299905060776 ) ) ;
#1470=CARTESIAN_POINT ( 'NONE',  ( 1.977436885025663837, -15.04044112860237625, 3.321781585408698056 ) ) ;
#1473=CARTESIAN_POINT ( 'NONE',  ( 1.861706995891668326, -3.332865258614060355, 12.00328602385079257 ) ) ;
#1476=CARTESIAN_POINT ( 'NONE',  ( 16.56872352241294521, -0.007240717549633937135, 0.007512283835805527027 ) ) ;
#1481=B_SPLINE_CURVE_WITH_KNOTS ( 'NONE', 3,
 ( #11747, #17682, #6200, #17871, #10314, #16240 ),
 .UNSPECIFIED., .F., .F.,
 ( 4, 2, 4 ),
 ( 0.000000000000000000, 0.001656992708823241348, 0.003313985417646482697 ),
 .UNSPECIFIED. ) ;
#1482=CARTESIAN_POINT ( 'NONE',  ( 1.254009781011254265, 9.426200207651111995, 11.25324419414182664 ) ) ;
#1483=CARTESIAN_POINT ( 'NONE',  ( 1.342453679581834924, -7.902645620902353230, -12.51077660954474702 ) ) ;
#1488=CARTESIAN_POINT ( 'NONE',  ( 16.58200780006414732, -0.01115192838421568723, -0.0006320991582349211584 ) ) ;
#1489=CARTESIAN_POINT ( 'NONE',  ( 2.705023505549863483, -3.294610156755986452, 12.88681800078731321 ) ) ;
#1491=CARTESIAN_POINT ( 'NONE',  ( 2.636624412716045196, 11.10302021257998994, -11.60464335004042447 ) ) ;
#1493=ORIENTED_EDGE ( 'NONE', *, *, #17018, .T. ) ;
#1500=CARTESIAN_POINT ( 'NONE',  ( 16.56679352167444819, -0.009170718284672554205, 0.001518074900131824228 ) ) ;
#1504=CARTESIAN_POINT ( 'NONE',  ( 3.512766787570837490, 10.40533104696128497, 10.87507422923887646 ) ) ;
#1508=VECTOR ( 'NONE', #17994, 1000.000000000000000 ) ;
#1509=CIRCLE ( 'NONE', #2412, 14.54644660717763927 ) ;
#1511=FACE_OUTER_BOUND ( 'NONE', #2606, .T. ) ;
#1522=LINE ( 'NONE', #14234, #10985 ) ;
#1528=CARTESIAN_POINT ( 'NONE',  ( 1.845756295923363322, -10.33914852636099191, -6.920504327368305120 ) ) ;
#1530=CARTESIAN_POINT ( 'NONE',  ( 0.4385251269669940277, 8.732456510146231921, -10.76637725024242442 ) ) ;
#1532=EDGE_CURVE ( 'NONE', #10202, #5002, #13321, .T. ) ;
#1533=CARTESIAN_POINT ( 'NONE',  ( 8.438534575730034959, -5.415535776177550886, 4.221456476902647914 ) ) ;
#1534=EDGE_CURVE ( 'NONE', #18142, #17352, #5581, .T. ) ;
#1536=ORIENTED_EDGE ( 'NONE', *, *, #18056, .T. ) ;
#1537=CARTESIAN_POINT ( 'NONE',  ( 3.950837973638675393, -10.51028938476224894, 10.05648675950122595 ) ) ;
#1539=ORIENTED_EDGE ( 'NONE', *, *, #1778, .F. ) ;
#1540=FACE_OUTER_BOUND ( 'NONE', #10498, .T. ) ;
#1542=CARTESIAN_POINT ( 'NONE',  ( 3.512766787570702487, -10.87507422923887113, -10.40533104696150701 ) ) ;
#1548=CARTESIAN_POINT ( 'NONE',  ( 0.3095370825347224519, 10.84046130709058886, 8.444334731364044444 ) ) ;
#1559=CARTESIAN_POINT ( 'NONE',  ( 1.846138399168762101, -12.43476674860266940, 0.4167076046095114505 ) ) ;
#1560=ORIENTED_EDGE ( 'NONE', *, *, #10909, .T. ) ;
#1568=CARTESIAN_POINT ( 'NONE',  ( 2.636624412714237309, 11.10302021257826866, 11.60464335004050973 ) ) ;
#1570=CARTESIAN_POINT ( 'NONE',  ( 16.58200780006414732, -0.007066318000004643239, -0.008650561019685603162 ) ) ;
#1571=DIRECTION ( 'NONE',  ( 0.7561779333270775005, 0.5081796452863215352, 0.4122479608995760492 ) ) ;
#1573=UNCERTAINTY_MEASURE_WITH_UNIT (LENGTH_MEASURE( 1.000000000000000082E-05 ), #18630, 'distance_accuracy_value', 'NONE');
#1575=CARTESIAN_POINT ( 'NONE',  ( 2.636624412714292376, 11.60464335004048309, 11.10302021257707850 ) ) ;
#1579=CARTESIAN_POINT ( 'NONE',  ( 0.3170788640506441158, -11.02668139258447866, 8.200855617524497987 ) ) ;
#1581=CIRCLE ( 'NONE', #1277, 16.06066017081991149 ) ;
#1585=ORIENTED_EDGE ( 'NONE', *, *, #13107, .F. ) ;
#1587=FACE_OUTER_BOUND ( 'NONE', #14766, .T. ) ;
#1595=CARTESIAN_POINT ( 'NONE',  ( 0.3720661004400037664, 13.34435358167257313, -3.575426119359045529 ) ) ;
#1599=DIRECTION ( 'NONE',  ( 0.7071067818211358436, 0.000000000000000000, -0.7071067805519591909 ) ) ;
#1601=CARTESIAN_POINT ( 'NONE',  ( 0.3151928476913555821, -8.075884471919669849, -11.11514699826559571 ) ) ;
#1602=ORIENTED_EDGE ( 'NONE', *, *, #2547, .F. ) ;
#1603=VERTEX_POINT ( 'NONE', #7385 ) ;
#1604=ORIENTED_EDGE ( 'NONE', *, *, #13965, .F. ) ;
#1606=CARTESIAN_POINT ( 'NONE',  ( 0.3720661004400040439, -3.575426119359279564, 13.34435358167251984 ) ) ;
#1610=CARTESIAN_POINT ( 'NONE',  ( 1.847247051441591070, 11.78111530882023317, 4.004229874809065670 ) ) ;
#1611=FACE_OUTER_BOUND ( 'NONE', #16509, .T. ) ;
#1612=B_SPLINE_CURVE_WITH_KNOTS ( 'NONE', 3,
 ( #18819, #5715, #1434, #14421, #7173, #10126, #15951, #13085, #8412, #14243, #17199, #8690, #7273 ),
 .UNSPECIFIED., .F., .F.,
 ( 4, 3, 3, 3, 4 ),
 ( 3.144186300207962859E-18, 0.0002299780670421060105, 0.0004599561239687904998, 0.0006896788984287882803, 0.0009194956271626397379 ),
 .UNSPECIFIED. ) ;
#1613=CARTESIAN_POINT ( 'NONE',  ( 8.438534575730034959, 0.2320579683291088824, -6.862570336891073097 ) ) ;
#1614=VERTEX_POINT ( 'NONE', #17312 ) ;
#1618=CARTESIAN_POINT ( 'NONE',  ( 16.56872352241294521, 0.01033355228142499721, 0.001442253899401261912 ) ) ;
#1620=CARTESIAN_POINT ( 'NONE',  ( 2.320521194584406199, 14.32454473830047270, -6.542541239687196253 ) ) ;
#1628=AXIS2_PLACEMENT_3D ( 'NONE', #15591, #9847, #7292 ) ;
#1630=CARTESIAN_POINT ( 'NONE',  ( 0.3095370825347224519, 8.444334731364161684, -10.84046130709049471 ) ) ;
#1635=EDGE_LOOP ( 'NONE', ( #3913, #371, #6936, #6859 ) ) ;
#1638=CARTESIAN_POINT ( 'NONE',  ( 2.636624412714236865, 0.000000000000000000, 0.000000000000000000 ) ) ;
#1644=CARTESIAN_POINT ( 'NONE',  ( 3.950837973638668288, 0.000000000000000000, 0.000000000000000000 ) ) ;
#1645=CARTESIAN_POINT ( 'NONE',  ( 0.3058872367615230181, -13.24582953854922529, -3.664492643742902178 ) ) ;
#1647=CARTESIAN_POINT ( 'NONE',  ( 0.3137051932979792457, 7.698472063774471685, 11.37800749014133928 ) ) ;
#1649=CARTESIAN_POINT ( 'NONE',  ( 0.3137051932979809665, -4.679953077377580151, 12.91601973349268917 ) ) ;
#1652=VERTEX_POINT ( 'NONE', #13006 ) ;
#1653=CARTESIAN_POINT ( 'NONE',  ( 0.4384471787762845851, -4.978024343488958614, -12.93784327393178302 ) ) ;
#1655=ORIENTED_EDGE ( 'NONE', *, *, #1264, .T. ) ;
#1656=CARTESIAN_POINT ( 'NONE',  ( 1.846138399168762989, -3.446241763653083101, 11.95493567637849530 ) ) ;
#1663=CARTESIAN_POINT ( 'NONE',  ( 0.4754618798421171855, 3.583352865732860604, -13.45049478164055756 ) ) ;
#1664=CARTESIAN_POINT ( 'NONE',  ( 1.959212340397946006, -4.509090217468600947, 11.71715421693496673 ) ) ;
#1667=CARTESIAN_POINT ( 'NONE',  ( 2.320520222538862143, 13.71278186123479870, -7.743191299716691844 ) ) ;
#1676=CARTESIAN_POINT ( 'NONE',  ( 1.847461586945728929, -11.82388984758122064, 3.877048136045332605 ) ) ;
#1679=ORIENTED_EDGE ( 'NONE', *, *, #4558, .F. ) ;
#1681=EDGE_LOOP ( 'NONE', ( #2116, #2959, #6082, #2082 ) ) ;
#1687=CARTESIAN_POINT ( 'NONE',  ( 1.846613052777651198, -12.43780859207240042, 0.3401093050881381363 ) ) ;
#1691=ADVANCED_FACE ( 'NONE', ( #505 ), #5914, .F. ) ;
#1692=CARTESIAN_POINT ( 'NONE',  ( 16.56753206892534891, 0.004368917149005337522, 0.008432171035096464387 ) ) ;
#1693=CARTESIAN_POINT ( 'NONE',  ( 3.950837973638677170, -1.958075594453692503, -14.41405733518062959 ) ) ;
#1694=CARTESIAN_POINT ( 'NONE',  ( 1.846138399168762101, 12.43476674860266584, -0.4167076046095982700 ) ) ;
#1696=CARTESIAN_POINT ( 'NONE',  ( 2.320520222537280741, -6.542539914240626864, 14.32454429810376162 ) ) ;
#1699=ORIENTED_EDGE ( 'NONE', *, *, #9940, .T. ) ;
#1700=VECTOR ( 'NONE', #15659, 1000.000000000000000 ) ;
#1706=ORIENTED_EDGE ( 'NONE', *, *, #17242, .F. ) ;
#1707=CARTESIAN_POINT ( 'NONE',  ( 0.3137051932979757485, -11.37800749014125223, -7.698472063774596030 ) ) ;
#1709=CARTESIAN_POINT ( 'NONE',  ( 2.747332970342022840, 14.63517873738947195, 7.289199830147158998 ) ) ;
#1712=VERTEX_POINT ( 'NONE', #3449 ) ;
#1715=EDGE_CURVE ( 'NONE', #13002, #14390, #9283, .T. ) ;
#1718=CARTESIAN_POINT ( 'NONE',  ( 1.847247051441591514, -10.16425585218606109, 7.177495230324669961 ) ) ;
#1720=B_SPLINE_CURVE_WITH_KNOTS ( 'NONE', 3,
 ( #9046, #10383, #4748, #17652, #16419, #4559, #352, #14875, #6281, #3100 ),
 .UNSPECIFIED., .F., .F.,
 ( 4, 3, 3, 4 ),
 ( 0.0004597478348664300451, 0.0004599561239687907166, 0.0006896788984287883888, 0.0009194956271626400631 ),
 .UNSPECIFIED. ) ;
#1726=CARTESIAN_POINT ( 'NONE',  ( 2.705023505549865703, 11.23800170568056878, 7.115606223895208693 ) ) ;
#1728=CARTESIAN_POINT ( 'NONE',  ( 1.959283090834841090, 11.71721539537261414, -4.509128209890848282 ) ) ;
#1729=EDGE_CURVE ( 'NONE', #10438, #8651, #15823, .T. ) ;
#1731=CARTESIAN_POINT ( 'NONE',  ( 16.56822296793089322, -0.002414375228568327748, 0.009847136207496262617 ) ) ;
#1734=ADVANCED_FACE ( 'NONE', ( #15115 ), #6555, .F. ) ;
#1739=CARTESIAN_POINT ( 'NONE',  ( 2.705023505549866591, -11.23800170568051371, -7.115606223895292182 ) ) ;
#1740=CARTESIAN_POINT ( 'NONE',  ( 3.950837973638677170, 1.958075594453790869, 14.41405733518061538 ) ) ;
#1750=CARTESIAN_POINT ( 'NONE',  ( 0.4754618798421162973, -0.7484603771383456783, -13.89949764182683545 ) ) ;
#1752=DIRECTION ( 'NONE',  ( 0.000000000000000000, 0.000000000000000000, 1.000000000000000000 ) ) ;
#1755=CARTESIAN_POINT ( 'NONE',  ( 2.747332970342022840, -7.555624153089749662, 14.49942876448589679 ) ) ;
#1762=CARTESIAN_POINT ( 'NONE',  ( 1.918918678667047129, -3.258447776119917094, 12.08296592096907318 ) ) ;
#1763=ORIENTED_EDGE ( 'NONE', *, *, #10294, .T. ) ;
#1767=( BOUNDED_SURFACE ( )  B_SPLINE_SURFACE ( 3, 1, ( 
 ( #15221, #2134 ),
 ( #13780, #6800 ),
 ( #12617, #1152 ),
 ( #15667, #15304 ) ),
 .UNSPECIFIED., .F., .F., .T. ) 
 B_SPLINE_SURFACE_WITH_KNOTS ( ( 4, 4 ),
 ( 2, 2 ),
 ( 0.000000000000000000, 1.000000000000000000 ),
 ( 0.000000000000000000, 1.000000000000000000 ),
 .UNSPECIFIED. ) 
 GEOMETRIC_REPRESENTATION_ITEM ( )  RATIONAL_B_SPLINE_SURFACE ( (
 ( 1.000000000000000000, 1.000000000000000000),
 ( 0.7792777138730158093, 0.9689936506012928330),
 ( 0.7792777138730158093, 0.9689936506012928330),
 ( 1.000000000000000000, 1.000000000000000000) ) ) 
 REPRESENTATION_ITEM ( '' )  SURFACE ( )  );
#1768=CARTESIAN_POINT ( 'NONE',  ( 2.320521194584054037, 7.743190876765937425, -13.71278319228217946 ) ) ;
#1769=CIRCLE ( 'NONE', #1145, 14.54644660717763927 ) ;
#1770=DIRECTION ( 'NONE',  ( 0.7635533937278214944, -0.3966532189476670300, 0.5095610256143814354 ) ) ;
#1771=PLANE ( 'NONE',  #5356 ) ;
#1776=CARTESIAN_POINT ( 'NONE',  ( 3.950837973638676281, 10.05648675950141602, -10.51028938476206953 ) ) ;
#1778=EDGE_CURVE ( 'NONE', #1652, #6835, #5758, .T. ) ;
#1779=EDGE_CURVE ( 'NONE', #2783, #5819, #16527, .T. ) ;
#1781=CARTESIAN_POINT ( 'NONE',  ( 2.002547531651519996, -12.17374746633575988, -3.242439124566779185 ) ) ;
#1783=AXIS2_PLACEMENT_3D ( 'NONE', #17178, #14226, #10108 ) ;
#1784=VERTEX_POINT ( 'NONE', #6794 ) ;
#1789=CARTESIAN_POINT ( 'NONE',  ( 1.845755665166724846, -3.386720041070645948, -11.97169564665394681 ) ) ;
#1792=CARTESIAN_POINT ( 'NONE',  ( 0.3132642857406528480, 13.72733058964895037, 0.5276792104582755938 ) ) ;
#1794=CARTESIAN_POINT ( 'NONE',  ( 16.56782317627811096, 0.005492611183758417011, 0.008141063682853501640 ) ) ;
#1796=CARTESIAN_POINT ( 'NONE',  ( 1.847372867223025628, 12.44269075185938789, 0.1054171785006922379 ) ) ;
#1798=CARTESIAN_POINT ( 'NONE',  ( 1.562796894703937678, 0.000000000000000000, -12.15840553252917289 ) ) ;
#1801=CARTESIAN_POINT ( 'NONE',  ( 0.3145729642390391878, -8.321438378985172690, -10.93201268464381748 ) ) ;
#1804=EDGE_CURVE ( 'NONE', #14815, #17303, #10104, .T. ) ;
#1815=LINE ( 'NONE', #382, #16634 ) ;
#1819=CARTESIAN_POINT ( 'NONE',  ( 0.4754618798421162973, 12.98792082933644743, 5.007009103465295929 ) ) ;
#1822=CARTESIAN_POINT ( 'NONE',  ( 16.56753206892534891, 0.008490833999798920451, 0.004253784598196212220 ) ) ;
#1823=EDGE_LOOP ( 'NONE', ( #3640, #8517, #8869, #3051 ) ) ;
#1825=EDGE_CURVE ( 'NONE', #16257, #13262, #3510, .T. ) ;
#1830=ORIENTED_EDGE ( 'NONE', *, *, #6341, .T. ) ;
#1833=B_SPLINE_CURVE_WITH_KNOTS ( 'NONE', 3,
 ( #7807, #12198, #3583, #18023, #15152, #4927 ),
 .UNSPECIFIED., .F., .F.,
 ( 4, 2, 4 ),
 ( 4.269227611140977934E-17, 0.0002014099069817279985, 0.0004028198139634133336 ),
 .UNSPECIFIED. ) ;
#1842=CARTESIAN_POINT ( 'NONE',  ( 16.56753206892534891, -0.009389754735542257466, -0.001421777558675915579 ) ) ;
#1846=CARTESIAN_POINT ( 'NONE',  ( 1.342453679581834924, -12.51077660954471504, 7.902645620902405632 ) ) ;
#1851=ORIENTED_EDGE ( 'NONE', *, *, #13046, .F. ) ;
#1857=AXIS2_PLACEMENT_3D ( 'NONE', #13320, #13613, #18017 ) ;
#1860=VERTEX_POINT ( 'NONE', #9746 ) ;
#1864=DIRECTION ( 'NONE',  ( 0.7635533937278214944, -0.6204116510013502062, 0.1790966170213858510 ) ) ;
#1865=CARTESIAN_POINT ( 'NONE',  ( 0.3720661004400040439, -13.79610186261030513, 0.7231997263364323691 ) ) ;
#1874=CARTESIAN_POINT ( 'NONE',  ( 1.847380140988740260, 7.224522571381473135, -10.13114603776188893 ) ) ;
#1878=CARTESIAN_POINT ( 'NONE',  ( 16.56872352241294521, -0.01027347319884365333, -0.001821578298043897851 ) ) ;
#1879=EDGE_LOOP ( 'NONE', ( #6954, #17432, #9993, #15185 ) ) ;
#1880=ORIENTED_EDGE ( 'NONE', *, *, #10677, .F. ) ;
#1884=( BOUNDED_SURFACE ( )  B_SPLINE_SURFACE ( 3, 1, ( 
 ( #2159, #7997 ),
 ( #11046, #18206 ),
 ( #10955, #16773 ),
 ( #12466, #18296 ) ),
 .UNSPECIFIED., .F., .F., .T. ) 
 B_SPLINE_SURFACE_WITH_KNOTS ( ( 4, 4 ),
 ( 2, 2 ),
 ( 0.000000000000000000, 1.000000000000000000 ),
 ( 0.000000000000000000, 1.000000000000000000 ),
 .UNSPECIFIED. ) 
 GEOMETRIC_REPRESENTATION_ITEM ( )  RATIONAL_B_SPLINE_SURFACE ( (
 ( 1.000000000000000000, 1.000000000000000000),
 ( 0.9933953342250438912, 0.8357391271907739227),
 ( 0.9933953342250438912, 0.8357391271907739227),
 ( 1.000000000000000000, 1.000000000000000000) ) ) 
 REPRESENTATION_ITEM ( '' )  SURFACE ( )  );
#1885=CARTESIAN_POINT ( 'NONE',  ( 2.002547531651519996, -12.17374746633580784, 3.242439124566603326 ) ) ;
#1887=CARTESIAN_POINT ( 'NONE',  ( 2.353870697619111052, -12.05847592522640355, -4.720869121224258613 ) ) ;
#1892=ADVANCED_FACE ( 'NONE', ( #11377 ), #3862, .F. ) ;
#1901=ORIENTED_EDGE ( 'NONE', *, *, #12678, .F. ) ;
#1902=VERTEX_POINT ( 'NONE', #1430 ) ;
#1906=DIRECTION ( 'NONE',  ( 0.000000000000000000, 0.000000000000000000, 1.000000000000000000 ) ) ;
#1911=ORIENTED_EDGE ( 'NONE', *, *, #824, .F. ) ;
#1914=EDGE_CURVE ( 'NONE', #7670, #5120, #11272, .T. ) ;
#1918=CARTESIAN_POINT ( 'NONE',  ( 1.847168016377980670, -9.955470380986684020, 7.464000291196382086 ) ) ;
#1922=B_SPLINE_CURVE_WITH_KNOTS ( 'NONE', 3,
 ( #18737, #2581, #1252, #15875, #17121, #4029 ),
 .UNSPECIFIED., .F., .F.,
 ( 4, 2, 4 ),
 ( 0.000000000000000000, 0.001657017934711440188, 0.003314035869422880375 ),
 .UNSPECIFIED. ) ;
#1925=ORIENTED_EDGE ( 'NONE', *, *, #9239, .T. ) ;
#1927=CARTESIAN_POINT ( 'NONE',  ( 1.254255976357533831, -13.61551404021209777, -5.487601330835152780 ) ) ;
#1934=DIRECTION ( 'NONE',  ( -1.000000000000000000, -0.000000000000000000, -0.000000000000000000 ) ) ;
#1940=B_SPLINE_CURVE_WITH_KNOTS ( 'NONE', 3,
 ( #3691, #6667, #13821, #4948, #12480, #9246 ),
 .UNSPECIFIED., .F., .F.,
 ( 4, 2, 4 ),
 ( 4.192373019364431701E-17, 0.0002014099069817294621, 0.0004028198139634169657 ),
 .UNSPECIFIED. ) ;
#1945=FACE_OUTER_BOUND ( 'NONE', #8653, .T. ) ;
#1948=CARTESIAN_POINT ( 'NONE',  ( 3.950837973638675393, 10.05648675950126325, 10.51028938476221342 ) ) ;
#1950=CARTESIAN_POINT ( 'NONE',  ( 0.3142014840576534684, -4.608051180497015231, 12.94260032291127160 ) ) ;
#1951=CARTESIAN_POINT ( 'NONE',  ( 2.697797270744666243, -13.26309265156976558, -0.9169917281808652731 ) ) ;
#1956=ORIENTED_EDGE ( 'NONE', *, *, #18463, .T. ) ;
#1962=CARTESIAN_POINT ( 'NONE',  ( 0.4862570985993235340, 10.79774104611385965, -8.769551628660616771 ) ) ;
#1968=CARTESIAN_POINT ( 'NONE',  ( 2.636624412717140764, -2.862162146982851763, -15.80357026013259514 ) ) ;
#1969=CARTESIAN_POINT ( 'NONE',  ( 0.3150692679895976678, 7.951395415075086959, 11.20465057551027854 ) ) ;
#1972=CARTESIAN_POINT ( 'NONE',  ( 2.636624412716062960, 6.973567714909310489, -14.46769361191320868 ) ) ;
#1974=ORIENTED_EDGE ( 'NONE', *, *, #2782, .F. ) ;
#1981=CARTESIAN_POINT ( 'NONE',  ( 1.846138399168762101, 0.4167076046095548603, 12.43476674860266762 ) ) ;
#1982=CARTESIAN_POINT ( 'NONE',  ( 1.845756295923360435, -7.694561132136879422, -9.776763338604684606 ) ) ;
#1983=CARTESIAN_POINT ( 'NONE',  ( 3.950837973638668288, 14.41405733518061716, 1.958075594453843493 ) ) ;
#1987=CARTESIAN_POINT ( 'NONE',  ( 0.3137051932979757485, -11.37800749014125223, -7.698472063774596030 ) ) ;
#1993=CARTESIAN_POINT ( 'NONE',  ( 16.56753206892534891, 0.004368917149004243779, -0.008432171035096398468 ) ) ;
#1995=CARTESIAN_POINT ( 'NONE',  ( 16.57778382496167424, -0.006312874906843954532, -0.01354073047775891311 ) ) ;
#1996=ORIENTED_EDGE ( 'NONE', *, *, #4691, .T. ) ;
#1997=( BOUNDED_SURFACE ( )  B_SPLINE_SURFACE ( 3, 1, ( 
 ( #13516, #7993 ),
 ( #6548, #16402 ),
 ( #12369, #17930 ),
 ( #4925, #15048 ) ),
 .UNSPECIFIED., .F., .F., .T. ) 
 B_SPLINE_SURFACE_WITH_KNOTS ( ( 4, 4 ),
 ( 2, 2 ),
 ( 0.000000000000000000, 1.000000000000000000 ),
 ( 0.000000000000000000, 1.000000000000000000 ),
 .UNSPECIFIED. ) 
 GEOMETRIC_REPRESENTATION_ITEM ( )  RATIONAL_B_SPLINE_SURFACE ( (
 ( 1.000000000000000000, 1.000000000000000000),
 ( 0.9933953342250436691, 0.8357391271907733676),
 ( 0.9933953342250436691, 0.8357391271907733676),
 ( 1.000000000000000000, 1.000000000000000000) ) ) 
 REPRESENTATION_ITEM ( '' )  SURFACE ( )  );
#1998=EDGE_CURVE ( 'NONE', #9992, #11554, #4191, .T. ) ;
#2001=ORIENTED_EDGE ( 'NONE', *, *, #18463, .F. ) ;
#2007=CARTESIAN_POINT ( 'NONE',  ( 2.636624412714236865, 0.000000000000000000, 0.000000000000000000 ) ) ;
#2013=FACE_OUTER_BOUND ( 'NONE', #6659, .T. ) ;
#2018=CARTESIAN_POINT ( 'NONE',  ( 1.846138399168762101, 0.4167076046097279440, -12.43476674860266051 ) ) ;
#2020=CARTESIAN_POINT ( 'NONE',  ( 0.4862570985993235340, -10.79774104611379215, 8.769551628660700260 ) ) ;
#2021=CARTESIAN_POINT ( 'NONE',  ( 1.846822687350019754, 11.92063725419904152, -3.566003975885565946 ) ) ;
#2022=ORIENTED_EDGE ( 'NONE', *, *, #5052, .T. ) ;
#2024=EDGE_CURVE ( 'NONE', #913, #1072, #14198, .T. ) ;
#2025=EDGE_CURVE ( 'NONE', #18618, #16284, #1815, .T. ) ;
#2030=AXIS2_PLACEMENT_3D ( 'NONE', #15716, #11248, #17249 ) ;
#2032=CARTESIAN_POINT ( 'NONE',  ( 8.522092701127531811, 3.777034505568607425, -5.841710761610089619 ) ) ;
#2037=CARTESIAN_POINT ( 'NONE',  ( 1.845756295923360657, -6.920504327368265152, 10.33914852636102033 ) ) ;
#2044=CARTESIAN_POINT ( 'NONE',  ( 2.002547531651519996, -12.57989064830759141, -0.6781519942173057647 ) ) ;
#2053=ORIENTED_EDGE ( 'NONE', *, *, #4035, .F. ) ;
#2055=CARTESIAN_POINT ( 'NONE',  ( 16.56753206892534891, -0.006669401563385243120, -0.006760771273035091553 ) ) ;
#2064=CARTESIAN_POINT ( 'NONE',  ( 0.3142014840576501378, -0.3830336514509840029, 13.73311050063163918 ) ) ;
#2065=CARTESIAN_POINT ( 'NONE',  ( 8.438534575730034959, -3.845978796786076348, 5.688336279099031501 ) ) ;
#2067=CARTESIAN_POINT ( 'NONE',  ( 0.4754618798421162973, -5.007009103465343003, 12.98792082933642789 ) ) ;
#2068=CARTESIAN_POINT ( 'NONE',  ( 0.4385251269669946939, -11.63205320541528209, 7.540955776459703053 ) ) ;
#2071=CONICAL_SURFACE ( 'NONE', #231, 14.54644660717763927, 0.8559913436420816257 ) ;
#2072=CARTESIAN_POINT ( 'NONE',  ( 2.636624412715138366, -15.91454522070249311, -2.161493821597819665 ) ) ;
#2074=CARTESIAN_POINT ( 'NONE',  ( 1.861706995891676764, 12.44571539481144384, -0.5394761475746276957 ) ) ;
#2079=EDGE_CURVE ( 'NONE', #14201, #447, #9442, .T. ) ;
#2080=ORIENTED_EDGE ( 'NONE', *, *, #2600, .F. ) ;
#2082=ORIENTED_EDGE ( 'NONE', *, *, #1532, .F. ) ;
#2083=ORIENTED_EDGE ( 'NONE', *, *, #6251, .T. ) ;
#2089=CARTESIAN_POINT ( 'NONE',  ( 2.636624412715999011, 2.161493821598055920, -15.91454522070273647 ) ) ;
#2092=CARTESIAN_POINT ( 'NONE',  ( 0.3720661004400040439, 10.73619472937714825, -8.694226082900476271 ) ) ;
#2094=CARTESIAN_POINT ( 'NONE',  ( 3.353306896162455697, 3.007732942432417289, 13.62210141459496171 ) ) ;
#2096=VERTEX_POINT ( 'NONE', #16897 ) ;
#2099=VERTEX_POINT ( 'NONE', #6590 ) ;
#2103=CARTESIAN_POINT ( 'NONE',  ( 1.847461586945729595, -7.341074796295863791, -10.04711372545053116 ) ) ;
#2107=CARTESIAN_POINT ( 'NONE',  ( 1.959212340397967766, -0.6675998551412658522, 12.53706137681888677 ) ) ;
#2108=ADVANCED_FACE ( 'NONE', ( #5051 ), #5798, .F. ) ;
#2115=( BOUNDED_SURFACE ( )  B_SPLINE_SURFACE ( 3, 1, ( 
 ( #8381, #6856 ),
 ( #7050, #3707 ),
 ( #12770, #2445 ),
 ( #8295, #14110 ) ),
 .UNSPECIFIED., .F., .F., .T. ) 
 B_SPLINE_SURFACE_WITH_KNOTS ( ( 4, 4 ),
 ( 2, 2 ),
 ( 0.000000000000000000, 1.000000000000000000 ),
 ( 0.000000000000000000, 1.000000000000000000 ),
 .UNSPECIFIED. ) 
 GEOMETRIC_REPRESENTATION_ITEM ( )  RATIONAL_B_SPLINE_SURFACE ( (
 ( 1.000000000000000000, 1.000000000000000000),
 ( 0.9933953342250436691, 0.8357391271907733676),
 ( 0.9933953342250436691, 0.8357391271907733676),
 ( 1.000000000000000000, 1.000000000000000000) ) ) 
 REPRESENTATION_ITEM ( '' )  SURFACE ( )  );
#2116=ORIENTED_EDGE ( 'NONE', *, *, #13575, .T. ) ;
#2117=CARTESIAN_POINT ( 'NONE',  ( 1.342453679581834924, -11.38190519890860131, 9.456403821038760427 ) ) ;
#2121=CARTESIAN_POINT ( 'NONE',  ( 1.959283090834840646, -4.509128209890892691, -11.71721539537259282 ) ) ;
#2125=CARTESIAN_POINT ( 'NONE',  ( 0.4754618798421162973, 13.89949764182682657, -0.7484603771384912285 ) ) ;
#2126=CARTESIAN_POINT ( 'NONE',  ( 1.845756295923359769, -11.97166802574123423, -3.386818134580184658 ) ) ;
#2134=CARTESIAN_POINT ( 'NONE',  ( 2.747332970342022840, -16.12459247543624130, -2.705255688518015234 ) ) ;
#2136=CARTESIAN_POINT ( 'NONE',  ( 1.918921323896323639, 10.48468902844562578, -6.832782632379261756 ) ) ;
#2140=ORIENTED_EDGE ( 'NONE', *, *, #18386, .T. ) ;
#2141=CARTESIAN_POINT ( 'NONE',  ( 16.56872352241294521, -0.007512283835804365630, 0.007240717549633862542 ) ) ;
#2148=VERTEX_POINT ( 'NONE', #4366 ) ;
#2151=CARTESIAN_POINT ( 'NONE',  ( 3.950837973638675393, 6.888253895133479965, -12.81214529934967672 ) ) ;
#2152=CARTESIAN_POINT ( 'NONE',  ( 16.57210152137263393, 0.01214401161737623663, 0.008007331252333469568 ) ) ;
#2156=CARTESIAN_POINT ( 'NONE',  ( 16.56782317627811096, -0.009228812961908680612, 0.003357783021327786360 ) ) ;
#2157=CARTESIAN_POINT ( 'NONE',  ( 1.846138399168762101, 3.446241763653166590, -11.95493567637846866 ) ) ;
#2158=ADVANCED_FACE ( 'NONE', ( #18791 ), #2563, .T. ) ;
#2159=CARTESIAN_POINT ( 'NONE',  ( 16.56872352241294521, 0.009207754980063749192, 0.004907101719994666836 ) ) ;
#2166=ORIENTED_EDGE ( 'NONE', *, *, #8213, .T. ) ;
#2168=ORIENTED_EDGE ( 'NONE', *, *, #8921, .F. ) ;
#2170=CARTESIAN_POINT ( 'NONE',  ( 0.3308579732647040639, 4.812490080619379995, -12.88563776947740358 ) ) ;
#2175=CARTESIAN_POINT ( 'NONE',  ( 2.353870697619111496, -10.90705766126224674, 6.980654702310806314 ) ) ;
#2176=CARTESIAN_POINT ( 'NONE',  ( 3.377929128793398128, -13.64476897106782083, -3.070552481925011179 ) ) ;
#2177=ADVANCED_FACE ( 'NONE', ( #9904 ), #7787, .F. ) ;
#2181=ORIENTED_EDGE ( 'NONE', *, *, #18056, .F. ) ;
#2182=ORIENTED_EDGE ( 'NONE', *, *, #11569, .F. ) ;
#2185=EDGE_CURVE ( 'NONE', #3512, #10137, #18159, .T. ) ;
#2189=CARTESIAN_POINT ( 'NONE',  ( 1.846822687350018866, 12.43915556955403900, 0.2922081769260583273 ) ) ;
#2190=CARTESIAN_POINT ( 'NONE',  ( 0.4862570985993252548, 13.44146924561381162, 3.580942890621718888 ) ) ;
#2192=CARTESIAN_POINT ( 'NONE',  ( 1.846138399168762101, -0.4167076046096411246, 12.43476674860266407 ) ) ;
#2196=DIRECTION ( 'NONE',  ( 0.000000000000000000, 0.000000000000000000, 1.000000000000000000 ) ) ;
#2201=LINE ( 'NONE', #677, #9660 ) ;
#2202=ORIENTED_EDGE ( 'NONE', *, *, #15444, .T. ) ;
#2206=EDGE_CURVE ( 'NONE', #6765, #5117, #17416, .T. ) ;
#2207=ORIENTED_EDGE ( 'NONE', *, *, #12285, .T. ) ;
#2208=CARTESIAN_POINT ( 'NONE',  ( 16.56753206892534891, -0.004253784598196824578, -0.008490833999797990639 ) ) ;
#2210=ORIENTED_EDGE ( 'NONE', *, *, #8999, .T. ) ;
#2211=CARTESIAN_POINT ( 'NONE',  ( 1.846613052777651198, -7.035606253495386930, 10.26230975746757146 ) ) ;
#2215=CIRCLE ( 'NONE', #4662, 14.54644660717763927 ) ;
#2221=AXIS2_PLACEMENT_3D ( 'NONE', #11734, #10493, #3208 ) ;
#2222=EDGE_LOOP ( 'NONE', ( #7269, #10524, #13507, #15791 ) ) ;
#2223=CARTESIAN_POINT ( 'NONE',  ( 3.353306896162455697, 12.78841260990237672, 5.573563251762143622 ) ) ;
#2228=DIRECTION ( 'NONE',  ( 0.7635533937278216055, 0.5095610256143827677, 0.3966532189476653092 ) ) ;
#2235=B_SPLINE_CURVE_WITH_KNOTS ( 'NONE', 3,
 ( #9726, #16810, #8125, #16724, #15460, #850 ),
 .UNSPECIFIED., .F., .F.,
 ( 4, 2, 4 ),
 ( 4.072016404827931570E-17, 0.0002014099069817292182, 0.0004028198139634177246 ),
 .UNSPECIFIED. ) ;
#2237=CARTESIAN_POINT ( 'NONE',  ( 16.57210152137263393, -0.01214401161737523396, 0.008007331252332839863 ) ) ;
#2238=DIRECTION ( 'NONE',  ( 0.000000000000000000, 0.000000000000000000, 1.000000000000000000 ) ) ;
#2239=CARTESIAN_POINT ( 'NONE',  ( 1.846524061778019199, 7.597197846158221246, -9.853584647934303220 ) ) ;
#2240=DIRECTION ( 'NONE',  ( -0.7561779333270775005, -0.6106991889125072959, 0.2350349629540161855 ) ) ;
#2248=EDGE_CURVE ( 'NONE', #17773, #4406, #6700, .T. ) ;
#2250=ORIENTED_EDGE ( 'NONE', *, *, #5310, .F. ) ;
#2252=CARTESIAN_POINT ( 'NONE',  ( 1.918918678667045130, -9.738328798462433156, 7.860057224348805605 ) ) ;
#2258=CARTESIAN_POINT ( 'NONE',  ( 16.56872352241294521, -0.01027347319884365333, -0.001821578298043897851 ) ) ;
#2260=DIRECTION ( 'NONE',  ( -0.7561779333270775005, -0.03481510524964337439, -0.6534392409364823129 ) ) ;
#2271=CARTESIAN_POINT ( 'NONE',  ( 16.56753206892534891, 0.006669401563384923064, -0.006760771273036194837 ) ) ;
#2281=B_SPLINE_CURVE_WITH_KNOTS ( 'NONE', 3,
 ( #5850, #17521, #4430, #18764, #1653, #16186 ),
 .UNSPECIFIED., .F., .F.,
 ( 4, 2, 4 ),
 ( 1.748223473168675632E-18, 0.0002017457492448088553, 0.0004034914984896159759 ),
 .UNSPECIFIED. ) ;
#2287=VERTEX_POINT ( 'NONE', #16321 ) ;
#2288=CARTESIAN_POINT ( 'NONE',  ( 16.56782317627811096, -0.0003415813796015412622, -0.009814734722106366327 ) ) ;
#2291=CARTESIAN_POINT ( 'NONE',  ( 1.846138399168762101, -0.4167076046096411246, 12.43476674860266407 ) ) ;
#2301=CARTESIAN_POINT ( 'NONE',  ( 2.636624412714236865, 0.000000000000000000, 0.000000000000000000 ) ) ;
#2302=AXIS2_PLACEMENT_3D ( 'NONE', #14884, #14687, #4470 ) ;
#2305=CARTESIAN_POINT ( 'NONE',  ( 0.8740779401510752056, 3.609949156401575543, -13.83508928787453662 ) ) ;
#2311=AXIS2_PLACEMENT_3D ( 'NONE', #17021, #3920, #11247 ) ;
#2313=CARTESIAN_POINT ( 'NONE',  ( 2.697797270744668463, 12.33058466479268844, 4.970631985779629503 ) ) ;
#2314=CARTESIAN_POINT ( 'NONE',  ( 0.3151926232592538457, -4.318679262939536301, -13.04305446098360122 ) ) ;
#2324=CARTESIAN_POINT ( 'NONE',  ( 0.3307726912345200776, -7.596084275798974161, 11.46720933246395369 ) ) ;
#2338=VECTOR ( 'NONE', #16459, 1000.000000000000227 ) ;
#2339=VERTEX_POINT ( 'NONE', #10387 ) ;
#2340=VERTEX_POINT ( 'NONE', #10291 ) ;
#2352=CARTESIAN_POINT ( 'NONE',  ( 0.4754618798421162973, -10.80499583390506224, -8.775436892861234739 ) ) ;
#2355=CARTESIAN_POINT ( 'NONE',  ( 3.950837973638675393, -13.10350451991835818, -6.316429227969608817 ) ) ;
#2358=ORIENTED_EDGE ( 'NONE', *, *, #18781, .F. ) ;
#2362=CARTESIAN_POINT ( 'NONE',  ( 2.353870697619111496, -0.7635393531607235218, 12.92712089195302561 ) ) ;
#2373=CARTESIAN_POINT ( 'NONE',  ( 3.074695600508759785, 15.30693405987895694, 2.772091048737280072 ) ) ;
#2374=CARTESIAN_POINT ( 'NONE',  ( 3.950837973638675393, -14.31366178983251380, -2.591948120961955926 ) ) ;
#2379=ORIENTED_EDGE ( 'NONE', *, *, #351, .T. ) ;
#2383=ORIENTED_EDGE ( 'NONE', *, *, #18035, .F. ) ;
#2393=CARTESIAN_POINT ( 'NONE',  ( 3.377929128793399016, 10.50432311212916225, -9.234024516648208447 ) ) ;
#2398=CARTESIAN_POINT ( 'NONE',  ( 0.3137051932979757485, -11.37800749014125223, -7.698472063774596030 ) ) ;
#2399=CARTESIAN_POINT ( 'NONE',  ( 1.918921323896324083, 4.466082741316370175, -11.69058285425785648 ) ) ;
#2400=EDGE_CURVE ( 'NONE', #5315, #2529, #4631, .T. ) ;
#2403=LINE ( 'NONE', #3749, #1092 ) ;
#2406=CARTESIAN_POINT ( 'NONE',  ( 1.845756295923363099, -0.4783934145701149721, -12.43231724724606835 ) ) ;
#2408=CARTESIAN_POINT ( 'NONE',  ( 2.002547531651519996, -11.75462648437105173, 4.532360870844282630 ) ) ;
#2411=CARTESIAN_POINT ( 'NONE',  ( 1.845755665166725068, 12.43231320373361193, 0.4784952423728983106 ) ) ;
#2412=AXIS2_PLACEMENT_3D ( 'NONE', #1147, #1042, #8054 ) ;
#2413=DIRECTION ( 'NONE',  ( -1.000000000000000000, -0.000000000000000000, -0.000000000000000000 ) ) ;
#2414=CARTESIAN_POINT ( 'NONE',  ( 2.002547531651519996, 0.6781519942173496185, -12.57989064830758785 ) ) ;
#2423=CARTESIAN_POINT ( 'NONE',  ( 1.562796894703937678, 0.000000000000000000, 0.000000000000000000 ) ) ;
#2424=ORIENTED_EDGE ( 'NONE', *, *, #17068, .T. ) ;
#2429=EDGE_CURVE ( 'NONE', #10554, #18537, #299, .T. ) ;
#2433=CARTESIAN_POINT ( 'NONE',  ( 16.56753206892534891, 0.009389754735542247058, 0.001421777558675981282 ) ) ;
#2442=EDGE_CURVE ( 'NONE', #5851, #5315, #17628, .T. ) ;
#2445=CARTESIAN_POINT ( 'NONE',  ( 0.3720661004400037664, 7.524064345033464107, 11.58636699658217672 ) ) ;
#2456=ORIENTED_EDGE ( 'NONE', *, *, #6278, .T. ) ;
#2459=CARTESIAN_POINT ( 'NONE',  ( 1.342453679581834924, -13.74702459364880269, -5.476372339890162699 ) ) ;
#2466=CARTESIAN_POINT ( 'NONE',  ( 1.847247051441591958, -3.685275815977108405, -11.88474976472816103 ) ) ;
#2467=DIRECTION ( 'NONE',  ( 0.7635533937278216055, -0.2197766120036547532, 0.6071939193889553943 ) ) ;
#2470=CARTESIAN_POINT ( 'NONE',  ( 0.4754618798421162973, 13.45049478164060019, 3.583352865732715387 ) ) ;
#2472=CARTESIAN_POINT ( 'NONE',  ( 1.846524061778018977, -7.597197846158149304, 9.853584647934361840 ) ) ;
#2476=CARTESIAN_POINT ( 'NONE',  ( 1.861706995891668770, 7.751853334747318414, 9.751699138048461890 ) ) ;
#2477=CARTESIAN_POINT ( 'NONE',  ( 8.438534575730034959, -1.899950616255234870, 6.598402093327873530 ) ) ;
#2478=VECTOR ( 'NONE', #4601, 1000.000000000000114 ) ;
#2481=VERTEX_POINT ( 'NONE', #14291 ) ;
#2484=CARTESIAN_POINT ( 'NONE',  ( 0.3137051932979792457, -3.805684345189695783, -13.20008686438109891 ) ) ;
#2485=VERTEX_POINT ( 'NONE', #1192 ) ;
#2494=CARTESIAN_POINT ( 'NONE',  ( 1.254255976357135038, 3.563435620217683120, 14.24071337840730322 ) ) ;
#2495=CARTESIAN_POINT ( 'NONE',  ( 2.636624412717099908, 15.80357026013547816, -2.862162146981609201 ) ) ;
#2499=CARTESIAN_POINT ( 'NONE',  ( 0.3058872367615230181, 7.578326039752771415, -11.46514199369349818 ) ) ;
#2500=CARTESIAN_POINT ( 'NONE',  ( 0.3095370825347234511, -12.91933430393604532, -4.681152801286298626 ) ) ;
#2505=EDGE_CURVE ( 'NONE', #14390, #5155, #11303, .T. ) ;
#2514=CARTESIAN_POINT ( 'NONE',  ( 8.522092701127531811, 5.397361180353144050, 4.388629235579598387 ) ) ;
#2517=DIRECTION ( 'NONE',  ( -0.7561779333270775005, 0.6534392409364818688, -0.03481510524965020920 ) ) ;
#2521=CARTESIAN_POINT ( 'NONE',  ( 2.123976203522053297, 1.531817366691969884, -15.54801196254785189 ) ) ;
#2523=AXIS2_PLACEMENT_3D ( 'NONE', #14864, #2992, #16408 ) ;
#2524=EDGE_CURVE ( 'NONE', #11551, #1902, #9126, .T. ) ;
#2526=B_SPLINE_CURVE_WITH_KNOTS ( 'NONE', 3,
 ( #5948, #7788, #703, #419, #18097, #6247 ),
 .UNSPECIFIED., .F., .F.,
 ( 4, 2, 4 ),
 ( 0.000000000000000000, 0.001656992708823057468, 0.003313985417646114935 ),
 .UNSPECIFIED. ) ;
#2529=VERTEX_POINT ( 'NONE', #17634 ) ;
#2530=ORIENTED_EDGE ( 'NONE', *, *, #14186, .T. ) ;
#2533=CARTESIAN_POINT ( 'NONE',  ( 0.3095370825347234511, 13.73357284481724783, 0.4597470195090685441 ) ) ;
#2536=CARTESIAN_POINT ( 'NONE',  ( 0.3058872367615226295, 8.562166468153870724, -10.75034008168906396 ) ) ;
#2544=CARTESIAN_POINT ( 'NONE',  ( 0.3307726912345222980, 4.812300915532974344, 12.88561780039860416 ) ) ;
#2546=CARTESIAN_POINT ( 'NONE',  ( 1.847412631396500693, -3.886120457021478902, 11.82061107079963413 ) ) ;
#2547=EDGE_CURVE ( 'NONE', #15093, #13901, #16786, .T. ) ;
#2552=CARTESIAN_POINT ( 'NONE',  ( 1.254255976357310010, 14.64488542023430817, 1.011593778944276822 ) ) ;
#2554=DIRECTION ( 'NONE',  ( -1.000000000000000000, -0.000000000000000000, -0.000000000000000000 ) ) ;
#2559=CARTESIAN_POINT ( 'NONE',  ( 1.847461586945730261, -7.286856109515127855, 10.08650590720933771 ) ) ;
#2562=CARTESIAN_POINT ( 'NONE',  ( 0.3150686449036049219, -13.11344473514185971, -4.099563462784791668 ) ) ;
#2563=CONICAL_SURFACE ( 'NONE', #5932, 14.54644660717763927, 0.8559913436420816257 ) ;
#2570=ADVANCED_FACE ( 'NONE', ( #11802 ), #7909, .F. ) ;
#2573=CARTESIAN_POINT ( 'NONE',  ( 2.002547531651520885, 10.57595306287292480, 6.845637710436228929 ) ) ;
#2574=ORIENTED_EDGE ( 'NONE', *, *, #15665, .F. ) ;
#2575=CARTESIAN_POINT ( 'NONE',  ( 16.56753206892534891, 0.009389754735542245323, 0.001421777558675984534 ) ) ;
#2576=CARTESIAN_POINT ( 'NONE',  ( 2.636624412715137922, -7.605649742761668719, 14.14563173255331741 ) ) ;
#2578=ORIENTED_EDGE ( 'NONE', *, *, #950, .T. ) ;
#2579=CARTESIAN_POINT ( 'NONE',  ( 0.3150686449036048109, 4.099563462784836965, -13.11344473514184372 ) ) ;
#2581=CARTESIAN_POINT ( 'NONE',  ( 0.8740779401510756497, -5.211551231203870316, -13.31469722824378721 ) ) ;
#2590=CARTESIAN_POINT ( 'NONE',  ( 1.846955891736114852, -9.909315188408097441, 7.525208385419928092 ) ) ;
#2597=CARTESIAN_POINT ( 'NONE',  ( 1.847426409206469611, 0.06227732482722434654, 12.44303504652092762 ) ) ;
#2598=CARTESIAN_POINT ( 'NONE',  ( 2.636624412716062071, -14.14563173255412742, -7.605649742760987486 ) ) ;
#2600=EDGE_CURVE ( 'NONE', #9475, #15162, #14038, .T. ) ;
#2606=EDGE_LOOP ( 'NONE', ( #448, #11624, #6831, #11583 ) ) ;
#2614=CARTESIAN_POINT ( 'NONE',  ( 16.56782317627811096, -0.005492611183758475124, -0.008141063682853461742 ) ) ;
#2620=CARTESIAN_POINT ( 'NONE',  ( 16.57778382496167424, 0.01466529584256671612, -0.002851818597093459199 ) ) ;
#2623=EDGE_CURVE ( 'NONE', #13434, #3961, #17948, .T. ) ;
#2626=ORIENTED_EDGE ( 'NONE', *, *, #18781, .T. ) ;
#2629=VECTOR ( 'NONE', #12719, 1000.000000000000000 ) ;
#2630=CARTESIAN_POINT ( 'NONE',  ( 2.697797270744669795, 12.89731672021094511, -3.226410068829295597 ) ) ;
#2631=CARTESIAN_POINT ( 'NONE',  ( 16.56872352241294521, 0.004907101719994633009, -0.009207754980063766539 ) ) ;
#2633=EDGE_LOOP ( 'NONE', ( #1155, #10769, #13128, #16470 ) ) ;
#2638=CARTESIAN_POINT ( 'NONE',  ( 16.56872352241294521, -0.007512283835805501873, -0.007240717549633963156 ) ) ;
#2640=CARTESIAN_POINT ( 'NONE',  ( 0.3145734862173242274, -11.29227530924451273, 7.825584895511488170 ) ) ;
#2645=CARTESIAN_POINT ( 'NONE',  ( 0.3137051932979775248, -12.91601973349273891, 4.679953077377436266 ) ) ;
#2658=DIRECTION ( 'NONE',  ( -1.000000000000000000, -0.000000000000000000, -0.000000000000000000 ) ) ;
#2663=CARTESIAN_POINT ( 'NONE',  ( 8.522092701127531811, 0.3779863304871219909, 6.946128462138597470 ) ) ;
#2666=CARTESIAN_POINT ( 'NONE',  ( 0.3137051932979809665, -3.805684345189881856, 13.20008686438104739 ) ) ;
#2670=CARTESIAN_POINT ( 'NONE',  ( 1.977436885026095270, -10.21547824869579202, 11.52792723756318694 ) ) ;
#2673=EDGE_LOOP ( 'NONE', ( #12168, #18642, #6177, #14113, #15562, #12382, #1974, #16845, #13432, #10639, #9231, #4809, #18735, #17944, #10207, #18283, #18032, #11645, #6230, #9875, #7360, #7957, #15401, #1402, #14920, #10737, #6933, #9733, #2456, #16872, #1129, #17055, #14894, #17571, #1925, #11671, #10678, #15877, #17549, #12972, #4481, #2083, #9858, #5582, #8820, #12181, #10447, #12950, #7750, #2202, #1536, #2831, #12949, #12142, #2685, #8756, #5153, #2022, #16007, #15721, #2168, #10039, #3661, #16623 ) ) ;
#2674=CARTESIAN_POINT ( 'NONE',  ( 8.522092701127531811, 1.786985377232127137, -6.722964936702079619 ) ) ;
#2676=EDGE_LOOP ( 'NONE', ( #1200, #12787 ) ) ;
#2678=EDGE_CURVE ( 'NONE', #3393, #13262, #16400, .T. ) ;
#2682=CARTESIAN_POINT ( 'NONE',  ( 8.438534575730034959, -0.2320579683289648587, -6.862570336891078426 ) ) ;
#2683=CARTESIAN_POINT ( 'NONE',  ( 1.861628059977341154, 7.751680370225533245, -9.751736252960284901 ) ) ;
#2684=CARTESIAN_POINT ( 'NONE',  ( 0.000000000000000000, 0.000000000000000000, 0.000000000000000000 ) ) ;
#2685=ORIENTED_EDGE ( 'NONE', *, *, #17500, .F. ) ;
#2687=CARTESIAN_POINT ( 'NONE',  ( 3.074695600507123761, 2.093687500612191776, -15.41438262616238575 ) ) ;
#2688=( BOUNDED_SURFACE ( )  B_SPLINE_SURFACE ( 3, 1, ( 
 ( #15239, #9220 ),
 ( #2152, #10951 ),
 ( #14952, #12279 ),
 ( #7710, #6263 ) ),
 .UNSPECIFIED., .F., .F., .T. ) 
 B_SPLINE_SURFACE_WITH_KNOTS ( ( 4, 4 ),
 ( 2, 2 ),
 ( 0.000000000000000000, 1.000000000000000000 ),
 ( 0.000000000000000000, 1.000000000000000000 ),
 .UNSPECIFIED. ) 
 GEOMETRIC_REPRESENTATION_ITEM ( )  RATIONAL_B_SPLINE_SURFACE ( (
 ( 1.000000000000000000, 1.000000000000000000),
 ( 0.7792777138730160313, 0.9689936506012927220),
 ( 0.7792777138730160313, 0.9689936506012927220),
 ( 1.000000000000000000, 1.000000000000000000) ) ) 
 REPRESENTATION_ITEM ( '' )  SURFACE ( )  );
#2693=DIRECTION ( 'NONE',  ( 0.000000000000000000, 0.000000000000000000, 1.000000000000000000 ) ) ;
#2696=ORIENTED_EDGE ( 'NONE', *, *, #17019, .T. ) ;
#2699=ORIENTED_EDGE ( 'NONE', *, *, #1825, .F. ) ;
#2705=CARTESIAN_POINT ( 'NONE',  ( 1.846613052777651198, -10.26230975746754659, -7.035606253495426898 ) ) ;
#2708=CARTESIAN_POINT ( 'NONE',  ( 0.4862570985993235340, 13.89016912371017476, -0.7479633556562934604 ) ) ;
#2715=CARTESIAN_POINT ( 'NONE',  ( 16.58200780006414732, -0.01115192838421470017, 0.0006320991582340292937 ) ) ;
#2716=FACE_OUTER_BOUND ( 'NONE', #2222, .T. ) ;
#2720=ORIENTED_EDGE ( 'NONE', *, *, #7923, .F. ) ;
#2721=LINE ( 'NONE', #18787, #9566 ) ;
#2722=CARTESIAN_POINT ( 'NONE',  ( 2.636624412714756005, -2.161493821597335607, 15.91454522070219113 ) ) ;
#2726=LINE ( 'NONE', #11446, #15668 ) ;
#2727=EDGE_CURVE ( 'NONE', #5155, #3, #5828, .T. ) ;
#2730=CARTESIAN_POINT ( 'NONE',  ( 3.512766787570765548, -13.25664064834477429, 7.127386085302765295 ) ) ;
#2736=VECTOR ( 'NONE', #16072, 1000.000000000000114 ) ;
#2741=ORIENTED_EDGE ( 'NONE', *, *, #15320, .F. ) ;
#2747=ORIENTED_EDGE ( 'NONE', *, *, #16564, .F. ) ;
#2751=CARTESIAN_POINT ( 'NONE',  ( 2.747332970342022840, 16.12459247543626617, 2.705255688517901103 ) ) ;
#2756=EDGE_CURVE ( 'NONE', #11554, #16490, #4940, .T. ) ;
#2757=CARTESIAN_POINT ( 'NONE',  ( 16.56679352167444819, -0.004277682826582317882, 0.008252760440870482092 ) ) ;
#2766=CARTESIAN_POINT ( 'NONE',  ( 3.074695600507241444, -15.30693405987796751, 2.772091048739207864 ) ) ;
#2767=B_SPLINE_CURVE_WITH_KNOTS ( 'NONE', 3,
 ( #15742, #6971, #6868, #7152, #15557, #5428 ),
 .UNSPECIFIED., .F., .F.,
 ( 4, 2, 4 ),
 ( 4.240893905418535831E-17, 0.0002014099069817285406, 0.0004028198139634146346 ),
 .UNSPECIFIED. ) ;
#2774=CARTESIAN_POINT ( 'NONE',  ( 1.845756295923359325, 11.97166802574126088, 3.386818134580099837 ) ) ;
#2775=ORIENTED_EDGE ( 'NONE', *, *, #2206, .F. ) ;
#2779=CARTESIAN_POINT ( 'NONE',  ( 0.3720661004400040439, -0.7231997263363842965, -13.79610186261031046 ) ) ;
#2781=CARTESIAN_POINT ( 'NONE',  ( 3.950837973638668288, 0.000000000000000000, 0.000000000000000000 ) ) ;
#2782=EDGE_CURVE ( 'NONE', #4341, #11242, #10600, .T. ) ;
#2783=VERTEX_POINT ( 'NONE', #2495 ) ;
#2784=CARTESIAN_POINT ( 'NONE',  ( 0.3137051932979792457, 11.37800749014142276, -7.698472063774345564 ) ) ;
#2786=ORIENTED_EDGE ( 'NONE', *, *, #6420, .T. ) ;
#2788=CARTESIAN_POINT ( 'NONE',  ( 2.636624412715362631, -15.80357026013197519, 2.862162146984090327 ) ) ;
#2792=ORIENTED_EDGE ( 'NONE', *, *, #16862, .F. ) ;
#2793=CARTESIAN_POINT ( 'NONE',  ( 0.4862570985993235340, 8.769551628660735787, 10.79774104611376373 ) ) ;
#2796=CARTESIAN_POINT ( 'NONE',  ( 0.3170788640506440603, 0.1533108587038062576, -13.74111462631963398 ) ) ;
#2797=( BOUNDED_SURFACE ( )  B_SPLINE_SURFACE ( 3, 1, ( 
 ( #1570, #14752 ),
 ( #11801, #3377 ),
 ( #7413, #5960 ),
 ( #17633, #1663 ) ),
 .UNSPECIFIED., .F., .F., .T. ) 
 B_SPLINE_SURFACE_WITH_KNOTS ( ( 4, 4 ),
 ( 2, 2 ),
 ( 0.000000000000000000, 1.000000000000000000 ),
 ( 0.000000000000000000, 1.000000000000000000 ),
 .UNSPECIFIED. ) 
 GEOMETRIC_REPRESENTATION_ITEM ( )  RATIONAL_B_SPLINE_SURFACE ( (
 ( 1.000000000000000000, 1.000000000000000000),
 ( 0.7792777138730158093, 0.9689936506012928330),
 ( 0.7792777138730158093, 0.9689936506012928330),
 ( 1.000000000000000000, 1.000000000000000000) ) ) 
 REPRESENTATION_ITEM ( '' )  SURFACE ( )  );
#2799=CARTESIAN_POINT ( 'NONE',  ( 1.845756295923359547, 4.296776483139476355, 11.67600463554274626 ) ) ;
#2808=ORIENTED_EDGE ( 'NONE', *, *, #3930, .T. ) ;
#2810=CARTESIAN_POINT ( 'NONE',  ( 3.950837973638676281, 13.10350451991840615, 6.316429227969512894 ) ) ;
#2811=CARTESIAN_POINT ( 'NONE',  ( 16.56753206892534891, -0.008432171035096417550, 0.004368917149005420789 ) ) ;
#2815=CARTESIAN_POINT ( 'NONE',  ( 3.512766787570727356, 6.535475144497194577, -13.55823433651945464 ) ) ;
#2817=CARTESIAN_POINT ( 'NONE',  ( 16.56822296793089322, -0.005339139727952723832, 0.008619100080559757848 ) ) ;
#2818=CARTESIAN_POINT ( 'NONE',  ( 0.3145729642390390768, -10.93201268464378373, 8.321438378985218876 ) ) ;
#2820=CARTESIAN_POINT ( 'NONE',  ( 16.57778382496167424, -0.001819584982832002807, 0.01482878558584568851 ) ) ;
#2823=CARTESIAN_POINT ( 'NONE',  ( 1.847168016377981781, -3.666915430942684129, 11.89018175117593934 ) ) ;
#2825=ORIENTED_EDGE ( 'NONE', *, *, #13866, .F. ) ;
#2826=ORIENTED_EDGE ( 'NONE', *, *, #12336, .F. ) ;
#2828=ORIENTED_EDGE ( 'NONE', *, *, #509, .F. ) ;
#2831=ORIENTED_EDGE ( 'NONE', *, *, #10308, .T. ) ;
#2833=CARTESIAN_POINT ( 'NONE',  ( 2.002547531651519996, -7.942910686618240845, 9.778737580845669797 ) ) ;
#2834=DIRECTION ( 'NONE',  ( 0.000000000000000000, 0.000000000000000000, 1.000000000000000000 ) ) ;
#2835=DIRECTION ( 'NONE',  ( 0.7635533937278214944, 0.2197766120036505344, -0.6071939193889570596 ) ) ;
#2840=CARTESIAN_POINT ( 'NONE',  ( 0.3170788640506440603, 7.952793437297573931, 11.20690911610906326 ) ) ;
#2841=CARTESIAN_POINT ( 'NONE',  ( 0.3939822652208126996, -8.678192463540247203, 10.75310269629518700 ) ) ;
#2844=ORIENTED_EDGE ( 'NONE', *, *, #9940, .F. ) ;
#2846=VECTOR ( 'NONE', #8489, 1000.000000000000114 ) ;
#2848=EDGE_CURVE ( 'NONE', #7476, #18002, #17000, .T. ) ;
#2852=DIRECTION ( 'NONE',  ( -0.7635533937278214944, 0.3620487483322560873, -0.5347026451755899634 ) ) ;
#2854=CARTESIAN_POINT ( 'NONE',  ( 0.3095370825347224519, -12.91933430393611282, 4.681152801286110332 ) ) ;
#2856=LINE ( 'NONE', #2674, #13569 ) ;
#2862=CARTESIAN_POINT ( 'NONE',  ( 0.3151928479966097374, -6.943324943027912228E-05, -13.73922861026898623 ) ) ;
#2863=AXIS2_PLACEMENT_3D ( 'NONE', #6424, #1934, #13683 ) ;
#2864=AXIS2_PLACEMENT_3D ( 'NONE', #6448, #5187, #9308 ) ;
#2865=EDGE_CURVE ( 'NONE', #9201, #10624, #18562, .T. ) ;
#2874=ORIENTED_EDGE ( 'NONE', *, *, #9936, .T. ) ;
#2876=DIRECTION ( 'NONE',  ( 0.000000000000000000, 0.000000000000000000, 1.000000000000000000 ) ) ;
#2885=CARTESIAN_POINT ( 'NONE',  ( 0.4862570985993252548, 11.67702470553365401, 7.559321496869467971 ) ) ;
#2886=CYLINDRICAL_SURFACE ( 'NONE', #12093, 2.500000000000000000 ) ;
#2887=CARTESIAN_POINT ( 'NONE',  ( 1.847372867223022297, -10.00438561114518521, -7.398914411685100667 ) ) ;
#2893=CARTESIAN_POINT ( 'NONE',  ( 3.950837973638675393, -2.591948120961912849, 14.31366178983252446 ) ) ;
#2896=ORIENTED_EDGE ( 'NONE', *, *, #7882, .T. ) ;
#2898=ORIENTED_EDGE ( 'NONE', *, *, #4126, .T. ) ;
#2899=ORIENTED_EDGE ( 'NONE', *, *, #6393, .T. ) ;
#2906=EDGE_LOOP ( 'NONE', ( #5067, #420, #18863, #7212 ) ) ;
#2908=ADVANCED_FACE ( 'NONE', ( #14447 ), #3970, .F. ) ;
#2914=CARTESIAN_POINT ( 'NONE',  ( 1.846138399168762101, -10.30487220521574976, 6.971848976710974810 ) ) ;
#2923=EDGE_CURVE ( 'NONE', #17620, #12792, #10632, .T. ) ;
#2926=CIRCLE ( 'NONE', #4178, 14.54644660717763927 ) ;
#2934=CARTESIAN_POINT ( 'NONE',  ( 2.002547531651519996, 4.532360870844327039, 11.75462648437103752 ) ) ;
#2936=CARTESIAN_POINT ( 'NONE',  ( 1.846613052777650976, -0.3401093050880946711, -12.43780859207240219 ) ) ;
#2938=CARTESIAN_POINT ( 'NONE',  ( 0.3095370825347224519, 13.20347358821914519, 3.806662003783459092 ) ) ;
#2940=CARTESIAN_POINT ( 'NONE',  ( 1.918918678667044686, -10.48466773720556766, -6.832809802519125064 ) ) ;
#2941=CARTESIAN_POINT ( 'NONE',  ( 3.950837973638676281, -10.05648675950133963, 10.51028938476214059 ) ) ;
#2943=CARTESIAN_POINT ( 'NONE',  ( 2.002547531651519996, 3.242439124566821818, -12.17374746633574745 ) ) ;
#2945=VECTOR ( 'NONE', #18300, 1000.000000000000114 ) ;
#2950=CARTESIAN_POINT ( 'NONE',  ( 0.8740764193767813772, -12.04241474977994208, 7.708542792189371440 ) ) ;
#2957=CARTESIAN_POINT ( 'NONE',  ( 0.3148208552358935930, 4.026279359288611026, -13.13564827777585187 ) ) ;
#2959=ORIENTED_EDGE ( 'NONE', *, *, #3458, .F. ) ;
#2968=B_SPLINE_CURVE_WITH_KNOTS ( 'NONE', 3,
 ( #5668, #11428, #8370, #6948, #8283, #3972 ),
 .UNSPECIFIED., .F., .F.,
 ( 4, 2, 4 ),
 ( 3.490137563248181679E-18, 0.0002017457492448096685, 0.0004034914984896158133 ),
 .UNSPECIFIED. ) ;
#2976=ORIENTED_EDGE ( 'NONE', *, *, #10158, .T. ) ;
#2981=CARTESIAN_POINT ( 'NONE',  ( 2.747332970342022840, 11.66639548242807578, 11.45495994260722306 ) ) ;
#2983=CARTESIAN_POINT ( 'NONE',  ( 16.56822296793089322, 0.003834730849370841625, -0.009385634690641637967 ) ) ;
#2984=CARTESIAN_POINT ( 'NONE',  ( 16.58200780006414732, 0.007066318000006001528, -0.008650561019685833880 ) ) ;
#2985=CARTESIAN_POINT ( 'NONE',  ( 0.3132635586635978409, 13.72732610560088773, -0.5277914263193584921 ) ) ;
#2986=CARTESIAN_POINT ( 'NONE',  ( 1.845755665166727066, -4.296872077620760066, 11.67596932341233007 ) ) ;
#2987=CARTESIAN_POINT ( 'NONE',  ( 0.4754618798421162973, 12.98792082933651493, -5.007009103465114741 ) ) ;
#2992=DIRECTION ( 'NONE',  ( 1.000000000000000000, 0.000000000000000000, 0.000000000000000000 ) ) ;
#2994=EDGE_CURVE ( 'NONE', #4199, #666, #18594, .T. ) ;
#2998=ADVANCED_FACE ( 'NONE', ( #291 ), #8996, .F. ) ;
#3015=CARTESIAN_POINT ( 'NONE',  ( 0.4862570985993252548, 13.44146924561381162, 3.580942890621718888 ) ) ;
#3017=VERTEX_POINT ( 'NONE', #7661 ) ;
#3019=B_SPLINE_CURVE_WITH_KNOTS ( 'NONE', 3,
 ( #4046, #9859, #15695, #8536, #5555, #2597, #11411 ),
 .UNSPECIFIED., .F., .F.,
 ( 4, 3, 4 ),
 ( 1.843143693225357538E-18, 0.0002299804304191480943, 0.0004168119862255878537 ),
 .UNSPECIFIED. ) ;
#3020=ADVANCED_FACE ( 'NONE', ( #385 ), #11791, .F. ) ;
#3022=ORIENTED_EDGE ( 'NONE', *, *, #2865, .T. ) ;
#3024=ORIENTED_EDGE ( 'NONE', *, *, #14053, .T. ) ;
#3025=CARTESIAN_POINT ( 'NONE',  ( 0.3307726912345205217, -11.46720933246392882, -7.596084275799019458 ) ) ;
#3027=CARTESIAN_POINT ( 'NONE',  ( 16.57210152137263393, -0.008007331252333342933, 0.01214401161737632510 ) ) ;
#3028=CARTESIAN_POINT ( 'NONE',  ( 1.847168016377982003, -0.1868244120188694568, -12.44137401948661292 ) ) ;
#3032=CARTESIAN_POINT ( 'NONE',  ( 1.846138399168762101, 3.446241763653166590, -11.95493567637846866 ) ) ;
#3033=CARTESIAN_POINT ( 'NONE',  ( 1.254009781012409341, 13.61532727684501509, -5.487405433548977030 ) ) ;
#3034=( NAMED_UNIT ( * ) PLANE_ANGLE_UNIT ( ) SI_UNIT ( $, .RADIAN. ) );
#3035=B_SPLINE_CURVE_WITH_KNOTS ( 'NONE', 3,
 ( #13045, #5772, #17741, #17644 ),
 .UNSPECIFIED., .F., .F.,
 ( 4, 4 ),
 ( 5.784724088816010014E-17, 0.002004993803842651783 ),
 .UNSPECIFIED. ) ;
#3046=CARTESIAN_POINT ( 'NONE',  ( 16.56753206892534891, -0.008490833999798035742, 0.004253784598196731770 ) ) ;
#3051=ORIENTED_EDGE ( 'NONE', *, *, #7216, .F. ) ;
#3054=CARTESIAN_POINT ( 'NONE',  ( 8.522092701127531811, -1.786985377231985694, -6.722964936702116034 ) ) ;
#3056=B_SPLINE_CURVE_WITH_KNOTS ( 'NONE', 3,
 ( #3335, #386, #4883, #4781 ),
 .UNSPECIFIED., .F., .F.,
 ( 4, 4 ),
 ( 1.629624753548408703E-17, 0.003005512676784843126 ),
 .UNSPECIFIED. ) ;
#3057=ORIENTED_EDGE ( 'NONE', *, *, #15897, .F. ) ;
#3063=CARTESIAN_POINT ( 'NONE',  ( 3.074695600508088322, 15.41438262616131283, 2.093687500611883578 ) ) ;
#3065=CARTESIAN_POINT ( 'NONE',  ( 0.3137051932979792457, -8.442169467526928983, 10.83767969834800127 ) ) ;
#3066=CARTESIAN_POINT ( 'NONE',  ( 0.4862570985993235340, -8.769551628660655851, -10.79774104611382946 ) ) ;
#3071=EDGE_CURVE ( 'NONE', #14584, #13704, #17452, .T. ) ;
#3072=ORIENTED_EDGE ( 'NONE', *, *, #9354, .T. ) ;
#3075=CARTESIAN_POINT ( 'NONE',  ( 16.56782317627811096, 0.002708056627497615852, -0.009439921864426480472 ) ) ;
#3077=FACE_OUTER_BOUND ( 'NONE', #13363, .T. ) ;
#3079=CARTESIAN_POINT ( 'NONE',  ( 1.861628059977343153, -4.358833901513129661, 11.66985327793197236 ) ) ;
#3090=DIRECTION ( 'NONE',  ( 0.7635533937278214944, -0.1790966170213922626, -0.6204116510013485408 ) ) ;
#3091=VECTOR ( 'NONE', #6397, 1000.000000000000114 ) ;
#3092=CARTESIAN_POINT ( 'NONE',  ( 2.123976203522053741, 11.67822624909940821, -10.37815841598478883 ) ) ;
#3093=EDGE_CURVE ( 'NONE', #15469, #13788, #11771, .T. ) ;
#3094=EDGE_LOOP ( 'NONE', ( #10283, #18034, #4, #3122 ) ) ;
#3100=CARTESIAN_POINT ( 'NONE',  ( 0.3137051932979775248, 0.4596302728639756197, 13.73004976592202198 ) ) ;
#3103=VERTEX_POINT ( 'NONE', #939 ) ;
#3107=CARTESIAN_POINT ( 'NONE',  ( 16.56782317627811096, -0.002708056627497679603, 0.009439921864426459655 ) ) ;
#3115=( BOUNDED_SURFACE ( )  B_SPLINE_SURFACE ( 3, 1, ( 
 ( #12045, #12148 ),
 ( #10517, #4592 ),
 ( #7568, #13378 ),
 ( #10416, #292 ) ),
 .UNSPECIFIED., .F., .F., .T. ) 
 B_SPLINE_SURFACE_WITH_KNOTS ( ( 4, 4 ),
 ( 2, 2 ),
 ( 0.000000000000000000, 1.000000000000000000 ),
 ( 0.000000000000000000, 1.000000000000000000 ),
 .UNSPECIFIED. ) 
 GEOMETRIC_REPRESENTATION_ITEM ( )  RATIONAL_B_SPLINE_SURFACE ( (
 ( 1.000000000000000000, 1.000000000000000000),
 ( 0.7792777138730160313, 0.9689936506012927220),
 ( 0.7792777138730160313, 0.9689936506012927220),
 ( 1.000000000000000000, 1.000000000000000000) ) ) 
 REPRESENTATION_ITEM ( '' )  SURFACE ( )  );
#3117=VERTEX_POINT ( 'NONE', #853 ) ;
#3120=EDGE_LOOP ( 'NONE', ( #11267, #5072 ) ) ;
#3122=ORIENTED_EDGE ( 'NONE', *, *, #14202, .T. ) ;
#3123=FACE_OUTER_BOUND ( 'NONE', #18092, .T. ) ;
#3128=CARTESIAN_POINT ( 'NONE',  ( 0.4384471787762797002, 3.577367180593735263, -13.39294437382614333 ) ) ;
#3129=CARTESIAN_POINT ( 'NONE',  ( 0.3151928476913583022, 13.06684726503526761, 4.245457024760265874 ) ) ;
#3135=CARTESIAN_POINT ( 'NONE',  ( 0.3095370825347224519, -8.444334731363925428, -10.84046130709067768 ) ) ;
#3144=FACE_OUTER_BOUND ( 'NONE', #15521, .T. ) ;
#3150=CARTESIAN_POINT ( 'NONE',  ( 0.3137051932979792457, -0.4596302728640728752, 13.73004976592201842 ) ) ;
#3151=CARTESIAN_POINT ( 'NONE',  ( 1.846138399168762101, 12.43476674860266584, 0.4167076046095977149 ) ) ;
#3152=CARTESIAN_POINT ( 'NONE',  ( 0.3132635586635977298, -13.72732610560088418, 0.5277914263192632349 ) ) ;
#3154=ADVANCED_FACE ( 'NONE', ( #18154 ), #16318, .F. ) ;
#3157=VECTOR ( 'NONE', #4687, 1000.000000000000114 ) ;
#3163=CARTESIAN_POINT ( 'NONE',  ( 0.3939875929385671105, 11.57636969881034084, 7.545068896001249747 ) ) ;
#3166=CARTESIAN_POINT ( 'NONE',  ( 0.3150692679895994996, -4.391039771493759680, 13.01874238516608884 ) ) ;
#3180=FACE_OUTER_BOUND ( 'NONE', #8133, .T. ) ;
#3184=EDGE_CURVE ( 'NONE', #12792, #17093, #7411, .T. ) ;
#3188=CARTESIAN_POINT ( 'NONE',  ( 0.4862570985993235340, -7.559321496869339185, -11.67702470553373750 ) ) ;
#3190=CARTESIAN_POINT ( 'NONE',  ( 0.3170788640506440603, -13.74111462631963398, -0.1533108587037582682 ) ) ;
#3193=ORIENTED_EDGE ( 'NONE', *, *, #17742, .F. ) ;
#3200=CARTESIAN_POINT ( 'NONE',  ( 1.847461586945731371, -12.44326124954594448, 0.03350899125588503030 ) ) ;
#3203=CARTESIAN_POINT ( 'NONE',  ( 3.950837973638668288, 0.000000000000000000, 0.000000000000000000 ) ) ;
#3205=CARTESIAN_POINT ( 'NONE',  ( 1.847461586945730483, 12.44326124954594626, -0.03350899125597195383 ) ) ;
#3206=EDGE_CURVE ( 'NONE', #11719, #17807, #17906, .T. ) ;
#3208=DIRECTION ( 'NONE',  ( 0.000000000000000000, 0.000000000000000000, 1.000000000000000000 ) ) ;
#3209=EDGE_CURVE ( 'NONE', #4291, #2287, #8093, .T. ) ;
#3228=CARTESIAN_POINT ( 'NONE',  ( 0.3148213771069380829, 12.99360322443203053, 4.463459503829039221 ) ) ;
#3229=CARTESIAN_POINT ( 'NONE',  ( 2.123976203522053741, 1.531817366691752502, 15.54801196254787676 ) ) ;
#3230=CARTESIAN_POINT ( 'NONE',  ( 0.3058872367615226295, 12.87003593440628357, 4.821066432589371509 ) ) ;
#3233=( BOUNDED_SURFACE ( )  B_SPLINE_SURFACE ( 3, 1, ( 
 ( #7310, #17237 ),
 ( #8731, #17431 ),
 ( #7113, #17626 ),
 ( #8635, #13127 ) ),
 .UNSPECIFIED., .F., .F., .T. ) 
 B_SPLINE_SURFACE_WITH_KNOTS ( ( 4, 4 ),
 ( 2, 2 ),
 ( 0.000000000000000000, 1.000000000000000000 ),
 ( 0.000000000000000000, 1.000000000000000000 ),
 .UNSPECIFIED. ) 
 GEOMETRIC_REPRESENTATION_ITEM ( )  RATIONAL_B_SPLINE_SURFACE ( (
 ( 1.000000000000000000, 1.000000000000000000),
 ( 0.7792777138730160313, 0.9689936506012927220),
 ( 0.7792777138730160313, 0.9689936506012927220),
 ( 1.000000000000000000, 1.000000000000000000) ) ) 
 REPRESENTATION_ITEM ( '' )  SURFACE ( )  );
#3236=CARTESIAN_POINT ( 'NONE',  ( 2.320520222536482713, 14.32454429810331220, 6.542539914239615229 ) ) ;
#3237=CARTESIAN_POINT ( 'NONE',  ( 8.438534575730034959, -6.454982381540271597, -2.341351102130346362 ) ) ;
#3241=CONICAL_SURFACE ( 'NONE', #16393, 12.15840553252917289, 0.7853981625000049371 ) ;
#3242=CARTESIAN_POINT ( 'NONE',  ( 0.3132642857406540138, -4.743831191224475496, 12.89240536501344536 ) ) ;
#3247=CARTESIAN_POINT ( 'NONE',  ( 0.3132642857406524595, -12.89240536501342760, -4.743831191224519905 ) ) ;
#3249=B_SPLINE_CURVE_WITH_KNOTS ( 'NONE', 3,
 ( #5613, #17281, #14799, #4583, #17774, #16535 ),
 .UNSPECIFIED., .F., .F.,
 ( 4, 2, 4 ),
 ( 0.000000000000000000, 0.0001828790815886951050, 0.0003657581631773902100 ),
 .UNSPECIFIED. ) ;
#3257=B_SPLINE_CURVE_WITH_KNOTS ( 'NONE', 3,
 ( #675, #12326, #17979, #5060, #16905, #487, #5245, #18156, #16548, #6317, #11090, #4885, #15288 ),
 .UNSPECIFIED., .F., .F.,
 ( 4, 3, 3, 3, 4 ),
 ( 3.035766082959412415E-18, 0.0002299780670421045197, 0.0004599561239687880061, 0.0006896788984287874130, 0.0009194956271626412558 ),
 .UNSPECIFIED. ) ;
#3267=CARTESIAN_POINT ( 'NONE',  ( 0.3151930723728453843, -4.318364831037682094, 13.04315954105013198 ) ) ;
#3275=ORIENTED_EDGE ( 'NONE', *, *, #14937, .F. ) ;
#3276=CARTESIAN_POINT ( 'NONE',  ( 1.861628059977344263, 3.332996951203627933, 12.00316790821102941 ) ) ;
#3277=ORIENTED_EDGE ( 'NONE', *, *, #10758, .F. ) ;
#3285=B_SPLINE_CURVE_WITH_KNOTS ( 'NONE', 3,
 ( #2784, #17517, #4424, #8359, #14178, #18660, #6926, #17139, #4050, #15700, #12833, #5559, #11415 ),
 .UNSPECIFIED., .F., .F.,
 ( 4, 3, 3, 3, 4 ),
 ( 8.673617379884034509E-19, 0.0002299780670421053329, 0.0004599561239687884940, 0.0006896788984287899067, 0.0009194956271626421231 ),
 .UNSPECIFIED. ) ;
#3286=CARTESIAN_POINT ( 'NONE',  ( 3.353306896162455253, -3.007732942432324474, -13.62210141459498303 ) ) ;
#3288=CARTESIAN_POINT ( 'NONE',  ( 2.002547531651519996, -3.242439124566736997, 12.17374746633577232 ) ) ;
#3289=CARTESIAN_POINT ( 'NONE',  ( 8.438534575730034959, 2.341351102130277528, 6.454982381540297354 ) ) ;
#3290=CARTESIAN_POINT ( 'NONE',  ( 2.747332970342022840, 11.66639548242823921, -11.45495994260705075 ) ) ;
#3295=ORIENTED_EDGE ( 'NONE', *, *, #8213, .F. ) ;
#3304=CARTESIAN_POINT ( 'NONE',  ( 1.846138399168762101, -3.446241763652916124, -11.95493567637853971 ) ) ;
#3307=DIRECTION ( 'NONE',  ( -1.000000000000000000, -0.000000000000000000, -0.000000000000000000 ) ) ;
#3313=AXIS2_PLACEMENT_3D ( 'NONE', #791, #701, #15404 ) ;
#3323=EDGE_CURVE ( 'NONE', #8935, #16984, #15388, .T. ) ;
#3329=VECTOR ( 'NONE', #12064, 1000.000000000000114 ) ;
#3331=CARTESIAN_POINT ( 'NONE',  ( 0.3142011359265332593, 13.17934269988458063, 3.879426116491735854 ) ) ;
#3332=CARTESIAN_POINT ( 'NONE',  ( 16.57778382496167424, 0.01482878558584569718, 0.001819584982831951199 ) ) ;
#3333=CARTESIAN_POINT ( 'NONE',  ( 16.56782317627811096, -0.009439921864426870785, 0.002708056627498742989 ) ) ;
#3335=CARTESIAN_POINT ( 'NONE',  ( 3.950837973638676281, 6.316429227969464932, 13.10350451991842569 ) ) ;
#3340=CONICAL_SURFACE ( 'NONE', #8242, 14.54644660717763927, 0.8559913436420816257 ) ;
#3341=CARTESIAN_POINT ( 'NONE',  ( 0.4862570985993252548, -12.97920246947875889, -5.003653737315625349 ) ) ;
#3342=CARTESIAN_POINT ( 'NONE',  ( 1.847168016377980670, 11.77471791462004802, -4.022276579849838996 ) ) ;
#3346=CARTESIAN_POINT ( 'NONE',  ( 16.56753206892534891, -0.001421777558676017277, 0.009389754735542238384 ) ) ;
#3347=ORIENTED_EDGE ( 'NONE', *, *, #15375, .F. ) ;
#3350=ORIENTED_EDGE ( 'NONE', *, *, #17148, .T. ) ;
#3353=CARTESIAN_POINT ( 'NONE',  ( 0.3170788640506440603, 11.02668139258442359, 8.200855617524574370 ) ) ;
#3354=( BOUNDED_SURFACE ( )  B_SPLINE_SURFACE ( 3, 1, ( 
 ( #17688, #16448 ),
 ( #16627, #16543 ),
 ( #3428, #4776 ),
 ( #1618, #10707 ) ),
 .UNSPECIFIED., .F., .F., .T. ) 
 B_SPLINE_SURFACE_WITH_KNOTS ( ( 4, 4 ),
 ( 2, 2 ),
 ( 0.000000000000000000, 1.000000000000000000 ),
 ( 0.000000000000000000, 1.000000000000000000 ),
 .UNSPECIFIED. ) 
 GEOMETRIC_REPRESENTATION_ITEM ( )  RATIONAL_B_SPLINE_SURFACE ( (
 ( 1.000000000000000000, 1.000000000000000000),
 ( 0.9933953342250436691, 0.8357391271907733676),
 ( 0.9933953342250436691, 0.8357391271907733676),
 ( 1.000000000000000000, 1.000000000000000000) ) ) 
 REPRESENTATION_ITEM ( '' )  SURFACE ( )  );
#3367=CARTESIAN_POINT ( 'NONE',  ( 0.3150692679895986670, -8.199139630396084399, 11.02465386701225469 ) ) ;
#3373=CARTESIAN_POINT ( 'NONE',  ( 3.664313757352976264, -7.012524439851403280, -12.42002390572634418 ) ) ;
#3376=CARTESIAN_POINT ( 'NONE',  ( 16.56822296793089322, 0.007741272030791082788, 0.006547366384935537215 ) ) ;
#3377=CARTESIAN_POINT ( 'NONE',  ( 2.123976203522053741, 3.347755036806118856, -15.26039569100256266 ) ) ;
#3378=CARTESIAN_POINT ( 'NONE',  ( 0.4862570985993235340, -7.559321496869506163, 11.67702470553362559 ) ) ;
#3385=CARTESIAN_POINT ( 'NONE',  ( 0.4862570985993235340, -3.580942890621579444, -13.44146924561384537 ) ) ;
#3388=CARTESIAN_POINT ( 'NONE',  ( 0.3307726912345205772, 8.558645027434268471, 10.76786801061209964 ) ) ;
#3392=EDGE_LOOP ( 'NONE', ( #11101, #17625, #2053, #7778 ) ) ;
#3393=VERTEX_POINT ( 'NONE', #11169 ) ;
#3394=VERTEX_POINT ( 'NONE', #4961 ) ;
#3395=VERTEX_POINT ( 'NONE', #16621 ) ;
#3396=B_SPLINE_CURVE_WITH_KNOTS ( 'NONE', 3,
 ( #2788, #14461, #1470, #1374, #4535, #5953 ),
 .UNSPECIFIED., .F., .F.,
 ( 4, 2, 4 ),
 ( 0.000000000000000000, 0.001656992708822367915, 0.003313985417644735830 ),
 .UNSPECIFIED. ) ;
#3399=CARTESIAN_POINT ( 'NONE',  ( 1.861628059977344041, 0.5393144007391995620, -12.44564375541076551 ) ) ;
#3407=B_SPLINE_CURVE_WITH_KNOTS ( 'NONE', 3,
 ( #18311, #5218, #917, #12568, #9881, #5574 ),
 .UNSPECIFIED., .F., .F.,
 ( 4, 2, 4 ),
 ( 2.710505431213761085E-19, 0.001657017934710631590, 0.003314035869421263179 ),
 .UNSPECIFIED. ) ;
#3408=EDGE_CURVE ( 'NONE', #15162, #13108, #8321, .T. ) ;
#3415=CARTESIAN_POINT ( 'NONE',  ( 3.950837973638677170, 12.81214529934985080, -6.888253895133152227 ) ) ;
#3416=ORIENTED_EDGE ( 'NONE', *, *, #10676, .F. ) ;
#3419=ORIENTED_EDGE ( 'NONE', *, *, #9936, .F. ) ;
#3420=EDGE_LOOP ( 'NONE', ( #4695, #1201, #12388, #11751 ) ) ;
#3428=CARTESIAN_POINT ( 'NONE',  ( 16.56822296793089322, 0.009847136207496274760, 0.002414375228568293487 ) ) ;
#3431=FACE_OUTER_BOUND ( 'NONE', #16067, .T. ) ;
#3433=CARTESIAN_POINT ( 'NONE',  ( 0.3150690434770175852, 0.1531837610935626592, -13.73846430619029313 ) ) ;
#3441=CARTESIAN_POINT ( 'NONE',  ( 1.918918678667046240, 11.69059232068584819, -4.466049546133788795 ) ) ;
#3442=CARTESIAN_POINT ( 'NONE',  ( 0.3307726912345181902, 10.76786801061219734, -8.558645027434160113 ) ) ;
#3443=EDGE_CURVE ( 'NONE', #3, #13002, #1228, .T. ) ;
#3448=EDGE_LOOP ( 'NONE', ( #6925, #17991, #9352, #2182 ) ) ;
#3449=CARTESIAN_POINT ( 'NONE',  ( 2.636624412715137922, -6.973567714907947135, 14.46769361191283920 ) ) ;
#3451=CARTESIAN_POINT ( 'NONE',  ( 2.002547531651519996, -12.17374746633575988, -3.242439124566779185 ) ) ;
#3458=EDGE_CURVE ( 'NONE', #3017, #11719, #15822, .T. ) ;
#3463=CARTESIAN_POINT ( 'NONE',  ( 16.57210152137263393, 0.01136813053532160708, -0.009075239946109073599 ) ) ;
#3470=ORIENTED_EDGE ( 'NONE', *, *, #4315, .F. ) ;
#3479=CARTESIAN_POINT ( 'NONE',  ( 1.918921323896322750, 12.49850046818175286, 0.6349083173280601899 ) ) ;
#3485=CARTESIAN_POINT ( 'NONE',  ( 3.664313757352975376, -2.831308606787148463, -13.97913389346637025 ) ) ;
#3487=CARTESIAN_POINT ( 'NONE',  ( 2.320520222537280297, -15.64520721754692190, -1.795797593768913236 ) ) ;
#3489=CARTESIAN_POINT ( 'NONE',  ( 1.847412631396502025, -11.84727953344286533, 3.804043368582616935 ) ) ;
#3490=CARTESIAN_POINT ( 'NONE',  ( 8.522092701127531811, 6.722964936702122252, -1.786985377231962380 ) ) ;
#3497=ADVANCED_FACE ( 'NONE', ( #12680 ), #14349, .F. ) ;
#3500=CARTESIAN_POINT ( 'NONE',  ( 1.861706995891668326, -7.751853334747247359, -9.751699138048525839 ) ) ;
#3505=DIRECTION ( 'NONE',  ( 0.7635533937278214944, 0.5347026451755962917, -0.3620487483322465949 ) ) ;
#3507=DIRECTION ( 'NONE',  ( 0.7635533937278216055, -0.5347026451755990673, 0.3620487483322425981 ) ) ;
#3509=CARTESIAN_POINT ( 'NONE',  ( 3.950837973638668288, 0.000000000000000000, 0.000000000000000000 ) ) ;
#3510=B_SPLINE_CURVE_WITH_KNOTS ( 'NONE', 3,
 ( #8325, #687, #13861, #8235, #18352, #6520 ),
 .UNSPECIFIED., .F., .F.,
 ( 4, 2, 4 ),
 ( 0.000000000000000000, 0.001500839035891550705, 0.003001678071783101410 ),
 .UNSPECIFIED. ) ;
#3511=CARTESIAN_POINT ( 'NONE',  ( 1.846138399168762989, 4.238866729160403857, 11.69739621335923729 ) ) ;
#3512=VERTEX_POINT ( 'NONE', #1568 ) ;
#3514=EDGE_LOOP ( 'NONE', ( #13591, #4843, #18601, #1880 ) ) ;
#3520=ADVANCED_FACE ( 'NONE', ( #17526 ), #1178, .F. ) ;
#3523=FACE_OUTER_BOUND ( 'NONE', #5826, .T. ) ;
#3528=CARTESIAN_POINT ( 'NONE',  ( 1.918921323896325193, -0.6349083173281016013, 12.49850046818174043 ) ) ;
#3529=CARTESIAN_POINT ( 'NONE',  ( 2.636624412715138366, -15.91454522070249311, -2.161493821597819665 ) ) ;
#3543=FACE_OUTER_BOUND ( 'NONE', #17305, .T. ) ;
#3548=VECTOR ( 'NONE', #706, 1000.000000000000000 ) ;
#3551=CARTESIAN_POINT ( 'NONE',  ( 0.4384471787762813100, -8.732395932355604629, -10.76632603192796722 ) ) ;
#3554=B_SPLINE_CURVE_WITH_KNOTS ( 'NONE', 3,
 ( #15575, #11107, #10756, #2476, #13514, #14141 ),
 .UNSPECIFIED., .F., .F.,
 ( 4, 2, 4 ),
 ( 3.499941646806256644E-17, 0.0001825746017570582086, 0.0003651492035140814518 ),
 .UNSPECIFIED. ) ;
#3559=ORIENTED_EDGE ( 'NONE', *, *, #510, .F. ) ;
#3561=DIRECTION ( 'NONE',  ( 0.7071067818211348444, 0.000000000000000000, -0.7071067805519601901 ) ) ;
#3562=CARTESIAN_POINT ( 'NONE',  ( 3.664313757352975376, -14.16986885736091395, -1.627055439596424513 ) ) ;
#3567=FACE_OUTER_BOUND ( 'NONE', #6810, .T. ) ;
#3568=VERTEX_POINT ( 'NONE', #10850 ) ;
#3571=CONICAL_SURFACE ( 'NONE', #12123, 14.54644660717763927, 0.8559913436420816257 ) ;
#3575=CARTESIAN_POINT ( 'NONE',  ( 2.002547531651519996, 12.57989064830759496, 0.6781519942172178350 ) ) ;
#3580=EDGE_CURVE ( 'NONE', #10871, #8470, #9311, .T. ) ;
#3583=CARTESIAN_POINT ( 'NONE',  ( 0.3939822652208109788, 0.7002900021919884477, -13.80035637018651684 ) ) ;
#3587=CARTESIAN_POINT ( 'NONE',  ( 0.3939875929385636688, 8.678227324501120776, 10.75308190953746212 ) ) ;
#3591=FACE_OUTER_BOUND ( 'NONE', #730, .T. ) ;
#3593=EDGE_LOOP ( 'NONE', ( #1132, #1706, #15924, #16239 ) ) ;
#3598=CARTESIAN_POINT ( 'NONE',  ( 0.4862570985993235340, 0.7479633556562450547, 13.89016912371017831 ) ) ;
#3605=CARTESIAN_POINT ( 'NONE',  ( 16.56782317627811096, -0.009814734722106369796, 0.0003415813796014346851 ) ) ;
#3607=CARTESIAN_POINT ( 'NONE',  ( 0.3170788640506441158, -8.200855617524453578, -11.02668139258451063 ) ) ;
#3617=CARTESIAN_POINT ( 'NONE',  ( 16.57210152137263393, 0.005118120558001911478, 0.01361613799508963087 ) ) ;
#3623=CARTESIAN_POINT ( 'NONE',  ( 16.56822296793089322, -0.0007467251401289379167, 0.01011126603341003759 ) ) ;
#3630=EDGE_CURVE ( 'NONE', #13002, #14893, #5793, .T. ) ;
#3633=CARTESIAN_POINT ( 'NONE',  ( 1.847034903785823579, 11.90269060117939048, -3.625649561595184700 ) ) ;
#3638=CARTESIAN_POINT ( 'NONE',  ( 1.846613052777651198, -4.166957398589769213, -11.72395935470502870 ) ) ;
#3640=ORIENTED_EDGE ( 'NONE', *, *, #5833, .F. ) ;
#3642=CARTESIAN_POINT ( 'NONE',  ( 1.254009781011930613, -12.44229282923100932, -7.789615163754561422 ) ) ;
#3643=CARTESIAN_POINT ( 'NONE',  ( 0.3939875929385628361, -8.678227324501040840, -10.75308190953752785 ) ) ;
#3650=CARTESIAN_POINT ( 'NONE',  ( 2.002547531651519996, -6.845637710436264456, 10.57595306287289638 ) ) ;
#3651=EDGE_CURVE ( 'NONE', #5420, #17676, #11975, .T. ) ;
#3653=CARTESIAN_POINT ( 'NONE',  ( 16.56822296793089322, 0.01011126603341004106, 0.0007467251401288980180 ) ) ;
#3656=CARTESIAN_POINT ( 'NONE',  ( 2.002547531651519996, 7.942910686618173344, 9.778737580845726640 ) ) ;
#3658=CARTESIAN_POINT ( 'NONE',  ( 3.664313757352963830, 12.97355833021539873, 5.926151963190401162 ) ) ;
#3659=CARTESIAN_POINT ( 'NONE',  ( 1.846138399168762101, -11.69739621335925328, 4.238866729160359448 ) ) ;
#3660=ORIENTED_EDGE ( 'NONE', *, *, #11096, .F. ) ;
#3661=ORIENTED_EDGE ( 'NONE', *, *, #12412, .T. ) ;
#3664=VERTEX_POINT ( 'NONE', #2408 ) ;
#3667=B_SPLINE_CURVE_WITH_KNOTS ( 'NONE', 3,
 ( #17368, #7059, #2544, #4285, #8307, #18608 ),
 .UNSPECIFIED., .F., .F.,
 ( 4, 2, 4 ),
 ( 1.748223473168675632E-18, 0.0002017457492448083403, 0.0004034914984896149459 ),
 .UNSPECIFIED. ) ;
#3670=CARTESIAN_POINT ( 'NONE',  ( 1.847372867223024073, 7.228345833872753978, 10.12831093686724238 ) ) ;
#3681=ORIENTED_EDGE ( 'NONE', *, *, #12726, .F. ) ;
#3684=B_SPLINE_CURVE_WITH_KNOTS ( 'NONE', 3,
 ( #212, #10341, #11873, #17712 ),
 .UNSPECIFIED., .F., .F.,
 ( 4, 4 ),
 ( 0.000000000000000000, 0.002004993803842688646 ),
 .UNSPECIFIED. ) ;
#3685=EDGE_LOOP ( 'NONE', ( #16840, #5021, #7062, #1851 ) ) ;
#3686=CARTESIAN_POINT ( 'NONE',  ( 0.3939875929385629472, 0.7003304234513173521, 13.80036004410494854 ) ) ;
#3691=CARTESIAN_POINT ( 'NONE',  ( 0.4862570985993252548, 10.79774104611373353, 8.769551628660776643 ) ) ;
#3702=ORIENTED_EDGE ( 'NONE', *, *, #3651, .F. ) ;
#3704=B_SPLINE_CURVE_WITH_KNOTS ( 'NONE', 3,
 ( #13450, #363, #8862, #271 ),
 .UNSPECIFIED., .F., .F.,
 ( 4, 4 ),
 ( 0.000000000000000000, 0.002004993803842899849 ),
 .UNSPECIFIED. ) ;
#3707=CARTESIAN_POINT ( 'NONE',  ( 0.3058872367615226295, 7.578326039752606214, 11.46514199369360298 ) ) ;
#3709=CARTESIAN_POINT ( 'NONE',  ( 2.002547531651520885, -4.532360870844412304, 11.75462648437100377 ) ) ;
#3714=CARTESIAN_POINT ( 'NONE',  ( 2.320520222536477384, 7.743191299717406828, 13.71278186123164922 ) ) ;
#3722=CARTESIAN_POINT ( 'NONE',  ( 2.636624412716062071, -11.10302021258080352, -11.60464335004061454 ) ) ;
#3724=CARTESIAN_POINT ( 'NONE',  ( 3.512766787570760663, -10.87507422923897238, 10.40533104696129918 ) ) ;
#3726=CARTESIAN_POINT ( 'NONE',  ( 1.846524061778019199, -0.3544704288993353880, 12.43723828841088341 ) ) ;
#3731=ORIENTED_EDGE ( 'NONE', *, *, #14047, .T. ) ;
#3733=EDGE_CURVE ( 'NONE', #13051, #13031, #6737, .T. ) ;
#3735=CARTESIAN_POINT ( 'NONE',  ( 2.002547531651519996, -11.75462648437098601, -4.532360870844453160 ) ) ;
#3736=CARTESIAN_POINT ( 'NONE',  ( 1.847168016377981115, 9.955470380986737311, -7.464000291196308368 ) ) ;
#3739=FACE_OUTER_BOUND ( 'NONE', #6006, .T. ) ;
#3743=( BOUNDED_SURFACE ( )  B_SPLINE_SURFACE ( 3, 1, ( 
 ( #15732, #13133 ),
 ( #9630, #1018 ),
 ( #16102, #9802 ),
 ( #2984, #14030 ) ),
 .UNSPECIFIED., .F., .F., .T. ) 
 B_SPLINE_SURFACE_WITH_KNOTS ( ( 4, 4 ),
 ( 2, 2 ),
 ( 0.000000000000000000, 1.000000000000000000 ),
 ( 0.000000000000000000, 1.000000000000000000 ),
 .UNSPECIFIED. ) 
 GEOMETRIC_REPRESENTATION_ITEM ( )  RATIONAL_B_SPLINE_SURFACE ( (
 ( 1.000000000000000000, 1.000000000000000000),
 ( 0.7792777138730160313, 0.9689936506012927220),
 ( 0.7792777138730160313, 0.9689936506012927220),
 ( 1.000000000000000000, 1.000000000000000000) ) ) 
 REPRESENTATION_ITEM ( '' )  SURFACE ( )  );
#3745=CARTESIAN_POINT ( 'NONE',  ( 0.3151930723728431083, -11.07033375389125673, -8.137566970826481949 ) ) ;
#3746=CARTESIAN_POINT ( 'NONE',  ( 2.002547531651519996, -11.75462648437105173, 4.532360870844282630 ) ) ;
#3749=CARTESIAN_POINT ( 'NONE',  ( 8.438534575730034959, -5.415535776177489602, -4.221456476902725186 ) ) ;
#3751=CARTESIAN_POINT ( 'NONE',  ( 16.58200780006414732, 0.006043560077721710048, -0.009393638146078546122 ) ) ;
#3763=CARTESIAN_POINT ( 'NONE',  ( 1.847461586945728707, 7.341074796295939286, 10.04711372545047254 ) ) ;
#3768=CARTESIAN_POINT ( 'NONE',  ( 1.846955891736117072, 7.098901504650503291, -10.21904526726839002 ) ) ;
#3771=CARTESIAN_POINT ( 'NONE',  ( 0.3170788640506441158, -4.100430649998053845, 13.11595226728156405 ) ) ;
#3772=ORIENTED_EDGE ( 'NONE', *, *, #721, .T. ) ;
#3777=CARTESIAN_POINT ( 'NONE',  ( 0.3150692679895995552, 11.02465386701228844, 8.199139630396045320 ) ) ;
#3780=LINE ( 'NONE', #14293, #17554 ) ;
#3787=CARTESIAN_POINT ( 'NONE',  ( 16.56753206892534891, -0.001421777558676855365, -0.009389754735541546229 ) ) ;
#3789=CARTESIAN_POINT ( 'NONE',  ( 3.353306896162454809, 12.02594772223106645, -7.069984850384678055 ) ) ;
#3790=ADVANCED_FACE ( 'NONE', ( #9388 ), #12895, .F. ) ;
#3791=ORIENTED_EDGE ( 'NONE', *, *, #13250, .F. ) ;
#3793=ORIENTED_EDGE ( 'NONE', *, *, #2185, .T. ) ;
#3795=CARTESIAN_POINT ( 'NONE',  ( 0.4754618798421171855, 8.775436892861110394, 10.80499583390516172 ) ) ;
#3796=CARTESIAN_POINT ( 'NONE',  ( 3.950837973638675393, 14.31366178983257242, -2.591948120961654833 ) ) ;
#3800=ORIENTED_EDGE ( 'NONE', *, *, #7188, .T. ) ;
#3801=CARTESIAN_POINT ( 'NONE',  ( 0.4754618798421162973, -8.775436892861034011, -10.80499583390522567 ) ) ;
#3802=AXIS2_PLACEMENT_3D ( 'NONE', #4204, #18711, #9924 ) ;
#3803=CARTESIAN_POINT ( 'NONE',  ( 1.846138399168762101, -11.95493567637848109, -3.446241763653124401 ) ) ;
#3807=CARTESIAN_POINT ( 'NONE',  ( 0.4754618798421171855, -3.583352865732766901, 13.45049478164058598 ) ) ;
#3810=CARTESIAN_POINT ( 'NONE',  ( 2.636624412716062960, 2.862162146982868194, -15.80357026013419564 ) ) ;
#3811=EDGE_CURVE ( 'NONE', #16337, #31, #12165, .T. ) ;
#3814=CIRCLE ( 'NONE', #472, 2.500000000000000000 ) ;
#3823=CARTESIAN_POINT ( 'NONE',  ( 2.697797270744668463, 4.970631985779762729, -12.33058466479263693 ) ) ;
#3832=CARTESIAN_POINT ( 'NONE',  ( 1.846822687350017311, 10.23524390843949483, -7.075150813727003829 ) ) ;
#3835=CARTESIAN_POINT ( 'NONE',  ( 2.636624412715137922, -14.46769361191291559, 6.973567714907789927 ) ) ;
#3836=CARTESIAN_POINT ( 'NONE',  ( 3.950837973638677170, 10.51028938476232355, -10.05648675950114956 ) ) ;
#3842=CARTESIAN_POINT ( 'NONE',  ( 0.3148208552358962020, -11.24855514421869529, -7.888357771040825028 ) ) ;
#3843=CARTESIAN_POINT ( 'NONE',  ( 0.3145734862173232838, -3.953068532979906458, -13.15783074029282673 ) ) ;
#3846=EDGE_LOOP ( 'NONE', ( #5583, #16320, #4399, #5039 ) ) ;
#3850=CARTESIAN_POINT ( 'NONE',  ( 1.959283090834842200, 10.53516775895160507, 6.829027319138286423 ) ) ;
#3855=CARTESIAN_POINT ( 'NONE',  ( 2.353870697619109720, 0.7635393531608140050, -12.92712089195301850 ) ) ;
#3862=( BOUNDED_SURFACE ( )  B_SPLINE_SURFACE ( 3, 1, ( 
 ( #14333, #2938 ),
 ( #8688, #11471 ),
 ( #18716, #18816 ),
 ( #14516, #5919 ) ),
 .UNSPECIFIED., .F., .F., .T. ) 
 B_SPLINE_SURFACE_WITH_KNOTS ( ( 4, 4 ),
 ( 2, 2 ),
 ( 0.000000000000000000, 1.000000000000000000 ),
 ( 0.000000000000000000, 1.000000000000000000 ),
 .UNSPECIFIED. ) 
 GEOMETRIC_REPRESENTATION_ITEM ( )  RATIONAL_B_SPLINE_SURFACE ( (
 ( 1.000000000000000000, 1.000000000000000000),
 ( 0.9593108457356467333, 0.9995965569486454649),
 ( 0.9593108457356467333, 0.9995965569486454649),
 ( 1.000000000000000000, 1.000000000000000000) ) ) 
 REPRESENTATION_ITEM ( '' )  SURFACE ( )  );
#3868=VECTOR ( 'NONE', #7669, 1000.000000000000114 ) ;
#3869=CARTESIAN_POINT ( 'NONE',  ( 0.4862570985993235340, -11.67702470553359539, -7.559321496869553236 ) ) ;
#3870=CARTESIAN_POINT ( 'NONE',  ( 2.123976203522053297, -6.261444813538658671, 14.31368049382967556 ) ) ;
#3873=VERTEX_POINT ( 'NONE', #3150 ) ;
#3876=CARTESIAN_POINT ( 'NONE',  ( 0.3142011359265333148, 11.33549115679423736, 7.762194356530812023 ) ) ;
#3877=VECTOR ( 'NONE', #16207, 999.9999999999998863 ) ;
#3885=CARTESIAN_POINT ( 'NONE',  ( 16.56872352241294521, 0.001821578298044641397, 0.01027347319884442528 ) ) ;
#3886=EDGE_CURVE ( 'NONE', #11883, #473, #13077, .T. ) ;
#3891=EDGE_CURVE ( 'NONE', #10554, #17590, #3923, .T. ) ;
#3894=ORIENTED_EDGE ( 'NONE', *, *, #4468, .F. ) ;
#3895=CARTESIAN_POINT ( 'NONE',  ( 1.846138399168762101, 3.446241763653166590, -11.95493567637846866 ) ) ;
#3907=LINE ( 'NONE', #6690, #12971 ) ;
#3913=ORIENTED_EDGE ( 'NONE', *, *, #17570, .T. ) ;
#3914=CARTESIAN_POINT ( 'NONE',  ( 3.074695600507254767, -11.23985886659442635, 10.75417554975694578 ) ) ;
#3916=CARTESIAN_POINT ( 'NONE',  ( 0.4862570985993235340, 13.89016912371017476, 0.7479633556562934604 ) ) ;
#3920=DIRECTION ( 'NONE',  ( -1.000000000000000000, -0.000000000000000000, -0.000000000000000000 ) ) ;
#3923=LINE ( 'NONE', #18174, #6099 ) ;
#3927=EDGE_CURVE ( 'NONE', #10438, #18549, #1509, .T. ) ;
#3930=EDGE_CURVE ( 'NONE', #4935, #7817, #11816, .T. ) ;
#3932=CARTESIAN_POINT ( 'NONE',  ( 16.58200780006414732, -0.007066318000005944282, 0.008650561019685880718 ) ) ;
#3937=CARTESIAN_POINT ( 'NONE',  ( 0.3170788640506441158, -13.02120094575831288, 4.392045232375760833 ) ) ;
#3938=CARTESIAN_POINT ( 'NONE',  ( 2.320520222536567090, 11.60169517779319293, 10.64885284334832960 ) ) ;
#3939=( BOUNDED_SURFACE ( )  B_SPLINE_SURFACE ( 3, 1, ( 
 ( #5969, #7617 ),
 ( #17343, #11805 ),
 ( #6074, #17641 ),
 ( #1488, #17537 ) ),
 .UNSPECIFIED., .F., .F., .T. ) 
 B_SPLINE_SURFACE_WITH_KNOTS ( ( 4, 4 ),
 ( 2, 2 ),
 ( 0.000000000000000000, 1.000000000000000000 ),
 ( 0.000000000000000000, 1.000000000000000000 ),
 .UNSPECIFIED. ) 
 GEOMETRIC_REPRESENTATION_ITEM ( )  RATIONAL_B_SPLINE_SURFACE ( (
 ( 1.000000000000000000, 1.000000000000000000),
 ( 0.7792777138730160313, 0.9689936506012927220),
 ( 0.7792777138730160313, 0.9689936506012927220),
 ( 1.000000000000000000, 1.000000000000000000) ) ) 
 REPRESENTATION_ITEM ( '' )  SURFACE ( )  );
#3943=ORIENTED_EDGE ( 'NONE', *, *, #491, .T. ) ;
#3950=CARTESIAN_POINT ( 'NONE',  ( 16.56872352241294521, 0.007240717549633990044, -0.007512283835805476720 ) ) ;
#3955=EDGE_CURVE ( 'NONE', #5950, #2340, #4058, .T. ) ;
#3956=CARTESIAN_POINT ( 'NONE',  ( 0.3720661004400037664, -12.89739157014188997, -4.951033743989776248 ) ) ;
#3961=VERTEX_POINT ( 'NONE', #5168 ) ;
#3964=EDGE_LOOP ( 'NONE', ( #928, #17965, #17196, #1901 ) ) ;
#3968=CARTESIAN_POINT ( 'NONE',  ( 0.4754618798421162973, 5.007009103465432709, -12.98792082933639058 ) ) ;
#3970=( BOUNDED_SURFACE ( )  B_SPLINE_SURFACE ( 3, 1, ( 
 ( #17129, #7099 ),
 ( #7199, #12917 ),
 ( #11499, #13011 ),
 ( #3950, #17316 ) ),
 .UNSPECIFIED., .F., .F., .T. ) 
 B_SPLINE_SURFACE_WITH_KNOTS ( ( 4, 4 ),
 ( 2, 2 ),
 ( 0.000000000000000000, 1.000000000000000000 ),
 ( 0.000000000000000000, 1.000000000000000000 ),
 .UNSPECIFIED. ) 
 GEOMETRIC_REPRESENTATION_ITEM ( )  RATIONAL_B_SPLINE_SURFACE ( (
 ( 1.000000000000000000, 1.000000000000000000),
 ( 0.9933953342250436691, 0.8357391271907733676),
 ( 0.9933953342250436691, 0.8357391271907733676),
 ( 1.000000000000000000, 1.000000000000000000) ) ) 
 REPRESENTATION_ITEM ( '' )  SURFACE ( )  );
#3972=CARTESIAN_POINT ( 'NONE',  ( 0.4862570985993235340, -12.97920246947883172, 5.003653737315437944 ) ) ;
#3982=DIRECTION ( 'NONE',  ( 0.7071067818211348444, 8.659560554583479511E-17, 0.7071067805519601901 ) ) ;
#3990=CARTESIAN_POINT ( 'NONE',  ( 1.846524061778021419, -11.71897913237546263, -4.180439405448447054 ) ) ;
#3994=CARTESIAN_POINT ( 'NONE',  ( 2.123976203522053741, -15.54801196254788209, 1.531817366691698545 ) ) ;
#4003=CONICAL_SURFACE ( 'NONE', #13459, 14.54644660717763927, 0.8559913436420816257 ) ;
#4004=CARTESIAN_POINT ( 'NONE',  ( 3.950837973638668288, 14.41405733518061538, -1.958075594453841273 ) ) ;
#4006=CARTESIAN_POINT ( 'NONE',  ( 3.950837973638668288, 0.000000000000000000, 0.000000000000000000 ) ) ;
#4009=LINE ( 'NONE', #4106, #1700 ) ;
#4010=ORIENTED_EDGE ( 'NONE', *, *, #1534, .F. ) ;
#4015=CARTESIAN_POINT ( 'NONE',  ( 1.846138399168762101, 10.30487220521580305, -6.971848976710897539 ) ) ;
#4018=EDGE_CURVE ( 'NONE', #14993, #13051, #8237, .T. ) ;
#4019=CARTESIAN_POINT ( 'NONE',  ( 16.57778382496167424, 0.002851818597093403688, 0.01466529584256672306 ) ) ;
#4020=AXIS2_PLACEMENT_3D ( 'NONE', #7263, #15188, #7652 ) ;
#4027=VERTEX_POINT ( 'NONE', #17582 ) ;
#4029=CARTESIAN_POINT ( 'NONE',  ( 2.636624412716062515, -6.973567714909003179, -14.46769361191335790 ) ) ;
#4034=AXIS2_PLACEMENT_3D ( 'NONE', #11606, #13831, #5659 ) ;
#4035=EDGE_CURVE ( 'NONE', #473, #1860, #8689, .T. ) ;
#4036=CARTESIAN_POINT ( 'NONE',  ( 0.3137051932979775248, -0.4596302728638797519, -13.73004976592202553 ) ) ;
#4039=ORIENTED_EDGE ( 'NONE', *, *, #17573, .F. ) ;
#4044=CARTESIAN_POINT ( 'NONE',  ( 0.3148208552358916501, -12.99355031785208681, 4.463611911212169936 ) ) ;
#4045=( BOUNDED_SURFACE ( )  B_SPLINE_SURFACE ( 3, 1, ( 
 ( #8781, #8586 ),
 ( #7359, #1606 ),
 ( #10402, #13263 ),
 ( #13169, #17572 ) ),
 .UNSPECIFIED., .F., .F., .T. ) 
 B_SPLINE_SURFACE_WITH_KNOTS ( ( 4, 4 ),
 ( 2, 2 ),
 ( 0.000000000000000000, 1.000000000000000000 ),
 ( 0.000000000000000000, 1.000000000000000000 ),
 .UNSPECIFIED. ) 
 GEOMETRIC_REPRESENTATION_ITEM ( )  RATIONAL_B_SPLINE_SURFACE ( (
 ( 1.000000000000000000, 1.000000000000000000),
 ( 0.9933953342250438912, 0.8357391271907739227),
 ( 0.9933953342250438912, 0.8357391271907739227),
 ( 1.000000000000000000, 1.000000000000000000) ) ) 
 REPRESENTATION_ITEM ( '' )  SURFACE ( )  );
#4046=CARTESIAN_POINT ( 'NONE',  ( 1.846138399168762101, 0.4167076046095548603, 12.43476674860266762 ) ) ;
#4050=CARTESIAN_POINT ( 'NONE',  ( 0.3150686449036038117, 11.02450593298030412, -8.199336701264417826 ) ) ;
#4055=EDGE_LOOP ( 'NONE', ( #11331, #17472, #4124, #8309 ) ) ;
#4056=CARTESIAN_POINT ( 'NONE',  ( 3.512766787570746452, -10.40533104696126898, -10.87507422923902034 ) ) ;
#4058=B_SPLINE_CURVE_WITH_KNOTS ( 'NONE', 3,
 ( #18540, #16743, #3642, #11291, #16829, #12436 ),
 .UNSPECIFIED., .F., .F.,
 ( 4, 2, 4 ),
 ( 1.084202172485504314E-19, 0.001657017934711308349, 0.003314035869422615830 ),
 .UNSPECIFIED. ) ;
#4060=DIRECTION ( 'NONE',  ( 0.000000000000000000, 0.000000000000000000, 1.000000000000000000 ) ) ;
#4063=CARTESIAN_POINT ( 'NONE',  ( 2.636624412716062515, -6.973567714909003179, -14.46769361191335790 ) ) ;
#4067=CARTESIAN_POINT ( 'NONE',  ( 0.4754618798421171855, -8.775436892861030458, -10.80499583390522744 ) ) ;
#4068=CARTESIAN_POINT ( 'NONE',  ( 1.846138399168762101, -12.43476674860266940, 0.4167076046095114505 ) ) ;
#4071=AXIS2_PLACEMENT_3D ( 'NONE', #11262, #17259, #12677 ) ;
#4076=ORIENTED_EDGE ( 'NONE', *, *, #1185, .F. ) ;
#4077=CARTESIAN_POINT ( 'NONE',  ( 2.002547531651519996, -12.17374746633580784, 3.242439124566603326 ) ) ;
#4078=CARTESIAN_POINT ( 'NONE',  ( 0.3939875929385642239, -0.7003304234512184312, -13.80036004410494854 ) ) ;
#4080=VERTEX_POINT ( 'NONE', #5311 ) ;
#4087=DIRECTION ( 'NONE',  ( -1.000000000000000000, -0.000000000000000000, -0.000000000000000000 ) ) ;
#4090=CARTESIAN_POINT ( 'NONE',  ( 1.847380140988739594, -3.740232970470839913, 11.86779270755357807 ) ) ;
#4093=ORIENTED_EDGE ( 'NONE', *, *, #10331, .F. ) ;
#4102=VERTEX_POINT ( 'NONE', #11378 ) ;
#4106=CARTESIAN_POINT ( 'NONE',  ( 8.522092701127531811, -4.388629235579615262, 5.397361180353127175 ) ) ;
#4108=CARTESIAN_POINT ( 'NONE',  ( 3.950837973638675393, 6.888253895133292559, 12.81214529934977797 ) ) ;
#4122=CARTESIAN_POINT ( 'NONE',  ( 0.3132642857406563452, -0.5276792104583234444, 13.72733058964894326 ) ) ;
#4123=EDGE_CURVE ( 'NONE', #16044, #1784, #17198, .T. ) ;
#4124=ORIENTED_EDGE ( 'NONE', *, *, #8624, .T. ) ;
#4125=CARTESIAN_POINT ( 'NONE',  ( 3.950837973638675393, -13.10350451991845055, 6.316429227969417859 ) ) ;
#4126=EDGE_CURVE ( 'NONE', #8651, #10554, #11341, .T. ) ;
#4133=CARTESIAN_POINT ( 'NONE',  ( 0.3145729642390356351, -0.3065092323350255277, -13.73540280162741389 ) ) ;
#4142=CARTESIAN_POINT ( 'NONE',  ( 0.3137051932979775248, -12.91601973349273891, 4.679953077377436266 ) ) ;
#4145=CARTESIAN_POINT ( 'NONE',  ( 16.56679352167444819, -0.008311568981097361419, 0.004162264567719621902 ) ) ;
#4152=CARTESIAN_POINT ( 'NONE',  ( 16.56753206892534891, 0.001421777558675947238, -0.009389754735542250527 ) ) ;
#4155=LINE ( 'NONE', #15804, #17789 ) ;
#4160=CARTESIAN_POINT ( 'NONE',  ( 2.320520222538103638, 6.542539914241700671, -14.32454429810417906 ) ) ;
#4167=CARTESIAN_POINT ( 'NONE',  ( 16.57778382496167424, 0.01482878558584695486, -0.001819584982831739346 ) ) ;
#4171=VERTEX_POINT ( 'NONE', #3529 ) ;
#4178=AXIS2_PLACEMENT_3D ( 'NONE', #17302, #8247, #4221 ) ;
#4182=ORIENTED_EDGE ( 'NONE', *, *, #16689, .F. ) ;
#4183=CARTESIAN_POINT ( 'NONE',  ( 3.353306896162455697, 13.88482890973696726, 1.348936822032873240 ) ) ;
#4185=EDGE_CURVE ( 'NONE', #181, #5397, #17747, .T. ) ;
#4190=CARTESIAN_POINT ( 'NONE',  ( 2.320521194583481606, -1.795798718314370213, -15.64520804578356561 ) ) ;
#4191=B_SPLINE_CURVE_WITH_KNOTS ( 'NONE', 3,
 ( #4876, #4681, #11945, #4775 ),
 .UNSPECIFIED., .F., .F.,
 ( 4, 4 ),
 ( 4.336808689942017736E-19, 0.003005512676784827947 ),
 .UNSPECIFIED. ) ;
#4194=CARTESIAN_POINT ( 'NONE',  ( 1.846613052777652531, -3.520031056876387954, 11.93415846513960332 ) ) ;
#4196=ORIENTED_EDGE ( 'NONE', *, *, #14979, .F. ) ;
#4199=VERTEX_POINT ( 'NONE', #15095 ) ;
#4204=CARTESIAN_POINT ( 'NONE',  ( 3.950837973638668288, 0.000000000000000000, 0.000000000000000000 ) ) ;
#4205=CARTESIAN_POINT ( 'NONE',  ( 16.58200780006414732, 0.008650561019685807859, 0.007066318000006031885 ) ) ;
#4206=CARTESIAN_POINT ( 'NONE',  ( 16.56753206892534891, -0.001549402974393209202, 0.009369540855502124857 ) ) ;
#4212=CARTESIAN_POINT ( 'NONE',  ( 1.342453679581834924, 14.34050741580207067, 3.649820028552781093 ) ) ;
#4214=EDGE_CURVE ( 'NONE', #1603, #2481, #6020, .T. ) ;
#4221=DIRECTION ( 'NONE',  ( 0.000000000000000000, 0.000000000000000000, 1.000000000000000000 ) ) ;
#4225=DIRECTION ( 'NONE',  ( 0.000000000000000000, 0.000000000000000000, -1.000000000000000000 ) ) ;
#4226=ORIENTED_EDGE ( 'NONE', *, *, #17570, .F. ) ;
#4227=CARTESIAN_POINT ( 'NONE',  ( 2.705023505549863039, -12.36217802824809020, 4.909285963184022883 ) ) ;
#4228=CARTESIAN_POINT ( 'NONE',  ( 2.636624412715362631, -15.80357026013197519, 2.862162146984090327 ) ) ;
#4229=ORIENTED_EDGE ( 'NONE', *, *, #11914, .F. ) ;
#4231=CARTESIAN_POINT ( 'NONE',  ( 0.4862570985993252548, -3.580942890621766406, 13.44146924561379741 ) ) ;
#4233=CARTESIAN_POINT ( 'NONE',  ( 0.4862570985993252548, 3.580942890621670482, 13.44146924561382583 ) ) ;
#4236=ADVANCED_FACE ( 'NONE', ( #2013 ), #3354, .F. ) ;
#4242=DIRECTION ( 'NONE',  ( 0.7635533937278216055, 0.02138673900302332995, -0.6453904417649386493 ) ) ;
#4244=CARTESIAN_POINT ( 'NONE',  ( 1.846138399168762101, -12.43476674860266229, -0.4167076046096845898 ) ) ;
#4247=CARTESIAN_POINT ( 'NONE',  ( 0.4754618798421167414, -5.007009103465340338, 12.98792082933642966 ) ) ;
#4249=ORIENTED_EDGE ( 'NONE', *, *, #9691, .T. ) ;
#4254=ORIENTED_EDGE ( 'NONE', *, *, #4447, .T. ) ;
#4256=CARTESIAN_POINT ( 'NONE',  ( 1.846138399168762101, -10.30487220521565028, -6.971848976711123136 ) ) ;
#4259=CARTESIAN_POINT ( 'NONE',  ( 0.3095370825347233956, -7.700448427571951804, 11.38092634279625948 ) ) ;
#4261=CARTESIAN_POINT ( 'NONE',  ( 0.4385251269669980800, -3.577373010348622540, -13.39302348765812312 ) ) ;
#4262=CARTESIAN_POINT ( 'NONE',  ( 0.4385251269669942498, -10.76637725024245462, -8.732456510146192841 ) ) ;
#4275=EDGE_LOOP ( 'NONE', ( #9085, #15313, #12875, #17450 ) ) ;
#4280=CARTESIAN_POINT ( 'NONE',  ( 0.3137051932979792457, -10.83767969834809008, 8.442169467526815296 ) ) ;
#4285=CARTESIAN_POINT ( 'NONE',  ( 0.3939875929385661668, 4.930599594904554017, 12.90850834464102270 ) ) ;
#4287=EDGE_LOOP ( 'NONE', ( #4480, #15707, #17179, #10381 ) ) ;
#4291=VERTEX_POINT ( 'NONE', #18514 ) ;
#4296=CARTESIAN_POINT ( 'NONE',  ( 3.950837973638668288, 0.000000000000000000, 0.000000000000000000 ) ) ;
#4302=DIRECTION ( 'NONE',  ( 0.000000000000000000, 0.000000000000000000, -1.000000000000000000 ) ) ;
#4303=DIRECTION ( 'NONE',  ( 0.000000000000000000, 0.000000000000000000, 1.000000000000000000 ) ) ;
#4308=AXIS2_PLACEMENT_3D ( 'NONE', #10712, #15203, #6596 ) ;
#4315=EDGE_CURVE ( 'NONE', #5180, #11553, #2235, .T. ) ;
#4317=CARTESIAN_POINT ( 'NONE',  ( 1.846955891736115740, 10.21904526726846640, 7.098901504650394934 ) ) ;
#4324=CARTESIAN_POINT ( 'NONE',  ( 0.3132642857406524040, 3.740125687984731773, 13.21852905223340535 ) ) ;
#4329=CARTESIAN_POINT ( 'NONE',  ( 1.846138399168762101, 0.4167076046095548603, 12.43476674860266762 ) ) ;
#4334=CARTESIAN_POINT ( 'NONE',  ( 16.56679352167444819, -0.004277682826583350043, -0.008252760440870175046 ) ) ;
#4336=EDGE_CURVE ( 'NONE', #3103, #14004, #7947, .T. ) ;
#4338=EDGE_CURVE ( 'NONE', #15500, #4964, #14033, .T. ) ;
#4341=VERTEX_POINT ( 'NONE', #8301 ) ;
#4348=CARTESIAN_POINT ( 'NONE',  ( 2.320521194584331148, 11.60169518685982304, -10.64885423995325198 ) ) ;
#4349=EDGE_CURVE ( 'NONE', #12310, #7136, #17494, .T. ) ;
#4354=CARTESIAN_POINT ( 'NONE',  ( 0.3137051932979757485, 13.73004976592202020, -0.4596302728640235258 ) ) ;
#4362=CARTESIAN_POINT ( 'NONE',  ( 1.846822687350018644, 4.121816957446363894, -11.74004266906800353 ) ) ;
#4366=CARTESIAN_POINT ( 'NONE',  ( 2.636624412714763555, 6.973567714907159321, 14.46769361191226722 ) ) ;
#4367=CARTESIAN_POINT ( 'NONE',  ( 1.342453679581834924, -0.9602753779831757486, 14.76648944001038899 ) ) ;
#4369=CARTESIAN_POINT ( 'NONE',  ( 3.950837973638668288, 14.41405733518061538, -1.958075594453841273 ) ) ;
#4370=CARTESIAN_POINT ( 'NONE',  ( 0.3137051932979792457, -11.37800749014136592, 7.698472063774431717 ) ) ;
#4372=CARTESIAN_POINT ( 'NONE',  ( 1.846138399168762101, 0.4167076046097279440, -12.43476674860266051 ) ) ;
#4373=CARTESIAN_POINT ( 'NONE',  ( 0.3095370825347233956, -11.38092634279623105, -7.700448427571997101 ) ) ;
#4382=ORIENTED_EDGE ( 'NONE', *, *, #4336, .T. ) ;
#4390=ADVANCED_FACE ( 'NONE', ( #15367 ), #1284, .F. ) ;
#4399=ORIENTED_EDGE ( 'NONE', *, *, #3927, .T. ) ;
#4400=CARTESIAN_POINT ( 'NONE',  ( 0.3058872367615230181, 3.664492643742949252, -13.24582953854921463 ) ) ;
#4402=LINE ( 'NONE', #10237, #2478 ) ;
#4406=VERTEX_POINT ( 'NONE', #7145 ) ;
#4414=VECTOR ( 'NONE', #3982, 1000.000000000000000 ) ;
#4422=VECTOR ( 'NONE', #982, 1000.000000000000114 ) ;
#4424=CARTESIAN_POINT ( 'NONE',  ( 0.3145734862173242830, 11.29227530924457312, -7.825584895511399353 ) ) ;
#4430=CARTESIAN_POINT ( 'NONE',  ( 0.3307726912345191894, -4.812300915532890855, -12.88561780039863436 ) ) ;
#4433=EDGE_LOOP ( 'NONE', ( #5874, #3791, #16540, #6204 ) ) ;
#4434=CARTESIAN_POINT ( 'NONE',  ( 3.377929128793398128, 7.136734442941011558, -12.02809354424093691 ) ) ;
#4436=DIRECTION ( 'NONE',  ( -1.000000000000000000, -0.000000000000000000, -0.000000000000000000 ) ) ;
#4437=( BOUNDED_SURFACE ( )  B_SPLINE_SURFACE ( 3, 1, ( 
 ( #1133, #15473 ),
 ( #8045, #18428 ),
 ( #2288, #11368 ),
 ( #16910, #12511 ) ),
 .UNSPECIFIED., .F., .F., .T. ) 
 B_SPLINE_SURFACE_WITH_KNOTS ( ( 4, 4 ),
 ( 2, 2 ),
 ( 0.000000000000000000, 1.000000000000000000 ),
 ( 0.000000000000000000, 1.000000000000000000 ),
 .UNSPECIFIED. ) 
 GEOMETRIC_REPRESENTATION_ITEM ( )  RATIONAL_B_SPLINE_SURFACE ( (
 ( 1.000000000000000000, 1.000000000000000000),
 ( 0.9933953342250438912, 0.8357391271907739227),
 ( 0.9933953342250438912, 0.8357391271907739227),
 ( 1.000000000000000000, 1.000000000000000000) ) ) 
 REPRESENTATION_ITEM ( '' )  SURFACE ( )  );
#4438=CARTESIAN_POINT ( 'NONE',  ( 0.3151926232592501265, 4.318679262939624230, 13.04305446098357635 ) ) ;
#4445=EDGE_CURVE ( 'NONE', #5155, #5851, #18429, .T. ) ;
#4447=EDGE_CURVE ( 'NONE', #15917, #5851, #15653, .T. ) ;
#4468=EDGE_CURVE ( 'NONE', #3512, #17476, #7010, .T. ) ;
#4469=EDGE_CURVE ( 'NONE', #11211, #3961, #2726, .T. ) ;
#4470=DIRECTION ( 'NONE',  ( 0.000000000000000000, 0.000000000000000000, -1.000000000000000000 ) ) ;
#4480=ORIENTED_EDGE ( 'NONE', *, *, #8314, .F. ) ;
#4481=ORIENTED_EDGE ( 'NONE', *, *, #2994, .T. ) ;
#4490=CARTESIAN_POINT ( 'NONE',  ( 0.4754618798421167414, 12.98792082933644743, 5.007009103465293265 ) ) ;
#4492=FACE_OUTER_BOUND ( 'NONE', #14439, .T. ) ;
#4493=ORIENTED_EDGE ( 'NONE', *, *, #3206, .T. ) ;
#4495=AXIS2_PLACEMENT_3D ( 'NONE', #2684, #8620, #11402 ) ;
#4499=CARTESIAN_POINT ( 'NONE',  ( 0.3137051932979792457, 8.442169467527008919, -10.83767969834794087 ) ) ;
#4502=CARTESIAN_POINT ( 'NONE',  ( 3.950837973638677170, 1.958075594453790869, 14.41405733518061538 ) ) ;
#4504=EDGE_CURVE ( 'NONE', #7817, #9425, #8571, .T. ) ;
#4512=CARTESIAN_POINT ( 'NONE',  ( 3.074695600507137083, -11.23985886659436773, -10.75417554975720869 ) ) ;
#4518=DIRECTION ( 'NONE',  ( -1.000000000000000000, -0.000000000000000000, -0.000000000000000000 ) ) ;
#4520=ORIENTED_EDGE ( 'NONE', *, *, #1001, .T. ) ;
#4524=CARTESIAN_POINT ( 'NONE',  ( 1.846138399168762101, -0.4167076046096411246, 12.43476674860266407 ) ) ;
#4535=CARTESIAN_POINT ( 'NONE',  ( 0.8740764193766769052, -13.83508774436000088, 3.609949042658186169 ) ) ;
#4536=EDGE_LOOP ( 'NONE', ( #8273, #13828, #6197, #7186 ) ) ;
#4537=FACE_OUTER_BOUND ( 'NONE', #5213, .T. ) ;
#4540=CARTESIAN_POINT ( 'NONE',  ( 0.4384471787762841966, -0.7363690479465361260, -13.84291427302852817 ) ) ;
#4541=DIRECTION ( 'NONE',  ( -1.000000000000000000, -0.000000000000000000, -0.000000000000000000 ) ) ;
#4557=( BOUNDED_SURFACE ( )  B_SPLINE_SURFACE ( 3, 1, ( 
 ( #16590, #17832 ),
 ( #13518, #6369 ),
 ( #12097, #10666 ),
 ( #13716, #2067 ) ),
 .UNSPECIFIED., .F., .F., .T. ) 
 B_SPLINE_SURFACE_WITH_KNOTS ( ( 4, 4 ),
 ( 2, 2 ),
 ( 0.000000000000000000, 1.000000000000000000 ),
 ( 0.000000000000000000, 1.000000000000000000 ),
 .UNSPECIFIED. ) 
 GEOMETRIC_REPRESENTATION_ITEM ( )  RATIONAL_B_SPLINE_SURFACE ( (
 ( 1.000000000000000000, 1.000000000000000000),
 ( 0.9933953342250436691, 0.8357391271907733676),
 ( 0.9933953342250436691, 0.8357391271907733676),
 ( 1.000000000000000000, 1.000000000000000000) ) ) 
 REPRESENTATION_ITEM ( '' )  SURFACE ( )  );
#4558=EDGE_CURVE ( 'NONE', #10485, #15469, #16361, .T. ) ;
#4559=CARTESIAN_POINT ( 'NONE',  ( 0.3150686449036074199, 0.1533607327085746430, 13.73846184595213771 ) ) ;
#4560=FACE_OUTER_BOUND ( 'NONE', #10869, .T. ) ;
#4565=CARTESIAN_POINT ( 'NONE',  ( 8.438534575730034959, -6.598402093327866424, -1.899950616255257740 ) ) ;
#4566=CARTESIAN_POINT ( 'NONE',  ( 2.636624412714237309, 15.91454522070173638, -2.161493821596664144 ) ) ;
#4571=CARTESIAN_POINT ( 'NONE',  ( 1.861628059977343597, -9.751736252960316875, -7.751680370225499495 ) ) ;
#4575=ORIENTED_EDGE ( 'NONE', *, *, #7391, .T. ) ;
#4578=ORIENTED_EDGE ( 'NONE', *, *, #7039, .F. ) ;
#4583=CARTESIAN_POINT ( 'NONE',  ( 1.918921323896324971, -6.832782632379298171, -10.48468902844559913 ) ) ;
#4592=CARTESIAN_POINT ( 'NONE',  ( 1.342453679581834924, 14.76648944001039254, 0.9602753779831241232 ) ) ;
#4594=( BOUNDED_SURFACE ( )  B_SPLINE_SURFACE ( 3, 1, ( 
 ( #7301, #8907 ),
 ( #10443, #14735 ),
 ( #13020, #1645 ),
 ( #17811, #14453 ) ),
 .UNSPECIFIED., .F., .F., .T. ) 
 B_SPLINE_SURFACE_WITH_KNOTS ( ( 4, 4 ),
 ( 2, 2 ),
 ( 0.000000000000000000, 1.000000000000000000 ),
 ( 0.000000000000000000, 1.000000000000000000 ),
 .UNSPECIFIED. ) 
 GEOMETRIC_REPRESENTATION_ITEM ( )  RATIONAL_B_SPLINE_SURFACE ( (
 ( 1.000000000000000000, 1.000000000000000000),
 ( 0.9933953342250438912, 0.8357391271907739227),
 ( 0.9933953342250438912, 0.8357391271907739227),
 ( 1.000000000000000000, 1.000000000000000000) ) ) 
 REPRESENTATION_ITEM ( '' )  SURFACE ( )  );
#4595=CARTESIAN_POINT ( 'NONE',  ( 16.56753206892534891, 0.001421777558676785977, 0.009389754735541558373 ) ) ;
#4599=ORIENTED_EDGE ( 'NONE', *, *, #9977, .F. ) ;
#4600=CARTESIAN_POINT ( 'NONE',  ( 0.3151930723728414985, 8.137566970826528134, -11.07033375389122831 ) ) ;
#4601=DIRECTION ( 'NONE',  ( 0.7635533937278216055, -0.3620487483322484823, -0.5347026451755951815 ) ) ;
#4602=VERTEX_POINT ( 'NONE', #17952 ) ;
#4609=EDGE_CURVE ( 'NONE', #18257, #18612, #5594, .T. ) ;
#4610=CARTESIAN_POINT ( 'NONE',  ( 2.002547531651519996, 3.242439124566821818, -12.17374746633574745 ) ) ;
#4611=CARTESIAN_POINT ( 'NONE',  ( 1.846138399168762101, -11.95493567637852905, 3.446241763652952539 ) ) ;
#4618=CARTESIAN_POINT ( 'NONE',  ( 1.845756295923353330, 0.4783934145702027352, 12.43231724724607190 ) ) ;
#4619=CARTESIAN_POINT ( 'NONE',  ( 2.002547531651519996, 0.6781519942173496185, -12.57989064830758785 ) ) ;
#4622=CARTESIAN_POINT ( 'NONE',  ( 0.3148213771069373057, -8.260246460850796169, 10.97836617636221845 ) ) ;
#4624=VERTEX_POINT ( 'NONE', #13248 ) ;
#4631=B_SPLINE_CURVE_WITH_KNOTS ( 'NONE', 3,
 ( #6473, #18037, #15526, #2170, #16601, #12298 ),
 .UNSPECIFIED., .F., .F.,
 ( 4, 2, 4 ),
 ( 4.005364051932256883E-17, 0.0002014099069817290285, 0.0004028198139634179956 ),
 .UNSPECIFIED. ) ;
#4633=CARTESIAN_POINT ( 'NONE',  ( 3.950837973638675393, 6.888253895133479965, -12.81214529934967672 ) ) ;
#4638=CARTESIAN_POINT ( 'NONE',  ( 0.3150686449036049219, 4.391272911157320991, 13.01866258978838609 ) ) ;
#4641=CARTESIAN_POINT ( 'NONE',  ( 3.950837973638676281, 12.81214529934975310, 6.888253895133341409 ) ) ;
#4645=CARTESIAN_POINT ( 'NONE',  ( 0.4862570985993235340, 13.44146924561385958, -3.580942890621532371 ) ) ;
#4653=B_SPLINE_CURVE_WITH_KNOTS ( 'NONE', 3,
 ( #15211, #12516, #8320, #1037 ),
 .UNSPECIFIED., .F., .F.,
 ( 4, 4 ),
 ( 1.226634733346699349E-18, 0.003005512676784830983 ),
 .UNSPECIFIED. ) ;
#4655=CARTESIAN_POINT ( 'NONE',  ( 3.664313757352974488, -12.97355833021536498, -5.926151963190507743 ) ) ;
#4656=ORIENTED_EDGE ( 'NONE', *, *, #14925, .F. ) ;
#4660=CARTESIAN_POINT ( 'NONE',  ( 0.4754618798421162973, -5.007009103465161814, -12.98792082933649539 ) ) ;
#4662=AXIS2_PLACEMENT_3D ( 'NONE', #10167, #1189, #5567 ) ;
#4672=( BOUNDED_SURFACE ( )  B_SPLINE_SURFACE ( 3, 1, ( 
 ( #5947, #1755 ),
 ( #7600, #17722 ),
 ( #13311, #11790 ),
 ( #7786, #9204 ) ),
 .UNSPECIFIED., .F., .F., .T. ) 
 B_SPLINE_SURFACE_WITH_KNOTS ( ( 4, 4 ),
 ( 2, 2 ),
 ( 0.000000000000000000, 1.000000000000000000 ),
 ( 0.000000000000000000, 1.000000000000000000 ),
 .UNSPECIFIED. ) 
 GEOMETRIC_REPRESENTATION_ITEM ( )  RATIONAL_B_SPLINE_SURFACE ( (
 ( 1.000000000000000000, 1.000000000000000000),
 ( 0.7792777138730158093, 0.9689936506012928330),
 ( 0.7792777138730158093, 0.9689936506012928330),
 ( 1.000000000000000000, 1.000000000000000000) ) ) 
 REPRESENTATION_ITEM ( '' )  SURFACE ( )  );
#4678=CARTESIAN_POINT ( 'NONE',  ( 1.846138399168762989, 11.69739621335922308, 4.238866729160444713 ) ) ;
#4680=ORIENTED_EDGE ( 'NONE', *, *, #13170, .T. ) ;
#4681=CARTESIAN_POINT ( 'NONE',  ( 3.377929128793385249, 13.64476897106782971, 3.070552481924919253 ) ) ;
#4683=CARTESIAN_POINT ( 'NONE',  ( 0.3145734862173258373, 12.96846406299306587, 4.535879238194977070 ) ) ;
#4687=DIRECTION ( 'NONE',  ( -0.7635533937278216055, 0.02138673900301891681, 0.6453904417649388714 ) ) ;
#4689=CARTESIAN_POINT ( 'NONE',  ( 3.512766787570699822, -13.55823433651950616, -6.535475144497160827 ) ) ;
#4691=EDGE_CURVE ( 'NONE', #13997, #3393, #12293, .T. ) ;
#4695=ORIENTED_EDGE ( 'NONE', *, *, #11637, .F. ) ;
#4699=CARTESIAN_POINT ( 'NONE',  ( 0.4385251269669976359, -4.978066129061780032, 12.93791070501032436 ) ) ;
#4701=CARTESIAN_POINT ( 'NONE',  ( 0.3939822652208129217, -12.90851734139303453, -4.930560016699199188 ) ) ;
#4702=CARTESIAN_POINT ( 'NONE',  ( 0.000000000000000000, 0.000000000000000000, -13.42403576283810906 ) ) ;
#4704=DIRECTION ( 'NONE',  ( -0.7561779333270775005, 0.3559159372837393809, -0.5491072561318300904 ) ) ;
#4707=CARTESIAN_POINT ( 'NONE',  ( 16.58200780006414732, 0.002844973367391573534, -0.01080144354108867819 ) ) ;
#4712=CARTESIAN_POINT ( 'NONE',  ( 2.747332970342022840, -14.49942876448597673, 7.555624153089596895 ) ) ;
#4715=CARTESIAN_POINT ( 'NONE',  ( 16.56753206892534891, 0.004368917149004243779, -0.008432171035096398468 ) ) ;
#4718=EDGE_CURVE ( 'NONE', #5038, #9139, #16858, .T. ) ;
#4719=ORIENTED_EDGE ( 'NONE', *, *, #5927, .F. ) ;
#4722=ORIENTED_EDGE ( 'NONE', *, *, #6828, .T. ) ;
#4726=CARTESIAN_POINT ( 'NONE',  ( 16.56872352241294521, -0.01027347319884440620, 0.001821578298044753286 ) ) ;
#4728=ORIENTED_EDGE ( 'NONE', *, *, #14023, .F. ) ;
#4732=CARTESIAN_POINT ( 'NONE',  ( 0.3137051932979792457, 12.91601973349270871, 4.679953077377533965 ) ) ;
#4746=ORIENTED_EDGE ( 'NONE', *, *, #9977, .T. ) ;
#4748=CARTESIAN_POINT ( 'NONE',  ( 0.3151928478948580192, 0.0001388664989280257334, 13.73922860964089665 ) ) ;
#4752=CARTESIAN_POINT ( 'NONE',  ( 1.846955891736115740, -12.44001089941741967, 0.2634721419534765685 ) ) ;
#4759=CARTESIAN_POINT ( 'NONE',  ( 1.847034903785825799, 0.2299360331935915713, -12.44051878787772480 ) ) ;
#4770=CARTESIAN_POINT ( 'NONE',  ( 16.56753206892534891, 0.004253784598196176658, -0.008490833999798941267 ) ) ;
#4773=DIRECTION ( 'NONE',  ( -0.7635533937278214944, 0.3966532189476597581, 0.5095610256143870975 ) ) ;
#4775=CARTESIAN_POINT ( 'NONE',  ( 2.002547531651519996, 12.17374746633578475, 3.242439124566693476 ) ) ;
#4776=CARTESIAN_POINT ( 'NONE',  ( 0.3720661004400037664, -7.524064345033377954, -11.58636699658223179 ) ) ;
#4779=CARTESIAN_POINT ( 'NONE',  ( 2.747332970342022840, -2.705255688517959722, 16.12459247543625551 ) ) ;
#4781=CARTESIAN_POINT ( 'NONE',  ( 2.002547531651519996, 4.532360870844327039, 11.75462648437103752 ) ) ;
#4782=ADVANCED_FACE ( 'NONE', ( #18621 ), #7775, .T. ) ;
#4785=VERTEX_POINT ( 'NONE', #15945 ) ;
#4786=CARTESIAN_POINT ( 'NONE',  ( 0.8740779401508858015, -11.05257166392043722, 9.070947476926702890 ) ) ;
#4790=AXIS2_PLACEMENT_3D ( 'NONE', #7401, #16183, #2876 ) ;
#4791=CARTESIAN_POINT ( 'NONE',  ( 0.3095370825347224519, 7.700448427572037069, -11.38092634279620263 ) ) ;
#4793=B_SPLINE_CURVE_WITH_KNOTS ( 'NONE', 3,
 ( #3835, #18447, #14061, #15491 ),
 .UNSPECIFIED., .F., .F.,
 ( 4, 4 ),
 ( 6.158879127553505933E-17, 0.002004993803842649181 ),
 .UNSPECIFIED. ) ;
#4795=ORIENTED_EDGE ( 'NONE', *, *, #7528, .F. ) ;
#4804=VECTOR ( 'NONE', #10036, 1000.000000000000114 ) ;
#4807=AXIS2_PLACEMENT_3D ( 'NONE', #14477, #14300, #11159 ) ;
#4809=ORIENTED_EDGE ( 'NONE', *, *, #695, .T. ) ;
#4811=CARTESIAN_POINT ( 'NONE',  ( 16.57210152137263393, -0.005118120558002011225, -0.01361613799508959964 ) ) ;
#4813=CARTESIAN_POINT ( 'NONE',  ( 16.56782317627811096, 0.005492611183757310257, -0.008141063682853423578 ) ) ;
#4817=VERTEX_POINT ( 'NONE', #2934 ) ;
#4818=CARTESIAN_POINT ( 'NONE',  ( 0.3151926232592506816, -4.172630140040890723, 13.09050869763091107 ) ) ;
#4823=ORIENTED_EDGE ( 'NONE', *, *, #12286, .T. ) ;
#4831=CARTESIAN_POINT ( 'NONE',  ( 1.846138399168762101, 9.815003036200520725, -7.646096044339786069 ) ) ;
#4832=CARTESIAN_POINT ( 'NONE',  ( 0.3137051932979809665, 3.805684345189785933, 13.20008686438107581 ) ) ;
#4834=CARTESIAN_POINT ( 'NONE',  ( 0.3145734862173242274, -0.3064017202076312341, 13.73540602248381148 ) ) ;
#4837=CARTESIAN_POINT ( 'NONE',  ( 3.512766787570925864, 13.25664064834466593, -7.127386085302575225 ) ) ;
#4838=ORIENTED_EDGE ( 'NONE', *, *, #2185, .F. ) ;
#4839=CARTESIAN_POINT ( 'NONE',  ( 0.3145734862173244495, 7.825584895511528138, 11.29227530924448430 ) ) ;
#4843=ORIENTED_EDGE ( 'NONE', *, *, #13834, .F. ) ;
#4845=ORIENTED_EDGE ( 'NONE', *, *, #10541, .F. ) ;
#4853=ADVANCED_FACE ( 'NONE', ( #18712 ), #9188, .F. ) ;
#4855=CARTESIAN_POINT ( 'NONE',  ( 2.002547531651519996, 11.75462648437108015, -4.532360870844206246 ) ) ;
#4858=CARTESIAN_POINT ( 'NONE',  ( 16.56822296793089322, -0.01011126603341003585, -0.0007467251401289729364 ) ) ;
#4859=CARTESIAN_POINT ( 'NONE',  ( 16.56753206892534891, -0.004368917149005391298, -0.008432171035096433162 ) ) ;
#4867=CARTESIAN_POINT ( 'NONE',  ( 16.56822296793089322, 0.002414375228568254022, -0.009847136207496285168 ) ) ;
#4870=CARTESIAN_POINT ( 'NONE',  ( 1.977436885025426694, 15.33079650480377154, 1.488549889121579817 ) ) ;
#4871=CIRCLE ( 'NONE', #9737, 16.06066017081991149 ) ;
#4876=CARTESIAN_POINT ( 'NONE',  ( 3.950837973638676281, 14.31366178983253512, 2.591948120961855118 ) ) ;
#4881=CARTESIAN_POINT ( 'NONE',  ( 1.846524061778018311, -10.27028962889602148, 7.023652644192237560 ) ) ;
#4883=CARTESIAN_POINT ( 'NONE',  ( 2.705023505549864371, 4.909285963184069956, 12.36217802824807421 ) ) ;
#4885=CARTESIAN_POINT ( 'NONE',  ( 0.3142011359265314829, 12.94258167753018895, -4.608101617236642689 ) ) ;
#4887=ORIENTED_EDGE ( 'NONE', *, *, #408, .T. ) ;
#4888=CARTESIAN_POINT ( 'NONE',  ( 0.4862570985993252548, 12.97920246947879441, 5.003653737315533867 ) ) ;
#4889=CARTESIAN_POINT ( 'NONE',  ( 16.57778382496167424, 0.007244066302946777433, 0.01306626476309292149 ) ) ;
#4893=CARTESIAN_POINT ( 'NONE',  ( 0.3137051932979775248, 10.83767969834815581, -8.442169467526731808 ) ) ;
#4899=CARTESIAN_POINT ( 'NONE',  ( 8.438534575730034959, -6.862570336891077538, 0.2320579683289888395 ) ) ;
#4905=CARTESIAN_POINT ( 'NONE',  ( 16.56822296793089322, 0.006547366384935510326, -0.007741272030791107074 ) ) ;
#4907=EDGE_LOOP ( 'NONE', ( #2976, #5526, #8634, #1539 ) ) ;
#4917=DIRECTION ( 'NONE',  ( 0.000000000000000000, 0.000000000000000000, 1.000000000000000000 ) ) ;
#4923=CARTESIAN_POINT ( 'NONE',  ( 2.002547531651520885, -4.532360870844412304, 11.75462648437100377 ) ) ;
#4924=CARTESIAN_POINT ( 'NONE',  ( 0.3148213771069364175, -0.2297580318215671491, 13.73693585713734144 ) ) ;
#4925=CARTESIAN_POINT ( 'NONE',  ( 16.56872352241294521, 0.009382111268607367521, 0.004564908236399998868 ) ) ;
#4927=CARTESIAN_POINT ( 'NONE',  ( 0.3137051932979792457, 0.4596302728641686874, -13.73004976592201487 ) ) ;
#4928=CARTESIAN_POINT ( 'NONE',  ( 0.3145729642390364678, 8.321438378985256179, 10.93201268464375353 ) ) ;
#4930=ADVANCED_FACE ( 'NONE', ( #1611 ), #16516, .F. ) ;
#4931=EDGE_CURVE ( 'NONE', #16009, #6505, #18439, .T. ) ;
#4935=VERTEX_POINT ( 'NONE', #9166 ) ;
#4939=ORIENTED_EDGE ( 'NONE', *, *, #16581, .T. ) ;
#4940=B_SPLINE_CURVE_WITH_KNOTS ( 'NONE', 3,
 ( #15688, #15788, #14080, #6818, #2774, #8531 ),
 .UNSPECIFIED., .F., .F.,
 ( 4, 2, 4 ),
 ( 3.522439207679730663E-17, 0.0001825746017570583171, 0.0003651492035140813976 ),
 .UNSPECIFIED. ) ;
#4941=CARTESIAN_POINT ( 'NONE',  ( 1.918921323896324971, 0.6349083173281891979, -12.49850046818173688 ) ) ;
#4945=ORIENTED_EDGE ( 'NONE', *, *, #10626, .T. ) ;
#4948=CARTESIAN_POINT ( 'NONE',  ( 0.3308579732647032867, 10.76782854710826776, 8.558831104906948539 ) ) ;
#4949=CARTESIAN_POINT ( 'NONE',  ( 0.4754618798421162973, 10.80499583390525586, -8.775436892860994931 ) ) ;
#4952=CARTESIAN_POINT ( 'NONE',  ( 2.002547531651519996, 3.242439124566649511, 12.17374746633579541 ) ) ;
#4961=CARTESIAN_POINT ( 'NONE',  ( 3.950837973638677170, 12.81214529934985080, -6.888253895133152227 ) ) ;
#4964=VERTEX_POINT ( 'NONE', #17971 ) ;
#4967=CARTESIAN_POINT ( 'NONE',  ( 0.3150686449036101955, 13.11344473514187925, 4.099563462784696632 ) ) ;
#4969=CARTESIAN_POINT ( 'NONE',  ( 1.847412631396506022, -10.09191835241968427, 7.278870946904215877 ) ) ;
#4979=CARTESIAN_POINT ( 'NONE',  ( 1.846138399168762101, -4.238866729160323032, -11.69739621335926394 ) ) ;
#4985=CARTESIAN_POINT ( 'NONE',  ( 1.846138399168762101, -11.95493567637848109, -3.446241763653124401 ) ) ;
#4986=CARTESIAN_POINT ( 'NONE',  ( 1.847380140988738484, 10.00162556679661741, -7.402792205948994564 ) ) ;
#4987=EDGE_CURVE ( 'NONE', #2340, #10438, #6134, .T. ) ;
#4989=CARTESIAN_POINT ( 'NONE',  ( 0.4754618798421167414, -11.68486377711971613, 7.564402563418431313 ) ) ;
#4993=CARTESIAN_POINT ( 'NONE',  ( 2.636624412715138366, -11.10302021257964888, 11.60464335004044223 ) ) ;
#4995=CARTESIAN_POINT ( 'NONE',  ( 16.56753206892534891, 0.009369540855502130061, 0.001549402974393180796 ) ) ;
#5002=VERTEX_POINT ( 'NONE', #9860 ) ;
#5003=CARTESIAN_POINT ( 'NONE',  ( 3.512766787570793969, 2.025881399556391127, 14.91422000116820179 ) ) ;
#5013=CARTESIAN_POINT ( 'NONE',  ( 0.4754618798421162973, 7.564402563418637371, -11.68486377711958468 ) ) ;
#5014=CARTESIAN_POINT ( 'NONE',  ( 2.697797270744668019, -3.226410068829341338, -12.89731672021093090 ) ) ;
#5018=B_SPLINE_CURVE_WITH_KNOTS ( 'NONE', 3,
 ( #8945, #9517, #15525, #3686, #8096, #3598 ),
 .UNSPECIFIED., .F., .F.,
 ( 4, 2, 4 ),
 ( 2.239080928920849783E-18, 0.0002017457492448096685, 0.0004034914984896170601 ),
 .UNSPECIFIED. ) ;
#5020=CARTESIAN_POINT ( 'NONE',  ( 16.56753206892534891, -0.001549402974394225099, -0.009369540855502527313 ) ) ;
#5021=ORIENTED_EDGE ( 'NONE', *, *, #3206, .F. ) ;
#5023=ORIENTED_EDGE ( 'NONE', *, *, #9195, .T. ) ;
#5026=CARTESIAN_POINT ( 'NONE',  ( 0.3150686449036065317, 11.20479228691397822, 7.951193823202440392 ) ) ;
#5029=ADVANCED_FACE ( 'NONE', ( #17136 ), #5877, .F. ) ;
#5031=CARTESIAN_POINT ( 'NONE',  ( 1.977436885026408353, 1.488549889122500192, -15.33079650480466860 ) ) ;
#5032=VECTOR ( 'NONE', #2467, 1000.000000000000114 ) ;
#5034=CARTESIAN_POINT ( 'NONE',  ( 0.4862570985993252548, 13.44146924561381162, 3.580942890621718888 ) ) ;
#5036=CARTESIAN_POINT ( 'NONE',  ( 0.3170788640506440603, -7.952793437297492218, -11.20690911610912543 ) ) ;
#5037=CARTESIAN_POINT ( 'NONE',  ( 3.664313757352971823, 2.831308606787245719, 13.97913389346634183 ) ) ;
#5038=VERTEX_POINT ( 'NONE', #14360 ) ;
#5039=ORIENTED_EDGE ( 'NONE', *, *, #11914, .T. ) ;
#5042=EDGE_LOOP ( 'NONE', ( #6703, #17230, #838, #5228 ) ) ;
#5045=CARTESIAN_POINT ( 'NONE',  ( 1.342453679581834924, 9.456403821038797730, 11.38190519890856933 ) ) ;
#5051=FACE_OUTER_BOUND ( 'NONE', #11840, .T. ) ;
#5052=EDGE_CURVE ( 'NONE', #14724, #8524, #6613, .T. ) ;
#5056=CARTESIAN_POINT ( 'NONE',  ( 16.56872352241294521, 0.009382111268606257298, -0.004564908236400254740 ) ) ;
#5060=CARTESIAN_POINT ( 'NONE',  ( 0.3148213771069354738, 13.13560149728606419, -4.026433757158845772 ) ) ;
#5063=ORIENTED_EDGE ( 'NONE', *, *, #10218, .T. ) ;
#5064=CARTESIAN_POINT ( 'NONE',  ( 2.123976203522053741, -11.67822624909933005, 10.37815841598487765 ) ) ;
#5067=ORIENTED_EDGE ( 'NONE', *, *, #16170, .T. ) ;
#5068=CARTESIAN_POINT ( 'NONE',  ( 0.3720661004400040439, 11.58636699658215541, 7.524064345033506740 ) ) ;
#5072=ORIENTED_EDGE ( 'NONE', *, *, #6420, .F. ) ;
#5086=B_SPLINE_CURVE_WITH_KNOTS ( 'NONE', 3,
 ( #424, #16389, #3276, #12088, #7407, #17921 ),
 .UNSPECIFIED., .F., .F.,
 ( 4, 2, 4 ),
 ( 4.336808689942017736E-19, 0.0001828790815886937498, 0.0003657581631773870658 ),
 .UNSPECIFIED. ) ;
#5090=ORIENTED_EDGE ( 'NONE', *, *, #3408, .T. ) ;
#5096=B_SPLINE_CURVE_WITH_KNOTS ( 'NONE', 3,
 ( #1537, #16259, #14715, #16057 ),
 .UNSPECIFIED., .F., .F.,
 ( 4, 4 ),
 ( 2.168404344971008868E-17, 0.003005512676784848763 ),
 .UNSPECIFIED. ) ;
#5097=VERTEX_POINT ( 'NONE', #7210 ) ;
#5099=VECTOR ( 'NONE', #6375, 1000.000000000000114 ) ;
#5116=CARTESIAN_POINT ( 'NONE',  ( 8.522092701127531811, -5.397361180353174248, 4.388629235579559307 ) ) ;
#5117=VERTEX_POINT ( 'NONE', #14736 ) ;
#5119=VERTEX_POINT ( 'NONE', #224 ) ;
#5120=VERTEX_POINT ( 'NONE', #11786 ) ;
#5122=AXIS2_PLACEMENT_3D ( 'NONE', #9223, #17833, #2238 ) ;
#5124=CARTESIAN_POINT ( 'NONE',  ( 1.959283090834838870, -9.750336807931205385, 7.909254450748972154 ) ) ;
#5127=VERTEX_POINT ( 'NONE', #4619 ) ;
#5129=CARTESIAN_POINT ( 'NONE',  ( 8.522092701127531811, 6.489356537178190720, 2.505958102592644288 ) ) ;
#5134=EDGE_CURVE ( 'NONE', #2099, #7234, #17530, .T. ) ;
#5136=ORIENTED_EDGE ( 'NONE', *, *, #10427, .T. ) ;
#5150=CARTESIAN_POINT ( 'NONE',  ( 3.377929128793395908, -7.136734442940921852, 12.02809354424098665 ) ) ;
#5153=ORIENTED_EDGE ( 'NONE', *, *, #13866, .T. ) ;
#5154=CARTESIAN_POINT ( 'NONE',  ( 1.254009781011991453, -9.426200207651724838, -11.25324419414228494 ) ) ;
#5155=VERTEX_POINT ( 'NONE', #11683 ) ;
#5161=CARTESIAN_POINT ( 'NONE',  ( 1.846822687350018866, -0.2922081769261017925, 12.43915556955403723 ) ) ;
#5163=CARTESIAN_POINT ( 'NONE',  ( 1.846955891736120181, -4.094751675596620011, -11.74973605926568077 ) ) ;
#5165=( BOUNDED_SURFACE ( )  B_SPLINE_SURFACE ( 3, 1, ( 
 ( #14101, #1007 ),
 ( #5408, #9790 ),
 ( #4167, #2521 ),
 ( #7129, #12946 ) ),
 .UNSPECIFIED., .F., .F., .T. ) 
 B_SPLINE_SURFACE_WITH_KNOTS ( ( 4, 4 ),
 ( 2, 2 ),
 ( 0.000000000000000000, 1.000000000000000000 ),
 ( 0.000000000000000000, 1.000000000000000000 ),
 .UNSPECIFIED. ) 
 GEOMETRIC_REPRESENTATION_ITEM ( )  RATIONAL_B_SPLINE_SURFACE ( (
 ( 1.000000000000000000, 1.000000000000000000),
 ( 0.7792777138730160313, 0.9689936506012927220),
 ( 0.7792777138730160313, 0.9689936506012927220),
 ( 1.000000000000000000, 1.000000000000000000) ) ) 
 REPRESENTATION_ITEM ( '' )  SURFACE ( )  );
#5168=CARTESIAN_POINT ( 'NONE',  ( 0.4862570985993235340, -7.559321496869506163, 11.67702470553362559 ) ) ;
#5169=DIRECTION ( 'NONE',  ( 0.000000000000000000, 0.000000000000000000, 1.000000000000000000 ) ) ;
#5180=VERTEX_POINT ( 'NONE', #13208 ) ;
#5183=ORIENTED_EDGE ( 'NONE', *, *, #824, .T. ) ;
#5184=ORIENTED_EDGE ( 'NONE', *, *, #5354, .T. ) ;
#5187=DIRECTION ( 'NONE',  ( -1.000000000000000000, -0.000000000000000000, -0.000000000000000000 ) ) ;
#5188=ORIENTED_EDGE ( 'NONE', *, *, #10541, .T. ) ;
#5190=CARTESIAN_POINT ( 'NONE',  ( 1.845756295923353996, 6.920504327368345976, -10.33914852636097592 ) ) ;
#5198=CARTESIAN_POINT ( 'NONE',  ( 2.636624412715137478, -2.862162146983530775, 15.80357026013314048 ) ) ;
#5202=CARTESIAN_POINT ( 'NONE',  ( 1.847412631396503357, 7.348689888531986014, -10.04119192206678512 ) ) ;
#5206=CARTESIAN_POINT ( 'NONE',  ( 16.56679352167444819, 0.004277682826582259769, -0.008252760440870513317 ) ) ;
#5208=EDGE_LOOP ( 'NONE', ( #8729, #18264, #18857, #4076 ) ) ;
#5210=EDGE_CURVE ( 'NONE', #7697, #4027, #16399, .T. ) ;
#5213=EDGE_LOOP ( 'NONE', ( #7112, #2747, #5872, #1234 ) ) ;
#5214=DIRECTION ( 'NONE',  ( 0.7561779333270773895, 0.2350349629540228469, -0.6106991889125047424 ) ) ;
#5218=CARTESIAN_POINT ( 'NONE',  ( 0.8740779401508861346, -7.708543377337782054, 12.04241618260063618 ) ) ;
#5221=CARTESIAN_POINT ( 'NONE',  ( 2.636624412714237309, 14.14563173255211126, 7.605649742762011556 ) ) ;
#5222=AXIS2_PLACEMENT_3D ( 'NONE', #13476, #592, #12153 ) ;
#5223=CARTESIAN_POINT ( 'NONE',  ( 2.002547531651519996, -12.17374746633575988, -3.242439124566779185 ) ) ;
#5227=ORIENTED_EDGE ( 'NONE', *, *, #15690, .F. ) ;
#5228=ORIENTED_EDGE ( 'NONE', *, *, #4718, .F. ) ;
#5231=CARTESIAN_POINT ( 'NONE',  ( 16.58200780006414732, 0.01041078477704048856, 0.004047297414159084679 ) ) ;
#5236=ORIENTED_EDGE ( 'NONE', *, *, #6491, .T. ) ;
#5238=B_SPLINE_CURVE_WITH_KNOTS ( 'NONE', 3,
 ( #14140, #12896, #8239, #5359, #18719, #12988, #18820, #14336, #2562, #11568, #8328, #17389, #10029 ),
 .UNSPECIFIED., .F., .F.,
 ( 4, 3, 3, 3, 4 ),
 ( 4.670885906470169154E-18, 0.0002299780670421044384, 0.0004599561239687884940, 0.0006896788984287876298, 0.0009194956271626387621 ),
 .UNSPECIFIED. ) ;
#5245=CARTESIAN_POINT ( 'NONE',  ( 0.3151928476913548605, 13.06671852871095574, -4.245853234426248513 ) ) ;
#5257=CARTESIAN_POINT ( 'NONE',  ( 1.846822687350024417, -7.547953575784189795, 9.891732594446548177 ) ) ;
#5260=CARTESIAN_POINT ( 'NONE',  ( 1.846138399168762101, 9.815003036200520725, -7.646096044339786069 ) ) ;
#5269=DIRECTION ( 'NONE',  ( -0.7561779333270775005, 0.2350349629540185170, 0.6106991889125065187 ) ) ;
#5271=CARTESIAN_POINT ( 'NONE',  ( 0.3137051932979792457, -10.83767969834796929, -8.442169467526971616 ) ) ;
#5272=CARTESIAN_POINT ( 'NONE',  ( 1.846138399168762101, 4.238866729160568170, -11.69739621335917690 ) ) ;
#5274=ORIENTED_EDGE ( 'NONE', *, *, #2400, .T. ) ;
#5276=CARTESIAN_POINT ( 'NONE',  ( 0.4862570985993235340, -8.769551628660812170, 10.79774104611370333 ) ) ;
#5277=CARTESIAN_POINT ( 'NONE',  ( 3.353306896162455697, -7.069984850384722463, -12.02594772223104869 ) ) ;
#5282=CARTESIAN_POINT ( 'NONE',  ( 2.636624412714756005, -2.161493821597335607, 15.91454522070219113 ) ) ;
#5283=CARTESIAN_POINT ( 'NONE',  ( 0.3939875929385635023, -7.545068896001288827, 11.57636969881031241 ) ) ;
#5292=CARTESIAN_POINT ( 'NONE',  ( 0.3151926232592482946, -13.04305446098359056, 4.318679262939574492 ) ) ;
#5300=ORIENTED_EDGE ( 'NONE', *, *, #9989, .F. ) ;
#5302=CARTESIAN_POINT ( 'NONE',  ( 0.3151928476913548050, 11.11539186930587242, 8.075547435846990751 ) ) ;
#5304=CARTESIAN_POINT ( 'NONE',  ( 0.4862570985993235340, 13.89016912371017476, 0.7479633556562934604 ) ) ;
#5305=CARTESIAN_POINT ( 'NONE',  ( 3.512766787570778870, -6.535475144496882827, -13.55823433651953636 ) ) ;
#5308=LINE ( 'NONE', #12945, #17319 ) ;
#5310=EDGE_CURVE ( 'NONE', #17659, #492, #2926, .T. ) ;
#5311=CARTESIAN_POINT ( 'NONE',  ( 0.3137051932979792457, 7.698472063774471685, 11.37800749014133928 ) ) ;
#5312=FACE_OUTER_BOUND ( 'NONE', #10962, .T. ) ;
#5315=VERTEX_POINT ( 'NONE', #17031 ) ;
#5317=B_SPLINE_CURVE_WITH_KNOTS ( 'NONE', 3,
 ( #18371, #16667, #9405, #5277, #3373, #798 ),
 .UNSPECIFIED., .F., .F.,
 ( 4, 2, 4 ),
 ( 0.000000000000000000, 0.001500839035891551789, 0.003001678071783103578 ),
 .UNSPECIFIED. ) ;
#5321=EDGE_CURVE ( 'NONE', #16055, #796, #14063, .T. ) ;
#5324=B_SPLINE_CURVE_WITH_KNOTS ( 'NONE', 3,
 ( #2020, #4786, #13383, #17887, #7761, #10622 ),
 .UNSPECIFIED., .F., .F.,
 ( 4, 2, 4 ),
 ( 9.215718466126787689E-19, 0.001657017934710630505, 0.003314035869421260144 ),
 .UNSPECIFIED. ) ;
#5325=FACE_OUTER_BOUND ( 'NONE', #2633, .T. ) ;
#5330=CARTESIAN_POINT ( 'NONE',  ( 1.846138399168762101, -11.69739621335919111, -4.238866729160527314 ) ) ;
#5353=CARTESIAN_POINT ( 'NONE',  ( 0.8740764193772003754, 13.83508774436055511, -3.609949042658134211 ) ) ;
#5354=EDGE_CURVE ( 'NONE', #10558, #5097, #12905, .T. ) ;
#5356=AXIS2_PLACEMENT_3D ( 'NONE', #10757, #11997, #17831 ) ;
#5359=CARTESIAN_POINT ( 'NONE',  ( 0.3148213771069381384, -12.99360322443199678, -4.463459503829131592 ) ) ;
#5363=DIRECTION ( 'NONE',  ( -1.000000000000000000, -0.000000000000000000, -0.000000000000000000 ) ) ;
#5368=CARTESIAN_POINT ( 'NONE',  ( 0.8740764193764966050, 11.05257066464512405, 9.070946295053792241 ) ) ;
#5372=CARTESIAN_POINT ( 'NONE',  ( 2.002547531651519996, -0.6781519942172617998, 12.57989064830759318 ) ) ;
#5376=CARTESIAN_POINT ( 'NONE',  ( 1.562796894703937678, 0.000000000000000000, 0.000000000000000000 ) ) ;
#5377=CARTESIAN_POINT ( 'NONE',  ( 0.3151928478948589074, -0.0001388664988634735829, -13.73922860964089487 ) ) ;
#5385=CARTESIAN_POINT ( 'NONE',  ( 0.3151930723728423867, -13.09040889075573411, 4.172946285306520231 ) ) ;
#5386=( BOUNDED_SURFACE ( )  B_SPLINE_SURFACE ( 3, 1, ( 
 ( #11748, #13266 ),
 ( #17683, #10315 ),
 ( #8874, #11845 ),
 ( #6201, #9165 ) ),
 .UNSPECIFIED., .F., .F., .T. ) 
 B_SPLINE_SURFACE_WITH_KNOTS ( ( 4, 4 ),
 ( 2, 2 ),
 ( 0.000000000000000000, 1.000000000000000000 ),
 ( 0.000000000000000000, 1.000000000000000000 ),
 .UNSPECIFIED. ) 
 GEOMETRIC_REPRESENTATION_ITEM ( )  RATIONAL_B_SPLINE_SURFACE ( (
 ( 1.000000000000000000, 1.000000000000000000),
 ( 0.9593108457356467333, 0.9995965569486454649),
 ( 0.9593108457356467333, 0.9995965569486454649),
 ( 1.000000000000000000, 1.000000000000000000) ) ) 
 REPRESENTATION_ITEM ( '' )  SURFACE ( )  );
#5388=CARTESIAN_POINT ( 'NONE',  ( 0.3170788640506440603, 11.20690911610915208, -7.952793437297452250 ) ) ;
#5395=EDGE_CURVE ( 'NONE', #2148, #12310, #16407, .T. ) ;
#5397=VERTEX_POINT ( 'NONE', #5727 ) ;
#5403=FACE_OUTER_BOUND ( 'NONE', #6720, .T. ) ;
#5405=VECTOR ( 'NONE', #5269, 1000.000000000000114 ) ;
#5408=CARTESIAN_POINT ( 'NONE',  ( 16.57210152137263393, 0.01402404281923039231, 0.003862718596009517575 ) ) ;
#5410=ORIENTED_EDGE ( 'NONE', *, *, #6617, .T. ) ;
#5416=CARTESIAN_POINT ( 'NONE',  ( 16.56782317627811096, 0.006045301465876368185, -0.007739510688079533247 ) ) ;
#5417=CARTESIAN_POINT ( 'NONE',  ( 0.4754618798421162973, -8.775436892861190330, 10.80499583390509954 ) ) ;
#5420=VERTEX_POINT ( 'NONE', #2573 ) ;
#5428=CARTESIAN_POINT ( 'NONE',  ( 0.3137051932979809665, 13.20008686438111312, -3.805684345189650042 ) ) ;
#5430=CARTESIAN_POINT ( 'NONE',  ( 1.846138399168762989, -3.446241763653083101, 11.95493567637849530 ) ) ;
#5431=ORIENTED_EDGE ( 'NONE', *, *, #9873, .F. ) ;
#5433=CARTESIAN_POINT ( 'NONE',  ( 3.950837973638668288, 0.000000000000000000, 0.000000000000000000 ) ) ;
#5438=CARTESIAN_POINT ( 'NONE',  ( 2.636624412714242194, 14.46769361191244485, 6.973567714906650394 ) ) ;
#5443=ORIENTED_EDGE ( 'NONE', *, *, #4445, .F. ) ;
#5444=CARTESIAN_POINT ( 'NONE',  ( 2.636624412715137922, -15.91454522070252153, 2.161493821597598508 ) ) ;
#5447=CARTESIAN_POINT ( 'NONE',  ( 3.512766787570810401, -2.025881399556277440, -14.91422000116817159 ) ) ;
#5449=EDGE_CURVE ( 'NONE', #9813, #14004, #5921, .T. ) ;
#5450=FILL_AREA_STYLE_COLOUR ( '', #8753 ) ;
#5452=CARTESIAN_POINT ( 'NONE',  ( 2.123976203522053297, 3.347755036805901252, 15.26039569100260884 ) ) ;
#5456=CARTESIAN_POINT ( 'NONE',  ( 0.3939822652208130327, -0.7002900021918908591, 13.80035637018651862 ) ) ;
#5459=CARTESIAN_POINT ( 'NONE',  ( 0.3137051932979792457, -13.20008686438103140, -3.805684345189927154 ) ) ;
#5471=CARTESIAN_POINT ( 'NONE',  ( 0.4384471787762820871, -13.39294437382615399, -3.577367180593688634 ) ) ;
#5472=EDGE_CURVE ( 'NONE', #3568, #2148, #17696, .T. ) ;
#5474=CARTESIAN_POINT ( 'NONE',  ( 3.950837973638668288, 0.000000000000000000, 0.000000000000000000 ) ) ;
#5477=ORIENTED_EDGE ( 'NONE', *, *, #10518, .F. ) ;
#5479=ORIENTED_EDGE ( 'NONE', *, *, #18361, .F. ) ;
#5483=CARTESIAN_POINT ( 'NONE',  ( 2.636624412716062960, 6.973567714909310489, -14.46769361191320868 ) ) ;
#5485=CARTESIAN_POINT ( 'NONE',  ( 1.846138399168762101, 6.971848976711011225, 10.30487220521572667 ) ) ;
#5488=CARTESIAN_POINT ( 'NONE',  ( 3.377929128793398128, -5.536064832134078628, -12.84367544717941456 ) ) ;
#5492=CARTESIAN_POINT ( 'NONE',  ( 1.861706995891674099, -12.44571539481144384, 0.5394761475745415424 ) ) ;
#5497=ORIENTED_EDGE ( 'NONE', *, *, #1804, .T. ) ;
#5500=CARTESIAN_POINT ( 'NONE',  ( 3.950837973638675393, -10.51028938476210328, -10.05648675950137871 ) ) ;
#5501=CARTESIAN_POINT ( 'NONE',  ( 0.3058872367615230181, 4.821066432589326212, 12.87003593440630311 ) ) ;
#5505=DIRECTION ( 'NONE',  ( -1.000000000000000000, -0.000000000000000000, -0.000000000000000000 ) ) ;
#5506=CARTESIAN_POINT ( 'NONE',  ( 3.074695600507708182, 10.75417554975745205, 11.23985886659407463 ) ) ;
#5508=CARTESIAN_POINT ( 'NONE',  ( 2.636624412714236865, 0.000000000000000000, 0.000000000000000000 ) ) ;
#5512=FACE_OUTER_BOUND ( 'NONE', #7162, .T. ) ;
#5515=CARTESIAN_POINT ( 'NONE',  ( 0.3137051932979792457, -13.73004976592201842, -0.4596302728641207813 ) ) ;
#5522=ORIENTED_EDGE ( 'NONE', *, *, #5547, .F. ) ;
#5526=ORIENTED_EDGE ( 'NONE', *, *, #6144, .F. ) ;
#5531=B_SPLINE_CURVE_WITH_KNOTS ( 'NONE', 3,
 ( #7209, #5842, #18851, #5743 ),
 .UNSPECIFIED., .F., .F.,
 ( 4, 4 ),
 ( 1.927807806696441531E-17, 0.003005512676784856570 ),
 .UNSPECIFIED. ) ;
#5539=CARTESIAN_POINT ( 'NONE',  ( 0.3137051932979792457, -0.4596302728640728752, 13.73004976592201842 ) ) ;
#5542=CARTESIAN_POINT ( 'NONE',  ( 0.3151928476913556376, 4.245457024760402653, -13.06684726503522320 ) ) ;
#5544=B_SPLINE_CURVE_WITH_KNOTS ( 'NONE', 3,
 ( #1100, #12764, #18588, #5492, #17157, #4068 ),
 .UNSPECIFIED., .F., .F.,
 ( 4, 2, 4 ),
 ( 5.421010862427522170E-19, 0.0001825746017570591031, 0.0003651492035141176641 ),
 .UNSPECIFIED. ) ;
#5547=EDGE_CURVE ( 'NONE', #13860, #5420, #6044, .T. ) ;
#5551=CARTESIAN_POINT ( 'NONE',  ( 3.950837973638668288, 0.000000000000000000, 0.000000000000000000 ) ) ;
#5555=CARTESIAN_POINT ( 'NONE',  ( 1.847340342630339860, 0.1245571717073309381, 12.44248139376886186 ) ) ;
#5559=CARTESIAN_POINT ( 'NONE',  ( 0.3142011359265348691, 10.88514493056454135, -8.382042760265784764 ) ) ;
#5565=FACE_OUTER_BOUND ( 'NONE', #4907, .T. ) ;
#5566=ORIENTED_EDGE ( 'NONE', *, *, #13261, .F. ) ;
#5567=DIRECTION ( 'NONE',  ( 0.000000000000000000, 0.000000000000000000, 1.000000000000000000 ) ) ;
#5568=VERTEX_POINT ( 'NONE', #17888 ) ;
#5571=DIRECTION ( 'NONE',  ( 0.000000000000000000, 0.000000000000000000, 1.000000000000000000 ) ) ;
#5572=CARTESIAN_POINT ( 'NONE',  ( 1.847461586945727152, -10.08650590720931284, -7.286856109515166047 ) ) ;
#5573=CARTESIAN_POINT ( 'NONE',  ( 16.56872352241294521, -0.007512283835805501873, -0.007240717549633963156 ) ) ;
#5574=CARTESIAN_POINT ( 'NONE',  ( 2.636624412715137922, -7.605649742761668719, 14.14563173255331741 ) ) ;
#5576=CARTESIAN_POINT ( 'NONE',  ( 16.56782317627811096, 0.009814734722107082768, 0.0003415813796006631126 ) ) ;
#5578=FACE_OUTER_BOUND ( 'NONE', #17867, .T. ) ;
#5581=CIRCLE ( 'NONE', #1628, 14.54644660717763927 ) ;
#5582=ORIENTED_EDGE ( 'NONE', *, *, #5547, .T. ) ;
#5583=ORIENTED_EDGE ( 'NONE', *, *, #1004, .F. ) ;
#5586=ORIENTED_EDGE ( 'NONE', *, *, #1420, .F. ) ;
#5589=CARTESIAN_POINT ( 'NONE',  ( 16.56872352241294521, 0.004564908236399969378, -0.009382111268607383134 ) ) ;
#5591=ORIENTED_EDGE ( 'NONE', *, *, #9626, .F. ) ;
#5592=CARTESIAN_POINT ( 'NONE',  ( 2.353870697619112384, 12.92712089195302738, 0.7635393531606785578 ) ) ;
#5594=CIRCLE ( 'NONE', #14762, 14.54644660717763927 ) ;
#5597=CARTESIAN_POINT ( 'NONE',  ( 0.3150692679895978898, -11.20465057551030874, 7.951395415075045214 ) ) ;
#5601=CARTESIAN_POINT ( 'NONE',  ( 1.846138399168762989, -4.238866729160486457, 11.69739621335920710 ) ) ;
#5602=VERTEX_POINT ( 'NONE', #7762 ) ;
#5609=EDGE_CURVE ( 'NONE', #16284, #13343, #7650, .T. ) ;
#5613=CARTESIAN_POINT ( 'NONE',  ( 1.846138399168762101, -6.971848976710933954, -10.30487220521577818 ) ) ;
#5615=CARTESIAN_POINT ( 'NONE',  ( 16.56872352241294521, -0.004564908236400030961, 0.009382111268607351909 ) ) ;
#5623=CARTESIAN_POINT ( 'NONE',  ( 3.353306896162455697, 1.348936822033017124, -13.88482890973694950 ) ) ;
#5630=ORIENTED_EDGE ( 'NONE', *, *, #6223, .F. ) ;
#5634=CARTESIAN_POINT ( 'NONE',  ( 1.846138399168762989, 10.30487220521570357, 6.971848976711047641 ) ) ;
#5636=CIRCLE ( 'NONE', #9017, 16.06066017081991149 ) ;
#5640=ADVANCED_FACE ( 'NONE', ( #9373 ), #17005, .F. ) ;
#5649=CARTESIAN_POINT ( 'NONE',  ( 2.002547531651519996, -7.942910686618240845, 9.778737580845669797 ) ) ;
#5650=CARTESIAN_POINT ( 'NONE',  ( 1.847412631396506244, 3.804043368582664009, 11.84727953344284579 ) ) ;
#5657=CARTESIAN_POINT ( 'NONE',  ( 0.3170788640506441158, -7.952793437297652090, 11.20690911610900997 ) ) ;
#5659=DIRECTION ( 'NONE',  ( 0.000000000000000000, 0.000000000000000000, 1.000000000000000000 ) ) ;
#5662=EDGE_CURVE ( 'NONE', #9516, #6835, #2201, .T. ) ;
#5664=DIRECTION ( 'NONE',  ( 0.000000000000000000, 0.000000000000000000, 1.000000000000000000 ) ) ;
#5666=DIRECTION ( 'NONE',  ( 0.7635533937278216055, 0.6453904417649386493, 0.02138673900302558509 ) ) ;
#5667=CARTESIAN_POINT ( 'NONE',  ( 1.254009781012375813, 11.25324419414251942, -9.426200207652035701 ) ) ;
#5668=CARTESIAN_POINT ( 'NONE',  ( 0.3137051932979775248, -12.91601973349273891, 4.679953077377436266 ) ) ;
#5672=EDGE_CURVE ( 'NONE', #12599, #8470, #1256, .T. ) ;
#5673=VECTOR ( 'NONE', #15431, 1000.000000000000000 ) ;
#5680=( BOUNDED_SURFACE ( )  B_SPLINE_SURFACE ( 3, 1, ( 
 ( #14458, #10161 ),
 ( #13408, #14940 ),
 ( #4334, #324 ),
 ( #17426, #10449 ) ),
 .UNSPECIFIED., .F., .F., .T. ) 
 B_SPLINE_SURFACE_WITH_KNOTS ( ( 4, 4 ),
 ( 2, 2 ),
 ( 0.000000000000000000, 1.000000000000000000 ),
 ( 0.000000000000000000, 1.000000000000000000 ),
 .UNSPECIFIED. ) 
 GEOMETRIC_REPRESENTATION_ITEM ( )  RATIONAL_B_SPLINE_SURFACE ( (
 ( 1.000000000000000000, 1.000000000000000000),
 ( 0.9593108457356467333, 0.9995965569486454649),
 ( 0.9593108457356467333, 0.9995965569486454649),
 ( 1.000000000000000000, 1.000000000000000000) ) ) 
 REPRESENTATION_ITEM ( '' )  SURFACE ( )  );
#5681=ORIENTED_EDGE ( 'NONE', *, *, #11569, .T. ) ;
#5686=CARTESIAN_POINT ( 'NONE',  ( 16.56822296793089322, -0.01011126603341077138, 0.0007467251401298242519 ) ) ;
#5687=VERTEX_POINT ( 'NONE', #5515 ) ;
#5693=CARTESIAN_POINT ( 'NONE',  ( 0.3058872367615226295, 3.664492643742762290, 13.24582953854926615 ) ) ;
#5694=CARTESIAN_POINT ( 'NONE',  ( 0.4754618798421171855, -13.89949764182683190, 0.7484603771383911974 ) ) ;
#5698=CARTESIAN_POINT ( 'NONE',  ( 1.846955891736115962, -3.593597880662430910, 11.91257079808167596 ) ) ;
#5704=CARTESIAN_POINT ( 'NONE',  ( 3.074695600507272086, 14.01296402267896291, -6.754521329824639153 ) ) ;
#5707=CARTESIAN_POINT ( 'NONE',  ( 2.002547531651519996, 6.845637710436190737, 10.57595306287294612 ) ) ;
#5710=CARTESIAN_POINT ( 'NONE',  ( 0.3170788640506440603, -4.100430649997872656, -13.11595226728161911 ) ) ;
#5715=CARTESIAN_POINT ( 'NONE',  ( 0.3142014840576499712, -13.73311050063163563, -0.3830336514510319090 ) ) ;
#5716=CARTESIAN_POINT ( 'NONE',  ( 0.000000000000000000, 0.000000000000000000, 0.000000000000000000 ) ) ;
#5718=CARTESIAN_POINT ( 'NONE',  ( 3.950837973638675393, -10.51028938476224894, 10.05648675950122595 ) ) ;
#5719=CARTESIAN_POINT ( 'NONE',  ( 0.4862570985993235340, -12.97920246947883172, 5.003653737315437944 ) ) ;
#5722=FACE_OUTER_BOUND ( 'NONE', #5208, .T. ) ;
#5725=ORIENTED_EDGE ( 'NONE', *, *, #489, .F. ) ;
#5727=CARTESIAN_POINT ( 'NONE',  ( 0.3137051932979792457, 13.20008686438105983, 3.805684345189833451 ) ) ;
#5728=EDGE_LOOP ( 'NONE', ( #9335, #18744, #5876, #12627 ) ) ;
#5732=CARTESIAN_POINT ( 'NONE',  ( 1.847461586945732037, 10.08650590720936258, 7.286856109515091440 ) ) ;
#5739=ORIENTED_EDGE ( 'NONE', *, *, #18650, .T. ) ;
#5743=CARTESIAN_POINT ( 'NONE',  ( 2.002547531651519996, 11.75462648437108015, -4.532360870844206246 ) ) ;
#5745=CARTESIAN_POINT ( 'NONE',  ( 2.002547531651519996, -12.57989064830759141, -0.6781519942173057647 ) ) ;
#5749=CARTESIAN_POINT ( 'NONE',  ( 2.320521194582820801, -15.43440938317095146, -3.126729093671786863 ) ) ;
#5751=B_SPLINE_CURVE_WITH_KNOTS ( 'NONE', 3,
 ( #4566, #6096, #13447, #4369 ),
 .UNSPECIFIED., .F., .F.,
 ( 4, 4 ),
 ( 0.000000000000000000, 0.002004993803842607548 ),
 .UNSPECIFIED. ) ;
#5754=LINE ( 'NONE', #14071, #8494 ) ;
#5757=VECTOR ( 'NONE', #8899, 1000.000000000000114 ) ;
#5758=B_SPLINE_CURVE_WITH_KNOTS ( 'NONE', 3,
 ( #11011, #2211, #13958, #12435, #779, #2559, #15570, #9476, #12707, #17023, #5257, #2472, #15391 ),
 .UNSPECIFIED., .F., .F.,
 ( 4, 3, 3, 3, 4 ),
 ( 3.127317220692750759E-18, 0.0002299804304191498290, 0.0004599608082120264186, 0.0006467586077648000654, 0.0008336169836825974228 ),
 .UNSPECIFIED. ) ;
#5763=( BOUNDED_SURFACE ( )  B_SPLINE_SURFACE ( 3, 1, ( 
 ( #3885, #18776 ),
 ( #16977, #14382 ),
 ( #9887, #9712 ),
 ( #18495, #15719 ) ),
 .UNSPECIFIED., .F., .F., .T. ) 
 B_SPLINE_SURFACE_WITH_KNOTS ( ( 4, 4 ),
 ( 2, 2 ),
 ( 0.000000000000000000, 1.000000000000000000 ),
 ( 0.000000000000000000, 1.000000000000000000 ),
 .UNSPECIFIED. ) 
 GEOMETRIC_REPRESENTATION_ITEM ( )  RATIONAL_B_SPLINE_SURFACE ( (
 ( 1.000000000000000000, 1.000000000000000000),
 ( 0.7792777138730160313, 0.9689936506012927220),
 ( 0.7792777138730160313, 0.9689936506012927220),
 ( 1.000000000000000000, 1.000000000000000000) ) ) 
 REPRESENTATION_ITEM ( '' )  SURFACE ( )  );
#5767=CARTESIAN_POINT ( 'NONE',  ( 0.3170788640506441158, -0.1533108587035203196, -13.74111462631963576 ) ) ;
#5769=CARTESIAN_POINT ( 'NONE',  ( 1.861706995891667882, 4.359009869687244354, 11.66987142852985748 ) ) ;
#5772=CARTESIAN_POINT ( 'NONE',  ( 3.074695600507258320, -7.366518011946037170, 13.70113613813197873 ) ) ;
#5777=ORIENTED_EDGE ( 'NONE', *, *, #4214, .T. ) ;
#5783=CARTESIAN_POINT ( 'NONE',  ( 16.56872352241294521, -0.01027347319884440620, 0.001821578298044753286 ) ) ;
#5785=DIRECTION ( 'NONE',  ( -1.000000000000000000, -0.000000000000000000, -0.000000000000000000 ) ) ;
#5787=CARTESIAN_POINT ( 'NONE',  ( 2.636624412714236865, 0.000000000000000000, 0.000000000000000000 ) ) ;
#5790=CARTESIAN_POINT ( 'NONE',  ( 0.3151926232592536792, -11.07013665200800645, 8.137833541809341042 ) ) ;
#5793=B_SPLINE_CURVE_WITH_KNOTS ( 'NONE', 3,
 ( #12543, #11126, #889, #13983, #5190, #11226 ),
 .UNSPECIFIED., .F., .F.,
 ( 4, 2, 4 ),
 ( 3.556447555475521540E-17, 0.0001825746017570583171, 0.0003651492035140810723 ),
 .UNSPECIFIED. ) ;
#5796=EDGE_LOOP ( 'NONE', ( #10652, #18073, #16821, #7183 ) ) ;
#5798=( BOUNDED_SURFACE ( )  B_SPLINE_SURFACE ( 3, 1, ( 
 ( #16723, #3801 ),
 ( #3623, #18329 ),
 ( #9632, #15458 ),
 ( #14032, #1303 ) ),
 .UNSPECIFIED., .F., .F., .T. ) 
 B_SPLINE_SURFACE_WITH_KNOTS ( ( 4, 4 ),
 ( 2, 2 ),
 ( 0.000000000000000000, 1.000000000000000000 ),
 ( 0.000000000000000000, 1.000000000000000000 ),
 .UNSPECIFIED. ) 
 GEOMETRIC_REPRESENTATION_ITEM ( )  RATIONAL_B_SPLINE_SURFACE ( (
 ( 1.000000000000000000, 1.000000000000000000),
 ( 0.9933953342250438912, 0.8357391271907739227),
 ( 0.9933953342250438912, 0.8357391271907739227),
 ( 1.000000000000000000, 1.000000000000000000) ) ) 
 REPRESENTATION_ITEM ( '' )  SURFACE ( )  );
#5800=EDGE_LOOP ( 'NONE', ( #55, #6322, #16487, #14350, #16599, #4493, #16807, #13765, #8584, #4939, #6418, #15314, #6813, #550, #17398, #17307, #10144, #11, #640, #13943, #11433, #1830, #974, #14831, #8276, #16595, #17748, #16896, #1032, #18255, #5236, #14323, #16755, #10836, #15825, #2424, #14434, #6469, #2808, #10697, #1560, #12472, #2696, #10190, #6107, #8420, #16818, #9654, #17238, #17032, #1373, #157, #8673, #2874, #14285, #10724, #10263, #816, #15308, #10311, #8803, #9600, #2899, #1278 ) ) ;
#5802=FACE_OUTER_BOUND ( 'NONE', #1879, .T. ) ;
#5805=CARTESIAN_POINT ( 'NONE',  ( 3.074695600507694859, 14.01296402267844066, 6.754521329824622278 ) ) ;
#5806=CARTESIAN_POINT ( 'NONE',  ( 3.353306896162453477, -9.252610477110343012, 10.44017738170053278 ) ) ;
#5808=CARTESIAN_POINT ( 'NONE',  ( 16.56753206892534891, 0.006760771273036169683, 0.006669401563384943880 ) ) ;
#5814=CARTESIAN_POINT ( 'NONE',  ( 0.3170788640506441158, 8.200855617524535290, 11.02668139258444846 ) ) ;
#5819=VERTEX_POINT ( 'NONE', #4645 ) ;
#5825=CARTESIAN_POINT ( 'NONE',  ( 0.4862570985993252548, -5.003653737315580052, 12.97920246947877665 ) ) ;
#5826=EDGE_LOOP ( 'NONE', ( #17522, #6906, #16386, #5522 ) ) ;
#5827=CARTESIAN_POINT ( 'NONE',  ( 3.512766787570708260, -14.91422000116825508, -2.025881399556554552 ) ) ;
#5828=B_SPLINE_CURVE_WITH_KNOTS ( 'NONE', 3,
 ( #13713, #629, #9412, #2151 ),
 .UNSPECIFIED., .F., .F.,
 ( 4, 4 ),
 ( 4.589925559575316169E-16, 0.002004993803842821786 ),
 .UNSPECIFIED. ) ;
#5831=ORIENTED_EDGE ( 'NONE', *, *, #5857, .T. ) ;
#5833=EDGE_CURVE ( 'NONE', #15093, #8524, #11813, .T. ) ;
#5834=EDGE_CURVE ( 'NONE', #14724, #13901, #12201, .T. ) ;
#5837=DIRECTION ( 'NONE',  ( 0.7561779333270775005, -0.5491072561318390832, 0.3559159372837255031 ) ) ;
#5842=CARTESIAN_POINT ( 'NONE',  ( 3.377929128793398572, 12.84367544717943410, -5.536064832134035996 ) ) ;
#5850=CARTESIAN_POINT ( 'NONE',  ( 0.3137051932979757485, -4.679953077377398074, -12.91601973349275134 ) ) ;
#5851=VERTEX_POINT ( 'NONE', #1972 ) ;
#5857=EDGE_CURVE ( 'NONE', #14019, #9425, #357, .T. ) ;
#5861=EDGE_CURVE ( 'NONE', #13196, #17057, #443, .T. ) ;
#5862=CARTESIAN_POINT ( 'NONE',  ( 1.846138399168762989, -4.238866729160486457, 11.69739621335920710 ) ) ;
#5869=CARTESIAN_POINT ( 'NONE',  ( 0.3148208552358917611, 13.73693263646118723, -0.2299193288887949882 ) ) ;
#5872=ORIENTED_EDGE ( 'NONE', *, *, #13033, .F. ) ;
#5874=ORIENTED_EDGE ( 'NONE', *, *, #15813, .T. ) ;
#5875=ORIENTED_EDGE ( 'NONE', *, *, #1048, .F. ) ;
#5876=ORIENTED_EDGE ( 'NONE', *, *, #15813, .F. ) ;
#5877=( BOUNDED_SURFACE ( )  B_SPLINE_SURFACE ( 3, 1, ( 
 ( #12925, #8356 ),
 ( #4145, #11412 ),
 ( #14173, #5388 ),
 ( #6922, #17051 ) ),
 .UNSPECIFIED., .F., .F., .T. ) 
 B_SPLINE_SURFACE_WITH_KNOTS ( ( 4, 4 ),
 ( 2, 2 ),
 ( 0.000000000000000000, 1.000000000000000000 ),
 ( 0.000000000000000000, 1.000000000000000000 ),
 .UNSPECIFIED. ) 
 GEOMETRIC_REPRESENTATION_ITEM ( )  RATIONAL_B_SPLINE_SURFACE ( (
 ( 1.000000000000000000, 1.000000000000000000),
 ( 0.9593108457356467333, 0.9995965569486454649),
 ( 0.9593108457356467333, 0.9995965569486454649),
 ( 1.000000000000000000, 1.000000000000000000) ) ) 
 REPRESENTATION_ITEM ( '' )  SURFACE ( )  );
#5878=DIRECTION ( 'NONE',  ( -1.000000000000000000, 0.000000000000000000, 0.000000000000000000 ) ) ;
#5880=CARTESIAN_POINT ( 'NONE',  ( 0.3095370825347234511, 10.84046130709058708, 8.444334731364046220 ) ) ;
#5885=EDGE_CURVE ( 'NONE', #13788, #3395, #9695, .T. ) ;
#5888=CARTESIAN_POINT ( 'NONE',  ( 0.3720661004400037664, 3.575426119359183197, 13.34435358167253938 ) ) ;
#5892=CARTESIAN_POINT ( 'NONE',  ( 0.3151928479966097374, 1.775918418904422640E-15, 13.73922861026898623 ) ) ;
#5900=CONICAL_SURFACE ( 'NONE', #6832, 16.06066017081991149, 0.7853981625000062694 ) ;
#5902=CARTESIAN_POINT ( 'NONE',  ( 0.4754618798421162973, -11.68486377711971969, 7.564402563418428649 ) ) ;
#5912=CARTESIAN_POINT ( 'NONE',  ( 0.3308579732647041749, 8.558831104907067555, -10.76782854710817716 ) ) ;
#5914=( BOUNDED_SURFACE ( )  B_SPLINE_SURFACE ( 3, 1, ( 
 ( #14827, #17710 ),
 ( #600, #15214 ),
 ( #9387, #17992 ),
 ( #16561, #10635 ) ),
 .UNSPECIFIED., .F., .F., .T. ) 
 B_SPLINE_SURFACE_WITH_KNOTS ( ( 4, 4 ),
 ( 2, 2 ),
 ( 0.000000000000000000, 1.000000000000000000 ),
 ( 0.000000000000000000, 1.000000000000000000 ),
 .UNSPECIFIED. ) 
 GEOMETRIC_REPRESENTATION_ITEM ( )  RATIONAL_B_SPLINE_SURFACE ( (
 ( 1.000000000000000000, 1.000000000000000000),
 ( 0.9593108457356467333, 0.9995965569486454649),
 ( 0.9593108457356467333, 0.9995965569486454649),
 ( 1.000000000000000000, 1.000000000000000000) ) ) 
 REPRESENTATION_ITEM ( '' )  SURFACE ( )  );
#5918=B_SPLINE_CURVE_WITH_KNOTS ( 'NONE', 3,
 ( #16874, #13732, #6754, #10877, #3777, #6472, #5302, #18125, #5026, #6663, #9434, #3876, #13908 ),
 .UNSPECIFIED., .F., .F.,
 ( 4, 3, 3, 3, 4 ),
 ( 3.878959614448864246E-18, 0.0002299780670421069050, 0.0004599561239687931019, 0.0006896788984287867625, 0.0009194956271626391958 ),
 .UNSPECIFIED. ) ;
#5919=CARTESIAN_POINT ( 'NONE',  ( 0.3095370825347224519, 12.91933430393608084, 4.681152801286204479 ) ) ;
#5920=CARTESIAN_POINT ( 'NONE',  ( 2.636624412715093513, -14.14563173255330142, 7.605649742761597665 ) ) ;
#5921=LINE ( 'NONE', #3237, #3868 ) ;
#5926=VERTEX_POINT ( 'NONE', #12378 ) ;
#5927=EDGE_CURVE ( 'NONE', #10089, #8935, #11058, .T. ) ;
#5928=CARTESIAN_POINT ( 'NONE',  ( 1.846524061778021419, 9.853584647934384932, 7.597197846158115553 ) ) ;
#5932=AXIS2_PLACEMENT_3D ( 'NONE', #8386, #5785, #17359 ) ;
#5936=AXIS2_PLACEMENT_3D ( 'NONE', #18013, #16759, #13792 ) ;
#5947=CARTESIAN_POINT ( 'NONE',  ( 16.58200780006414732, 0.004047297414157893791, 0.01041078477703983804 ) ) ;
#5948=CARTESIAN_POINT ( 'NONE',  ( 2.636624412715384391, -11.60464335004044223, -11.10302021258006278 ) ) ;
#5950=VERTEX_POINT ( 'NONE', #3869 ) ;
#5952=ORIENTED_EDGE ( 'NONE', *, *, #15150, .T. ) ;
#5953=CARTESIAN_POINT ( 'NONE',  ( 0.4862570985993235340, -13.44146924561383827, 3.580942890621619412 ) ) ;
#5958=B_SPLINE_CURVE_WITH_KNOTS ( 'NONE', 3,
 ( #9359, #13664, #12229, #10796, #15191, #2103, #7940, #13750, #662, #12315, #9535, #15545, #12496 ),
 .UNSPECIFIED., .F., .F.,
 ( 4, 3, 3, 3, 4 ),
 ( 0.000000000000000000, 0.0002299804304191505879, 0.0004599608082120279365, 0.0006467586077648024507, 0.0008336169836825989407 ),
 .UNSPECIFIED. ) ;
#5960=CARTESIAN_POINT ( 'NONE',  ( 1.342453679581834924, 3.649820028552932971, -14.34050741580202981 ) ) ;
#5964=CARTESIAN_POINT ( 'NONE',  ( 0.3720661004400040439, 12.89739157014199833, -4.951033743989506242 ) ) ;
#5965=CARTESIAN_POINT ( 'NONE',  ( 2.636624412716913390, 14.14563173255587536, -7.605649742760633991 ) ) ;
#5967=B_SPLINE_CURVE_WITH_KNOTS ( 'NONE', 3,
 ( #2414, #3855, #7276, #5623, #15955, #9588 ),
 .UNSPECIFIED., .F., .F.,
 ( 4, 2, 4 ),
 ( 9.263427422397552964E-19, 0.001500839035891551789, 0.003001678071783102711 ),
 .UNSPECIFIED. ) ;
#5969=CARTESIAN_POINT ( 'NONE',  ( 16.56872352241294521, -0.001821578298044716857, -0.01027347319884440967 ) ) ;
#5970=CARTESIAN_POINT ( 'NONE',  ( 0.3308579732647007887, -10.76782854710821269, -8.558831104907037357 ) ) ;
#5971=CARTESIAN_POINT ( 'NONE',  ( 0.3170788640506440603, -11.20690911610909168, 7.952793437297537515 ) ) ;
#5972=CARTESIAN_POINT ( 'NONE',  ( 0.3151926232592509591, 13.73922722301401400, -0.07678256780562460471 ) ) ;
#5976=CARTESIAN_POINT ( 'NONE',  ( 1.846138399168762101, -11.95493567637852905, 3.446241763652952539 ) ) ;
#5977=CARTESIAN_POINT ( 'NONE',  ( 16.57778382496167424, -0.007244066302946679421, -0.01306626476309297180 ) ) ;
#5979=ORIENTED_EDGE ( 'NONE', *, *, #2923, .T. ) ;
#5981=CIRCLE ( 'NONE', #1411, 16.06066017081991149 ) ;
#5985=CARTESIAN_POINT ( 'NONE',  ( 0.000000000000000000, 3.061616997868383141E-16, -2.500000000000000000 ) ) ;
#5995=CARTESIAN_POINT ( 'NONE',  ( 16.56872352241294521, 0.001442253899401802278, 0.01033355228142402403 ) ) ;
#5998=CARTESIAN_POINT ( 'NONE',  ( 0.3148208552358953138, -8.260375059853256374, -10.97826876274321428 ) ) ;
#6006=EDGE_LOOP ( 'NONE', ( #13152, #16508, #9386, #1416 ) ) ;
#6007=B_SPLINE_CURVE_WITH_KNOTS ( 'NONE', 3,
 ( #5920, #1443, #17301, #13283, #2950, #8798 ),
 .UNSPECIFIED., .F., .F.,
 ( 4, 2, 4 ),
 ( 0.000000000000000000, 0.001656992708822777310, 0.003313985417645554619 ),
 .UNSPECIFIED. ) ;
#6013=CARTESIAN_POINT ( 'NONE',  ( 1.847461586945732703, 11.84459954310610463, 3.813310247068479431 ) ) ;
#6014=CARTESIAN_POINT ( 'NONE',  ( 2.123976203522053297, 14.31368049382969687, 6.261444813538606269 ) ) ;
#6018=DIRECTION ( 'NONE',  ( -0.7561779333270775005, -0.4122479608995667788, -0.5081796452863290847 ) ) ;
#6020=LINE ( 'NONE', #10513, #15988 ) ;
#6021=FACE_OUTER_BOUND ( 'NONE', #3392, .T. ) ;
#6023=CARTESIAN_POINT ( 'NONE',  ( 1.977228804421969688, 1.488378900182327991, 15.33060379559086073 ) ) ;
#6024=SURFACE_STYLE_USAGE ( .BOTH. , #17588 ) ;
#6025=VECTOR ( 'NONE', #13501, 1000.000000000000227 ) ;
#6026=B_SPLINE_CURVE_WITH_KNOTS ( 'NONE', 3,
 ( #6211, #16453, #16546, #6023, #17691, #8979 ),
 .UNSPECIFIED., .F., .F.,
 ( 4, 2, 4 ),
 ( 5.421010862427522170E-20, 0.001657017934710529891, 0.003314035869421059783 ),
 .UNSPECIFIED. ) ;
#6030=ADVANCED_FACE ( 'NONE', ( #14554 ), #18526, .T. ) ;
#6034=CARTESIAN_POINT ( 'NONE',  ( 0.3150692679895986115, 8.199139630396166112, -11.02465386701219252 ) ) ;
#6044=B_SPLINE_CURVE_WITH_KNOTS ( 'NONE', 3,
 ( #8986, #14814, #1726, #7577 ),
 .UNSPECIFIED., .F., .F.,
 ( 4, 4 ),
 ( 1.140836248210248932E-17, 0.003005512676784841391 ),
 .UNSPECIFIED. ) ;
#6047=EDGE_CURVE ( 'NONE', #796, #1036, #116, .T. ) ;
#6054=CARTESIAN_POINT ( 'NONE',  ( 0.3939822652208154752, 7.545099438012025317, 11.57634296752770453 ) ) ;
#6069=CARTESIAN_POINT ( 'NONE',  ( 0.3150692679896004988, 4.099798979280845579, 13.11337225490253644 ) ) ;
#6071=CARTESIAN_POINT ( 'NONE',  ( 0.3095370825347233956, 12.91933430393614302, -4.681152801286028620 ) ) ;
#6074=CARTESIAN_POINT ( 'NONE',  ( 16.57778382496167424, -0.01306626476309383916, -0.007244066302947642193 ) ) ;
#6079=CARTESIAN_POINT ( 'NONE',  ( 3.950837973638668288, 0.000000000000000000, 0.000000000000000000 ) ) ;
#6082=ORIENTED_EDGE ( 'NONE', *, *, #16834, .F. ) ;
#6087=CARTESIAN_POINT ( 'NONE',  ( 1.846138399168762101, 0.4167076046097279440, -12.43476674860266051 ) ) ;
#6092=CARTESIAN_POINT ( 'NONE',  ( 3.074695600507274307, 11.23985886659449029, -10.75417554975685341 ) ) ;
#6095=CARTESIAN_POINT ( 'NONE',  ( 3.950837973638675393, 10.05648675950126325, 10.51028938476221342 ) ) ;
#6096=CARTESIAN_POINT ( 'NONE',  ( 3.074695600507272086, 15.41438262616223298, -2.093687500612007923 ) ) ;
#6097=CARTESIAN_POINT ( 'NONE',  ( 1.846613052777651198, 12.43780859207240042, -0.3401093050882249558 ) ) ;
#6099=VECTOR ( 'NONE', #18441, 1000.000000000000114 ) ;
#6101=CARTESIAN_POINT ( 'NONE',  ( 0.8740764193768004731, -5.211550415969136374, 13.31469591265773289 ) ) ;
#6107=ORIENTED_EDGE ( 'NONE', *, *, #13982, .T. ) ;
#6109=EDGE_CURVE ( 'NONE', #11553, #8437, #3285, .T. ) ;
#6111=ORIENTED_EDGE ( 'NONE', *, *, #13692, .T. ) ;
#6113=CARTESIAN_POINT ( 'NONE',  ( 1.847372867223028070, 11.80112642014554325, 3.945260592619082907 ) ) ;
#6116=EDGE_LOOP ( 'NONE', ( #4838, #18191, #13790, #935 ) ) ;
#6118=DIRECTION ( 'NONE',  ( -0.7635533937278216055, -0.2197766120036420967, -0.6071939193889598352 ) ) ;
#6120=CARTESIAN_POINT ( 'NONE',  ( 16.56753206892534891, -0.009369540855502522109, 0.001549402974394263697 ) ) ;
#6128=VERTEX_POINT ( 'NONE', #12177 ) ;
#6133=CARTESIAN_POINT ( 'NONE',  ( 0.3137051932979809665, -4.679953077377580151, 12.91601973349268917 ) ) ;
#6134=B_SPLINE_CURVE_WITH_KNOTS ( 'NONE', 3,
 ( #2598, #8627, #1364, #8442 ),
 .UNSPECIFIED., .F., .F.,
 ( 4, 4 ),
 ( 4.459867448574166155E-16, 0.002004993803842844771 ),
 .UNSPECIFIED. ) ;
#6136=CARTESIAN_POINT ( 'NONE',  ( 0.4862570985993252548, -12.97920246947875889, -5.003653737315625349 ) ) ;
#6140=CARTESIAN_POINT ( 'NONE',  ( 0.3095370825347233956, 13.73357284481724783, -0.4597470195090692657 ) ) ;
#6144=EDGE_CURVE ( 'NONE', #9516, #13434, #9222, .T. ) ;
#6148=CARTESIAN_POINT ( 'NONE',  ( 1.918918678667072886, 0.6348738215465219437, 12.49849921341423453 ) ) ;
#6150=CARTESIAN_POINT ( 'NONE',  ( 3.512766787571172333, 14.91422000116773994, 2.025881399556380469 ) ) ;
#6152=CARTESIAN_POINT ( 'NONE',  ( 0.3145729642390375225, -3.952965287571204023, 13.15786090015082799 ) ) ;
#6170=CARTESIAN_POINT ( 'NONE',  ( 1.562796894703937678, 3.061616997868383141E-16, -2.500000000000000000 ) ) ;
#6172=ADVANCED_FACE ( 'NONE', ( #8821 ), #4672, .F. ) ;
#6177=ORIENTED_EDGE ( 'NONE', *, *, #10676, .T. ) ;
#6183=CARTESIAN_POINT ( 'NONE',  ( 1.918921323896323639, -3.258415356426438869, -12.08297777410668417 ) ) ;
#6185=CARTESIAN_POINT ( 'NONE',  ( 2.636624412716061627, -7.605649742761058540, -14.14563173255469408 ) ) ;
#6186=CARTESIAN_POINT ( 'NONE',  ( 0.3720661004400037664, 0.7231997263366731765, -13.79610186261028559 ) ) ;
#6187=LINE ( 'NONE', #5129, #12544 ) ;
#6190=CARTESIAN_POINT ( 'NONE',  ( 1.845755665166724402, -9.776700214453573068, -7.694641135842929636 ) ) ;
#6197=ORIENTED_EDGE ( 'NONE', *, *, #10655, .F. ) ;
#6198=ORIENTED_EDGE ( 'NONE', *, *, #8882, .T. ) ;
#6200=CARTESIAN_POINT ( 'NONE',  ( 1.977436885026404134, 10.21547824869624321, -11.52792723756320470 ) ) ;
#6201=CARTESIAN_POINT ( 'NONE',  ( 16.56753206892534891, 0.009369540855502530782, -0.001549402974394192573 ) ) ;
#6204=ORIENTED_EDGE ( 'NONE', *, *, #5672, .F. ) ;
#6209=CARTESIAN_POINT ( 'NONE',  ( 2.002547531651519996, 11.75462648437101976, 4.532360870844369671 ) ) ;
#6211=CARTESIAN_POINT ( 'NONE',  ( 0.4862570985993235340, 0.7479633556562450547, 13.89016912371017831 ) ) ;
#6212=( LENGTH_UNIT ( ) NAMED_UNIT ( * ) SI_UNIT ( .MILLI., .METRE. ) );
#6214=B_SPLINE_CURVE_WITH_KNOTS ( 'NONE', 3,
 ( #15000, #11950, #10519, #2943 ),
 .UNSPECIFIED., .F., .F.,
 ( 4, 4 ),
 ( 2.006682199098010609E-17, 0.003005512676784850064 ),
 .UNSPECIFIED. ) ;
#6218=CARTESIAN_POINT ( 'NONE',  ( 0.8740764193766143997, 13.31469591265758545, 5.211550415968988936 ) ) ;
#6220=ORIENTED_EDGE ( 'NONE', *, *, #3184, .T. ) ;
#6223=EDGE_CURVE ( 'NONE', #8687, #11022, #11721, .T. ) ;
#6224=EDGE_CURVE ( 'NONE', #14019, #14561, #6351, .T. ) ;
#6230=ORIENTED_EDGE ( 'NONE', *, *, #2678, .F. ) ;
#6232=CARTESIAN_POINT ( 'NONE',  ( 2.705023505549867036, 0.8488853074252974418, 13.27418276223636440 ) ) ;
#6234=CARTESIAN_POINT ( 'NONE',  ( 2.747332970342022840, 14.63517873738956965, -7.289199830146954717 ) ) ;
#6236=AXIS2_PLACEMENT_3D ( 'NONE', #674, #15466, #13846 ) ;
#6239=CARTESIAN_POINT ( 'NONE',  ( 16.56872352241294521, 0.001442253899401220278, -0.01033355228142500415 ) ) ;
#6247=CARTESIAN_POINT ( 'NONE',  ( 0.4862570985993235340, -10.79774104611366781, -8.769551628660854803 ) ) ;
#6251=EDGE_CURVE ( 'NONE', #666, #1293, #10164, .T. ) ;
#6253=DIRECTION ( 'NONE',  ( 0.000000000000000000, 0.000000000000000000, 1.000000000000000000 ) ) ;
#6259=FACE_OUTER_BOUND ( 'NONE', #14478, .T. ) ;
#6261=CARTESIAN_POINT ( 'NONE',  ( 16.57778382496167424, 0.01092721432669108844, -0.01018821665058837478 ) ) ;
#6263=CARTESIAN_POINT ( 'NONE',  ( 2.747332970342022840, 7.289199830147313541, -14.63517873738939379 ) ) ;
#6265=CARTESIAN_POINT ( 'NONE',  ( 16.57778382496167424, -0.01466529584256673520, 0.002851818597093359019 ) ) ;
#6269=CARTESIAN_POINT ( 'NONE',  ( 1.846822687350019754, 7.547953575784267066, -9.891732594446496662 ) ) ;
#6272=PRODUCT_DEFINITION ( 'UNKNOWN', '', #15091, #18039 ) ;
#6275=EDGE_CURVE ( 'NONE', #7476, #17964, #12448, .T. ) ;
#6278=EDGE_CURVE ( 'NONE', #8470, #12351, #12667, .T. ) ;
#6279=ORIENTED_EDGE ( 'NONE', *, *, #14146, .T. ) ;
#6281=CARTESIAN_POINT ( 'NONE',  ( 0.3142011359265339254, 0.3830873813806325301, 13.73310835363014171 ) ) ;
#6282=VECTOR ( 'NONE', #539, 1000.000000000000114 ) ;
#6283=CARTESIAN_POINT ( 'NONE',  ( 0.3137051932979792457, -13.73004976592201842, -0.4596302728641207813 ) ) ;
#6284=VECTOR ( 'NONE', #3507, 1000.000000000000114 ) ;
#6292=ADVANCED_FACE ( 'NONE', ( #15311 ), #8082, .F. ) ;
#6294=FACE_OUTER_BOUND ( 'NONE', #5042, .T. ) ;
#6316=CARTESIAN_POINT ( 'NONE',  ( 2.002547531651519996, -6.845637710436264456, 10.57595306287289638 ) ) ;
#6317=CARTESIAN_POINT ( 'NONE',  ( 0.3148208552358952583, 12.99355031785211168, -4.463611911212083783 ) ) ;
#6322=ORIENTED_EDGE ( 'NONE', *, *, #2848, .F. ) ;
#6326=CARTESIAN_POINT ( 'NONE',  ( 0.3132635586635977853, 10.79541209008116454, -8.495712071659280440 ) ) ;
#6327=STYLED_ITEM ( 'NONE', ( #16836 ), #556 ) ;
#6334=CARTESIAN_POINT ( 'NONE',  ( 3.377929128793396352, -12.02809354424095822, -7.136734442940969814 ) ) ;
#6341=EDGE_CURVE ( 'NONE', #9965, #17590, #18167, .T. ) ;
#6349=CARTESIAN_POINT ( 'NONE',  ( 16.56872352241294521, 0.01027347319884441834, -0.001821578298044677175 ) ) ;
#6351=LINE ( 'NONE', #14939, #6025 ) ;
#6352=CARTESIAN_POINT ( 'NONE',  ( 1.861706995891668992, -11.66987142852987169, 4.359009869687201721 ) ) ;
#6354=EDGE_LOOP ( 'NONE', ( #14798, #12451, #1395, #11133 ) ) ;
#6359=ORIENTED_EDGE ( 'NONE', *, *, #13742, .T. ) ;
#6362=CARTESIAN_POINT ( 'NONE',  ( 3.950837973638668288, 0.000000000000000000, 0.000000000000000000 ) ) ;
#6363=CARTESIAN_POINT ( 'NONE',  ( 0.3307726912345197445, 13.74203354050372106, -0.5948952607473121379 ) ) ;
#6369=CARTESIAN_POINT ( 'NONE',  ( 0.3058872367615226295, -4.821066432589418582, 12.87003593440626403 ) ) ;
#6375=DIRECTION ( 'NONE',  ( -0.7561779333270775005, -0.5081796452863273084, 0.4122479608995688327 ) ) ;
#6377=ADVANCED_FACE ( 'NONE', ( #6439 ), #9784, .F. ) ;
#6379=ORIENTED_EDGE ( 'NONE', *, *, #2505, .F. ) ;
#6384=DIRECTION ( 'NONE',  ( -1.000000000000000000, -0.000000000000000000, -0.000000000000000000 ) ) ;
#6386=CARTESIAN_POINT ( 'NONE',  ( 1.846138399168762989, 10.30487220521570357, 6.971848976711047641 ) ) ;
#6387=CARTESIAN_POINT ( 'NONE',  ( 3.950837973638676281, -6.316429227969562632, 13.10350451991838128 ) ) ;
#6389=CARTESIAN_POINT ( 'NONE',  ( 0.3307726912345200776, 12.88561780039865745, -4.812300915532842005 ) ) ;
#6391=CARTESIAN_POINT ( 'NONE',  ( 2.747332970342022840, -16.12459247543628393, 2.705255688517782975 ) ) ;
#6393=EDGE_CURVE ( 'NONE', #1012, #3873, #13590, .T. ) ;
#6396=ORIENTED_EDGE ( 'NONE', *, *, #15010, .F. ) ;
#6397=DIRECTION ( 'NONE',  ( 0.7635533937278216055, 0.3620487483322444855, 0.5347026451755978460 ) ) ;
#6400=CARTESIAN_POINT ( 'NONE',  ( 3.950837973638675393, -2.591948120961706792, -14.31366178983255466 ) ) ;
#6401=CARTESIAN_POINT ( 'NONE',  ( 3.353306896162455697, -5.573563251762193360, 12.78841260990236428 ) ) ;
#6403=CARTESIAN_POINT ( 'NONE',  ( 8.438534575730034959, 4.221456476902665678, 5.415535776177536675 ) ) ;
#6407=CARTESIAN_POINT ( 'NONE',  ( 0.3137051932979792457, 12.91601973349270871, 4.679953077377533965 ) ) ;
#6410=( BOUNDED_SURFACE ( )  B_SPLINE_SURFACE ( 3, 1, ( 
 ( #948, #13852 ),
 ( #6604, #2459 ),
 ( #1033, #12428 ),
 ( #11280, #12788 ) ),
 .UNSPECIFIED., .F., .F., .T. ) 
 B_SPLINE_SURFACE_WITH_KNOTS ( ( 4, 4 ),
 ( 2, 2 ),
 ( 0.000000000000000000, 1.000000000000000000 ),
 ( 0.000000000000000000, 1.000000000000000000 ),
 .UNSPECIFIED. ) 
 GEOMETRIC_REPRESENTATION_ITEM ( )  RATIONAL_B_SPLINE_SURFACE ( (
 ( 1.000000000000000000, 1.000000000000000000),
 ( 0.7792777138730160313, 0.9689936506012927220),
 ( 0.7792777138730160313, 0.9689936506012927220),
 ( 1.000000000000000000, 1.000000000000000000) ) ) 
 REPRESENTATION_ITEM ( '' )  SURFACE ( )  );
#6411=VECTOR ( 'NONE', #1864, 1000.000000000000227 ) ;
#6413=CARTESIAN_POINT ( 'NONE',  ( 2.636624412714237309, 15.80357026013209953, 2.862162146984226663 ) ) ;
#6416=CARTESIAN_POINT ( 'NONE',  ( 0.8740764193767259771, -13.31469591265765118, -5.211550415969147920 ) ) ;
#6417=CARTESIAN_POINT ( 'NONE',  ( 1.977228804422745512, -10.21522664410476366, -11.52787183731191512 ) ) ;
#6418=ORIENTED_EDGE ( 'NONE', *, *, #109, .T. ) ;
#6420=EDGE_CURVE ( 'NONE', #1319, #2485, #18075, .T. ) ;
#6424=CARTESIAN_POINT ( 'NONE',  ( 3.950837973638668288, 0.000000000000000000, 0.000000000000000000 ) ) ;
#6426=VERTEX_POINT ( 'NONE', #2576 ) ;
#6427=CARTESIAN_POINT ( 'NONE',  ( 3.950837973638676281, -12.81214529934970336, -6.888253895133431115 ) ) ;
#6428=CARTESIAN_POINT ( 'NONE',  ( 16.56753206892534891, -0.008432171035096412345, -0.004368917149004214288 ) ) ;
#6439=FACE_OUTER_BOUND ( 'NONE', #4275, .T. ) ;
#6446=CARTESIAN_POINT ( 'NONE',  ( 0.3137051932979792457, 12.91601973349270871, 4.679953077377533965 ) ) ;
#6448=CARTESIAN_POINT ( 'NONE',  ( 3.950837973638668288, 0.000000000000000000, 0.000000000000000000 ) ) ;
#6452=CARTESIAN_POINT ( 'NONE',  ( 1.846138399168762101, 12.43476674860266584, 0.4167076046095977149 ) ) ;
#6454=CARTESIAN_POINT ( 'NONE',  ( 3.950837973638668288, 0.000000000000000000, 0.000000000000000000 ) ) ;
#6455=CARTESIAN_POINT ( 'NONE',  ( 8.522092701127531811, 5.397361180353207111, -4.388629235579518451 ) ) ;
#6456=CARTESIAN_POINT ( 'NONE',  ( 2.636624412716913390, 14.14563173255587536, -7.605649742760633991 ) ) ;
#6457=B_SPLINE_CURVE_WITH_KNOTS ( 'NONE', 3,
 ( #7542, #1696, #16027, #14885, #6101, #11924 ),
 .UNSPECIFIED., .F., .F.,
 ( 4, 2, 4 ),
 ( 0.000000000000000000, 0.001656992708822828484, 0.003313985417645657836 ),
 .UNSPECIFIED. ) ;
#6458=CARTESIAN_POINT ( 'NONE',  ( 0.3151926232592457966, 8.137833541809381899, 11.07013665200797625 ) ) ;
#6462=CARTESIAN_POINT ( 'NONE',  ( 16.56679352167444819, 0.001390132774594440108, -0.009190982326619726375 ) ) ;
#6469=ORIENTED_EDGE ( 'NONE', *, *, #56, .T. ) ;
#6472=CARTESIAN_POINT ( 'NONE',  ( 0.3151930723728406103, 11.07033375389132246, 8.137566970826403789 ) ) ;
#6473=CARTESIAN_POINT ( 'NONE',  ( 0.4862570985993235340, 5.003653737315670647, -12.97920246947874112 ) ) ;
#6475=CARTESIAN_POINT ( 'NONE',  ( 2.636624412716062960, 2.862162146982868194, -15.80357026013419564 ) ) ;
#6485=ORIENTED_EDGE ( 'NONE', *, *, #509, .T. ) ;
#6486=B_SPLINE_CURVE_WITH_KNOTS ( 'NONE', 3,
 ( #17600, #1542, #4512, #14534 ),
 .UNSPECIFIED., .F., .F.,
 ( 4, 4 ),
 ( 0.000000000000000000, 0.002004993803842769744 ),
 .UNSPECIFIED. ) ;
#6488=CARTESIAN_POINT ( 'NONE',  ( 1.846138399168762101, -7.646096044339961040, 9.815003036200383946 ) ) ;
#6490=CARTESIAN_POINT ( 'NONE',  ( 16.57778382496167424, 0.01306626476309289374, -0.007244066302946823403 ) ) ;
#6491=EDGE_CURVE ( 'NONE', #1036, #4171, #1581, .T. ) ;
#6495=B_SPLINE_CURVE_WITH_KNOTS ( 'NONE', 3,
 ( #17740, #16863, #3768, #9225, #1874, #9326, #5202, #7810, #13803, #15154, #6269, #2239, #10861 ),
 .UNSPECIFIED., .F., .F.,
 ( 4, 3, 3, 3, 4 ),
 ( 0.000000000000000000, 0.0002299804304191490972, 0.0004599608082120256055, 0.0006467586077648033180, 0.0008336169836825999165 ),
 .UNSPECIFIED. ) ;
#6497=ORIENTED_EDGE ( 'NONE', *, *, #11876, .F. ) ;
#6504=CARTESIAN_POINT ( 'NONE',  ( 0.8740764193768816304, 0.8420116711623857331, -14.27348595579795010 ) ) ;
#6505=VERTEX_POINT ( 'NONE', #16461 ) ;
#6506=EDGE_CURVE ( 'NONE', #17181, #8687, #15636, .T. ) ;
#6507=CARTESIAN_POINT ( 'NONE',  ( 1.847380140988738484, 11.79969976631077699, -3.949801494731646656 ) ) ;
#6511=ADVANCED_FACE ( 'NONE', ( #3144 ), #10651, .F. ) ;
#6515=CARTESIAN_POINT ( 'NONE',  ( 16.56872352241294521, -0.001442253899401880124, -0.01033355228142401362 ) ) ;
#6518=( BOUNDED_SURFACE ( )  B_SPLINE_SURFACE ( 3, 1, ( 
 ( #7467, #11479 ),
 ( #2757, #17298 ),
 ( #17488, #14711 ),
 ( #15957, #13281 ) ),
 .UNSPECIFIED., .F., .F., .T. ) 
 B_SPLINE_SURFACE_WITH_KNOTS ( ( 4, 4 ),
 ( 2, 2 ),
 ( 0.000000000000000000, 1.000000000000000000 ),
 ( 0.000000000000000000, 1.000000000000000000 ),
 .UNSPECIFIED. ) 
 GEOMETRIC_REPRESENTATION_ITEM ( )  RATIONAL_B_SPLINE_SURFACE ( (
 ( 1.000000000000000000, 1.000000000000000000),
 ( 0.9593108457356467333, 0.9995965569486454649),
 ( 0.9593108457356467333, 0.9995965569486454649),
 ( 1.000000000000000000, 1.000000000000000000) ) ) 
 REPRESENTATION_ITEM ( '' )  SURFACE ( )  );
#6519=ORIENTED_EDGE ( 'NONE', *, *, #18386, .F. ) ;
#6520=CARTESIAN_POINT ( 'NONE',  ( 3.950837973638676281, 10.05648675950141602, -10.51028938476206953 ) ) ;
#6522=CARTESIAN_POINT ( 'NONE',  ( 2.636624412714236865, 0.000000000000000000, 0.000000000000000000 ) ) ;
#6528=CARTESIAN_POINT ( 'NONE',  ( 16.58200780006414732, -0.01041078477704051979, -0.004047297414159007484 ) ) ;
#6532=CARTESIAN_POINT ( 'NONE',  ( 16.57778382496167424, 0.007244066302947695102, -0.01306626476309380794 ) ) ;
#6534=ORIENTED_EDGE ( 'NONE', *, *, #513, .F. ) ;
#6541=VERTEX_POINT ( 'NONE', #108 ) ;
#6548=CARTESIAN_POINT ( 'NONE',  ( 16.56782317627811096, 0.007739510688079516768, 0.006045301465876390737 ) ) ;
#6554=( BOUNDED_SURFACE ( )  B_SPLINE_SURFACE ( 3, 1, ( 
 ( #1993, #7734 ),
 ( #16611, #12126 ),
 ( #17959, #15264 ),
 ( #4859, #16526 ) ),
 .UNSPECIFIED., .F., .F., .T. ) 
 B_SPLINE_SURFACE_WITH_KNOTS ( ( 4, 4 ),
 ( 2, 2 ),
 ( 0.000000000000000000, 1.000000000000000000 ),
 ( 0.000000000000000000, 1.000000000000000000 ),
 .UNSPECIFIED. ) 
 GEOMETRIC_REPRESENTATION_ITEM ( )  RATIONAL_B_SPLINE_SURFACE ( (
 ( 1.000000000000000000, 1.000000000000000000),
 ( 0.9593108457356467333, 0.9995965569486454649),
 ( 0.9593108457356467333, 0.9995965569486454649),
 ( 1.000000000000000000, 1.000000000000000000) ) ) 
 REPRESENTATION_ITEM ( '' )  SURFACE ( )  );
#6555=( BOUNDED_SURFACE ( )  B_SPLINE_SURFACE ( 3, 1, ( 
 ( #9190, #7873 ),
 ( #9098, #7770 ),
 ( #13686, #12163 ),
 ( #7587, #17803 ) ),
 .UNSPECIFIED., .F., .F., .T. ) 
 B_SPLINE_SURFACE_WITH_KNOTS ( ( 4, 4 ),
 ( 2, 2 ),
 ( 0.000000000000000000, 1.000000000000000000 ),
 ( 0.000000000000000000, 1.000000000000000000 ),
 .UNSPECIFIED. ) 
 GEOMETRIC_REPRESENTATION_ITEM ( )  RATIONAL_B_SPLINE_SURFACE ( (
 ( 1.000000000000000000, 1.000000000000000000),
 ( 0.7792777138730158093, 0.9689936506012928330),
 ( 0.7792777138730158093, 0.9689936506012928330),
 ( 1.000000000000000000, 1.000000000000000000) ) ) 
 REPRESENTATION_ITEM ( '' )  SURFACE ( )  );
#6568=CIRCLE ( 'NONE', #17233, 16.06066017081991149 ) ;
#6571=CARTESIAN_POINT ( 'NONE',  ( 0.3137051932979757485, 12.91601973349276733, -4.679953077377353665 ) ) ;
#6572=EDGE_CURVE ( 'NONE', #4080, #12131, #4402, .T. ) ;
#6575=LINE ( 'NONE', #9247, #241 ) ;
#6583=ORIENTED_EDGE ( 'NONE', *, *, #12462, .F. ) ;
#6585=CARTESIAN_POINT ( 'NONE',  ( 2.123976203522053741, 10.37815841598491851, 11.67822624909929452 ) ) ;
#6590=CARTESIAN_POINT ( 'NONE',  ( 0.3137051932979792457, 11.37800749014131263, 7.698472063774513430 ) ) ;
#6595=CARTESIAN_POINT ( 'NONE',  ( 3.950837973638675393, -6.888253895133384930, 12.81214529934972823 ) ) ;
#6596=DIRECTION ( 'NONE',  ( 0.000000000000000000, 0.000000000000000000, 1.000000000000000000 ) ) ;
#6602=CARTESIAN_POINT ( 'NONE',  ( 16.56872352241294521, 0.01027347319884366721, 0.001821578298043820656 ) ) ;
#6604=CARTESIAN_POINT ( 'NONE',  ( 16.57210152137263393, 0.008007331252333427934, -0.01214401161737626612 ) ) ;
#6605=ADVANCED_FACE ( 'NONE', ( #10428 ), #12579, .F. ) ;
#6611=VERTEX_POINT ( 'NONE', #16553 ) ;
#6613=B_SPLINE_CURVE_WITH_KNOTS ( 'NONE', 3,
 ( #8724, #18751, #1079, #11598, #12646, #18570, #5650, #15696, #10062, #12830, #6826, #14550, #18657 ),
 .UNSPECIFIED., .F., .F.,
 ( 4, 3, 3, 3, 4 ),
 ( 1.734723475976807094E-18, 0.0002299804304191470643, 0.0004599608082120238165, 0.0006467586077648016917, 0.0008336169836825990491 ),
 .UNSPECIFIED. ) ;
#6615=CARTESIAN_POINT ( 'NONE',  ( 0.4862570985993252548, -5.003653737315580052, 12.97920246947877665 ) ) ;
#6617=EDGE_CURVE ( 'NONE', #8437, #16664, #1052, .T. ) ;
#6620=EDGE_CURVE ( 'NONE', #1184, #17773, #17013, .T. ) ;
#6623=B_SPLINE_CURVE_WITH_KNOTS ( 'NONE', 3,
 ( #11018, #2305, #8150, #6717, #12526, #18360 ),
 .UNSPECIFIED., .F., .F.,
 ( 4, 2, 4 ),
 ( 1.939479807224432123E-18, 0.001657017934711440621, 0.003314035869422879074 ),
 .UNSPECIFIED. ) ;
#6624=CARTESIAN_POINT ( 'NONE',  ( 16.56872352241294521, 0.007512283835804314455, -0.007240717549633915451 ) ) ;
#6629=CARTESIAN_POINT ( 'NONE',  ( 16.58200780006414732, -0.009393638146078483672, -0.006043560077721808060 ) ) ;
#6638=EDGE_LOOP ( 'NONE', ( #13503, #17754, #10790, #17207 ) ) ;
#6646=B_SPLINE_CURVE_WITH_KNOTS ( 'NONE', 3,
 ( #5198, #12828, #18655, #11044 ),
 .UNSPECIFIED., .F., .F.,
 ( 4, 4 ),
 ( 9.796581096179191873E-17, 0.002004993803842611885 ),
 .UNSPECIFIED. ) ;
#6647=DIRECTION ( 'NONE',  ( -1.000000000000000000, -0.000000000000000000, -0.000000000000000000 ) ) ;
#6655=CARTESIAN_POINT ( 'NONE',  ( 0.4754618798421171855, -11.68486377711960778, -7.564402563418600067 ) ) ;
#6656=ORIENTED_EDGE ( 'NONE', *, *, #510, .T. ) ;
#6659=EDGE_LOOP ( 'NONE', ( #14671, #4196, #18164, #18040 ) ) ;
#6660=B_SPLINE_CURVE_WITH_KNOTS ( 'NONE', 3,
 ( #7764, #17794, #679, #13572 ),
 .UNSPECIFIED., .F., .F.,
 ( 4, 4 ),
 ( 1.464275143509529362E-17, 0.003005512676784844427 ),
 .UNSPECIFIED. ) ;
#6663=CARTESIAN_POINT ( 'NONE',  ( 0.3148208552358953138, 11.24855514421875569, 7.888357771040743316 ) ) ;
#6665=CARTESIAN_POINT ( 'NONE',  ( 3.074695600507118431, 2.772091048739504959, -15.30693405987805811 ) ) ;
#6667=CARTESIAN_POINT ( 'NONE',  ( 0.4385251269669978580, 10.76637725024251857, 8.732456510146114681 ) ) ;
#6668=CARTESIAN_POINT ( 'NONE',  ( 0.3137051932979757485, 12.91601973349276733, -4.679953077377353665 ) ) ;
#6669=CARTESIAN_POINT ( 'NONE',  ( 1.959212340397943120, -7.909199412631233272, 9.750290364083607386 ) ) ;
#6671=CARTESIAN_POINT ( 'NONE',  ( 2.697797270744669351, 3.226410068829429711, 12.89731672021091846 ) ) ;
#6674=VERTEX_POINT ( 'NONE', #4004 ) ;
#6676=ORIENTED_EDGE ( 'NONE', *, *, #10308, .F. ) ;
#6680=EDGE_CURVE ( 'NONE', #1784, #14201, #18390, .T. ) ;
#6681=CARTESIAN_POINT ( 'NONE',  ( 2.697797270744668019, -0.9169917281808188658, 13.26309265156976913 ) ) ;
#6690=CARTESIAN_POINT ( 'NONE',  ( 8.522092701127531811, 4.388629235579577070, 5.397361180353158261 ) ) ;
#6692=CARTESIAN_POINT ( 'NONE',  ( 3.074695600507159732, -15.30693405987801370, -2.772091048739451669 ) ) ;
#6696=CARTESIAN_POINT ( 'NONE',  ( 1.846955891736114852, 11.74973605926570386, -4.094751675596581819 ) ) ;
#6700=B_SPLINE_CURVE_WITH_KNOTS ( 'NONE', 3,
 ( #9049, #17951, #10483, #12015, #1792, #13439 ),
 .UNSPECIFIED., .F., .F.,
 ( 4, 2, 4 ),
 ( 4.206917491929696500E-17, 0.0002014099069817281611, 0.0004028198139634142552 ),
 .UNSPECIFIED. ) ;
#6703=ORIENTED_EDGE ( 'NONE', *, *, #11235, .T. ) ;
#6705=CARTESIAN_POINT ( 'NONE',  ( 3.950837973638668288, 0.000000000000000000, 0.000000000000000000 ) ) ;
#6712=EDGE_CURVE ( 'NONE', #12585, #6128, #12902, .T. ) ;
#6714=CARTESIAN_POINT ( 'NONE',  ( 1.846524061778019199, 10.27028962889607477, -7.023652644192158512 ) ) ;
#6717=CARTESIAN_POINT ( 'NONE',  ( 1.977228804422745068, 3.321884655131805975, -15.04020501276218091 ) ) ;
#6720=EDGE_LOOP ( 'NONE', ( #12578, #14239, #10892, #8230 ) ) ;
#6721=LINE ( 'NONE', #11023, #5405 ) ;
#6724=CARTESIAN_POINT ( 'NONE',  ( 0.3137051932979757485, -4.679953077377398074, -12.91601973349275134 ) ) ;
#6733=ADVANCED_FACE ( 'NONE', ( #5802 ), #4045, .F. ) ;
#6737=B_SPLINE_CURVE_WITH_KNOTS ( 'NONE', 3,
 ( #4231, #14637, #10245, #13007, #13110, #14539 ),
 .UNSPECIFIED., .F., .F.,
 ( 4, 2, 4 ),
 ( 0.000000000000000000, 0.001657017934710630505, 0.003314035869421261011 ),
 .UNSPECIFIED. ) ;
#6754=CARTESIAN_POINT ( 'NONE',  ( 0.3145734862173260038, 10.93207848441433683, 8.321353293018871611 ) ) ;
#6756=CARTESIAN_POINT ( 'NONE',  ( 1.846138399168762101, 7.646096044339892650, 9.815003036200437236 ) ) ;
#6757=CARTESIAN_POINT ( 'NONE',  ( 16.56872352241294521, -0.01033355228142500762, -0.001442253899401184716 ) ) ;
#6765=VERTEX_POINT ( 'NONE', #13074 ) ;
#6766=VERTEX_POINT ( 'NONE', #11464 ) ;
#6767=EDGE_CURVE ( 'NONE', #8500, #16009, #152, .T. ) ;
#6770=CARTESIAN_POINT ( 'NONE',  ( 16.58200780006414732, 0.01115192838421469497, -0.0006320991582341122352 ) ) ;
#6772=CARTESIAN_POINT ( 'NONE',  ( 0.4754618798421162973, -13.45049478164062329, 3.583352865732616355 ) ) ;
#6774=CARTESIAN_POINT ( 'NONE',  ( 0.3058872367615226295, -8.562166468153792565, 10.75034008168912791 ) ) ;
#6781=DIRECTION ( 'NONE',  ( -0.7561779333270775005, 0.4122479608995705536, 0.5081796452863259761 ) ) ;
#6788=AXIS2_PLACEMENT_3D ( 'NONE', #14532, #18733, #4225 ) ;
#6794=CARTESIAN_POINT ( 'NONE',  ( 1.847426409206450959, -2.029922383240494730E-11, 12.44303504652081038 ) ) ;
#6796=CARTESIAN_POINT ( 'NONE',  ( 0.3939875929385618369, 7.545068896001375869, -11.57636969881026801 ) ) ;
#6797=CARTESIAN_POINT ( 'NONE',  ( 16.58200780006414732, 0.008650561019685530303, -0.007066318000004736047 ) ) ;
#6800=CARTESIAN_POINT ( 'NONE',  ( 2.123976203522053741, -15.26039569100257509, -3.347755036806064677 ) ) ;
#6806=CARTESIAN_POINT ( 'NONE',  ( 16.56679352167444819, 0.006526964904752955397, 0.006618561353599231728 ) ) ;
#6809=CARTESIAN_POINT ( 'NONE',  ( 1.959212340397945118, 4.509090217468684436, -11.71715421693493830 ) ) ;
#6810=EDGE_LOOP ( 'NONE', ( #180, #17862, #4599, #9469 ) ) ;
#6813=ORIENTED_EDGE ( 'NONE', *, *, #10539, .T. ) ;
#6818=CARTESIAN_POINT ( 'NONE',  ( 1.861706995891668104, 12.00328602385080679, 3.332865258614018611 ) ) ;
#6820=CARTESIAN_POINT ( 'NONE',  ( 3.950837973638668288, 0.000000000000000000, 0.000000000000000000 ) ) ;
#6824=CARTESIAN_POINT ( 'NONE',  ( 16.56753206892534891, 0.009369540855502532517, -0.001549402974394196693 ) ) ;
#6826=CARTESIAN_POINT ( 'NONE',  ( 1.846822687350020198, 3.566003975885688515, 11.92063725419900777 ) ) ;
#6828=EDGE_CURVE ( 'NONE', #2096, #16044, #17146, .T. ) ;
#6829=CARTESIAN_POINT ( 'NONE',  ( 8.522092701127531811, -3.777034505568479528, -5.841710761610173108 ) ) ;
#6831=ORIENTED_EDGE ( 'NONE', *, *, #3891, .F. ) ;
#6832=AXIS2_PLACEMENT_3D ( 'NONE', #7490, #16085, #17512 ) ;
#6835=VERTEX_POINT ( 'NONE', #6488 ) ;
#6837=EDGE_CURVE ( 'NONE', #11580, #9697, #15274, .T. ) ;
#6839=CARTESIAN_POINT ( 'NONE',  ( 1.846822687350014869, -9.891732594446525084, -7.547953575784235092 ) ) ;
#6841=CARTESIAN_POINT ( 'NONE',  ( 1.918921323896325193, 6.832782632379378107, 10.48468902844554052 ) ) ;
#6843=CARTESIAN_POINT ( 'NONE',  ( 16.56822296793089322, 0.01011126603341077484, -0.0007467251401297481410 ) ) ;
#6847=FACE_OUTER_BOUND ( 'NONE', #9184, .T. ) ;
#6856=CARTESIAN_POINT ( 'NONE',  ( 0.3095370825347234511, 7.700448427571873644, 11.38092634279631277 ) ) ;
#6859=ORIENTED_EDGE ( 'NONE', *, *, #4336, .F. ) ;
#6863=CARTESIAN_POINT ( 'NONE',  ( 1.847247051441594179, -11.78111530882020297, -4.004229874809150047 ) ) ;
#6867=CARTESIAN_POINT ( 'NONE',  ( 3.074695600507264537, -13.70113613813205689, 7.366518011945889732 ) ) ;
#6868=CARTESIAN_POINT ( 'NONE',  ( 0.3939822652208125886, 13.34132036472942318, -3.598529276937123544 ) ) ;
#6870=LINE ( 'NONE', #12693, #6969 ) ;
#6871=ORIENTED_EDGE ( 'NONE', *, *, #16460, .T. ) ;
#6874=ORIENTED_EDGE ( 'NONE', *, *, #8699, .T. ) ;
#6880=B_SPLINE_CURVE_WITH_KNOTS ( 'NONE', 3,
 ( #17949, #13533, #450, #12209, #10683, #6283 ),
 .UNSPECIFIED., .F., .F.,
 ( 4, 2, 4 ),
 ( 4.276569467073304015E-17, 0.0002014099069817285948, 0.0004028198139634144178 ),
 .UNSPECIFIED. ) ;
#6887=CIRCLE ( 'NONE', #17567, 14.54644660717763927 ) ;
#6889=AXIS2_PLACEMENT_3D ( 'NONE', #5508, #4087, #15740 ) ;
#6906=ORIENTED_EDGE ( 'NONE', *, *, #16626, .F. ) ;
#6918=CARTESIAN_POINT ( 'NONE',  ( 16.56753206892534891, -0.008490833999798035742, 0.004253784598196731770 ) ) ;
#6922=CARTESIAN_POINT ( 'NONE',  ( 16.56753206892534891, -0.004253784598196240843, 0.008490833999798906573 ) ) ;
#6925=ORIENTED_EDGE ( 'NONE', *, *, #4469, .T. ) ;
#6926=CARTESIAN_POINT ( 'NONE',  ( 0.3151928476913523069, 11.11514699826562946, -8.075884471919630769 ) ) ;
#6927=DIRECTION ( 'NONE',  ( 1.000000000000000000, 0.000000000000000000, 0.000000000000000000 ) ) ;
#6928=B_SPLINE_CURVE_WITH_KNOTS ( 'NONE', 3,
 ( #3836, #2393, #7084, #8246 ),
 .UNSPECIFIED., .F., .F.,
 ( 4, 4 ),
 ( 2.359479019930958314E-17, 0.003005512676784853534 ),
 .UNSPECIFIED. ) ;
#6929=EDGE_LOOP ( 'NONE', ( #5431, #17373, #280, #13218 ) ) ;
#6930=CONICAL_SURFACE ( 'NONE', #4807, 14.54644660717763927, 0.8559913436420816257 ) ;
#6931=VECTOR ( 'NONE', #10960, 1000.000000000000227 ) ;
#6933=ORIENTED_EDGE ( 'NONE', *, *, #15837, .T. ) ;
#6934=( GEOMETRIC_REPRESENTATION_CONTEXT ( 3 ) GLOBAL_UNCERTAINTY_ASSIGNED_CONTEXT ( ( #1573 ) ) GLOBAL_UNIT_ASSIGNED_CONTEXT ( ( #18630, #18272, #15490 ) ) REPRESENTATION_CONTEXT ( 'NONE', 'WORKASPACE' ) );
#6936=ORIENTED_EDGE ( 'NONE', *, *, #5449, .T. ) ;
#6938=VECTOR ( 'NONE', #4704, 1000.000000000000114 ) ;
#6939=CARTESIAN_POINT ( 'NONE',  ( 2.636624412714236865, 0.000000000000000000, 0.000000000000000000 ) ) ;
#6942=VECTOR ( 'NONE', #3090, 1000.000000000000000 ) ;
#6948=CARTESIAN_POINT ( 'NONE',  ( 0.3939875929385670550, -12.90850834464103691, 4.930599594904505167 ) ) ;
#6954=ORIENTED_EDGE ( 'NONE', *, *, #4018, .T. ) ;
#6956=VERTEX_POINT ( 'NONE', #13926 ) ;
#6965=CARTESIAN_POINT ( 'NONE',  ( 16.56872352241294521, 0.001821578298044641397, 0.01027347319884442528 ) ) ;
#6966=DIRECTION ( 'NONE',  ( 0.7635533937278214944, 0.6204116510013490959, -0.1790966170213899034 ) ) ;
#6969=VECTOR ( 'NONE', #18524, 1000.000000000000000 ) ;
#6971=CARTESIAN_POINT ( 'NONE',  ( 0.4385251269669947494, 13.39302348765813910, -3.577373010348575910 ) ) ;
#6983=LINE ( 'NONE', #8785, #10051 ) ;
#6985=CARTESIAN_POINT ( 'NONE',  ( 0.4754618798421167414, 13.45049478164064638, -3.583352865732531534 ) ) ;
#6998=EDGE_CURVE ( 'NONE', #6128, #3394, #17155, .T. ) ;
#7001=CARTESIAN_POINT ( 'NONE',  ( 3.074695600507147297, -15.41438262616236088, -2.093687500612132268 ) ) ;
#7010=B_SPLINE_CURVE_WITH_KNOTS ( 'NONE', 3,
 ( #8770, #5506, #1504, #18887 ),
 .UNSPECIFIED., .F., .F.,
 ( 4, 4 ),
 ( 3.019714627835872489E-16, 0.002004993803842318283 ),
 .UNSPECIFIED. ) ;
#7011=ORIENTED_EDGE ( 'NONE', *, *, #12790, .T. ) ;
#7029=LINE ( 'NONE', #2514, #17907 ) ;
#7032=CARTESIAN_POINT ( 'NONE',  ( 8.522092701127531811, 6.946128462138595694, -0.3779863304871462493 ) ) ;
#7039=EDGE_CURVE ( 'NONE', #10260, #10485, #2215, .T. ) ;
#7045=( BOUNDED_SURFACE ( )  B_SPLINE_SURFACE ( 3, 1, ( 
 ( #9609, #11335 ),
 ( #8552, #1193 ),
 ( #14376, #7124 ),
 ( #15438, #3968 ) ),
 .UNSPECIFIED., .F., .F., .T. ) 
 B_SPLINE_SURFACE_WITH_KNOTS ( ( 4, 4 ),
 ( 2, 2 ),
 ( 0.000000000000000000, 1.000000000000000000 ),
 ( 0.000000000000000000, 1.000000000000000000 ),
 .UNSPECIFIED. ) 
 GEOMETRIC_REPRESENTATION_ITEM ( )  RATIONAL_B_SPLINE_SURFACE ( (
 ( 1.000000000000000000, 1.000000000000000000),
 ( 0.9933953342250436691, 0.8357391271907733676),
 ( 0.9933953342250436691, 0.8357391271907733676),
 ( 1.000000000000000000, 1.000000000000000000) ) ) 
 REPRESENTATION_ITEM ( '' )  SURFACE ( )  );
#7046=ORIENTED_EDGE ( 'NONE', *, *, #14186, .F. ) ;
#7048=CARTESIAN_POINT ( 'NONE',  ( 1.847372867223028070, 3.945260592619209028, -11.80112642014550239 ) ) ;
#7050=CARTESIAN_POINT ( 'NONE',  ( 16.56782317627811096, -0.009228812961909619098, -0.003357783021327203059 ) ) ;
#7051=CARTESIAN_POINT ( 'NONE',  ( 8.522092701127531811, 0.3779863304872196350, -6.946128462138591253 ) ) ;
#7057=CARTESIAN_POINT ( 'NONE',  ( 0.3151928476913618549, -11.11514699826556196, 8.075884471919712482 ) ) ;
#7058=LINE ( 'NONE', #14223, #2846 ) ;
#7059=CARTESIAN_POINT ( 'NONE',  ( 0.3132635586635980629, 4.743936529203241825, 12.89236642382223508 ) ) ;
#7062=ORIENTED_EDGE ( 'NONE', *, *, #13575, .F. ) ;
#7064=ORIENTED_EDGE ( 'NONE', *, *, #17094, .T. ) ;
#7068=CARTESIAN_POINT ( 'NONE',  ( 1.847421816787902404, -0.02876707915213067360, 12.44300551404155541 ) ) ;
#7073=CARTESIAN_POINT ( 'NONE',  ( 1.847426409206471831, -0.06227732482761883653, -12.44303504652092229 ) ) ;
#7079=CARTESIAN_POINT ( 'NONE',  ( 0.3137051932979792457, -8.442169467526928983, 10.83767969834800127 ) ) ;
#7080=SURFACE_SIDE_STYLE ('',( #8332 ) ) ;
#7083=EDGE_CURVE ( 'NONE', #1012, #447, #4155, .T. ) ;
#7084=CARTESIAN_POINT ( 'NONE',  ( 2.705023505549863039, 10.24007717649592841, -8.489131503859667305 ) ) ;
#7086=ORIENTED_EDGE ( 'NONE', *, *, #15625, .T. ) ;
#7087=CARTESIAN_POINT ( 'NONE',  ( 0.3148213771069372502, 8.260246460850879657, -10.97836617636215628 ) ) ;
#7092=CARTESIAN_POINT ( 'NONE',  ( 1.847247051441594179, 9.967131402978196775, 7.448813758297206711 ) ) ;
#7093=CARTESIAN_POINT ( 'NONE',  ( 2.123976203522053741, 15.54801196254787143, -1.531817366691807125 ) ) ;
#7098=CARTESIAN_POINT ( 'NONE',  ( 1.977436885025100510, 3.321781585409006698, 15.04044112860174209 ) ) ;
#7099=CARTESIAN_POINT ( 'NONE',  ( 0.3095370825347234511, -13.73357284481724427, -0.4597470195091644674 ) ) ;
#7102=COLOUR_RGB ( '', 0.09019608, 0.27058824, 0.51372549) ;
#7109=CARTESIAN_POINT ( 'NONE',  ( 0.8740779401509238822, -13.83508928787439096, -3.609949156401517367 ) ) ;
#7110=DIRECTION ( 'NONE',  ( 0.000000000000000000, 0.000000000000000000, -1.000000000000000000 ) ) ;
#7112=ORIENTED_EDGE ( 'NONE', *, *, #8906, .F. ) ;
#7113=CARTESIAN_POINT ( 'NONE',  ( 16.57778382496167424, -0.001819584982831791388, -0.01482878558584694619 ) ) ;
#7116=ORIENTED_EDGE ( 'NONE', *, *, #8349, .T. ) ;
#7117=EDGE_CURVE ( 'NONE', #13343, #5119, #16935, .T. ) ;
#7119=B_SPLINE_CURVE_WITH_KNOTS ( 'NONE', 3,
 ( #6400, #17970, #18242, #16620 ),
 .UNSPECIFIED., .F., .F.,
 ( 4, 4 ),
 ( 0.000000000000000000, 0.002004993803840905784 ),
 .UNSPECIFIED. ) ;
#7120=CARTESIAN_POINT ( 'NONE',  ( 16.57605080000000086, 0.000000000000000000, 0.000000000000000000 ) ) ;
#7124=CARTESIAN_POINT ( 'NONE',  ( 0.3720661004400037664, 4.951033743989821545, -12.89739157014187221 ) ) ;
#7125=CARTESIAN_POINT ( 'NONE',  ( 0.3058872367615230181, -7.578326039752686150, 11.46514199369355325 ) ) ;
#7129=CARTESIAN_POINT ( 'NONE',  ( 16.58200780006414732, 0.009393638146079845430, -0.006043560077721606832 ) ) ;
#7136=VERTEX_POINT ( 'NONE', #10359 ) ;
#7137=EDGE_LOOP ( 'NONE', ( #17451, #18344, #6111, #5183 ) ) ;
#7138=CARTESIAN_POINT ( 'NONE',  ( 1.846138399168762101, 4.238866729160568170, -11.69739621335917690 ) ) ;
#7140=FACE_OUTER_BOUND ( 'NONE', #13932, .T. ) ;
#7145=CARTESIAN_POINT ( 'NONE',  ( 0.3137051932979792457, 13.73004976592202198, 0.4596302728640249136 ) ) ;
#7150=CARTESIAN_POINT ( 'NONE',  ( 2.002547531651519996, -10.57595306287296921, 6.845637710436153434 ) ) ;
#7151=CARTESIAN_POINT ( 'NONE',  ( 1.342453679581834924, -14.76648944001040142, 0.9602753779830212055 ) ) ;
#7152=CARTESIAN_POINT ( 'NONE',  ( 0.3308579732647022875, 13.25341063505880967, -3.680601586799737923 ) ) ;
#7158=EDGE_CURVE ( 'NONE', #6426, #1712, #11988, .T. ) ;
#7162=EDGE_LOOP ( 'NONE', ( #5443, #9206, #1655, #4254 ) ) ;
#7169=CARTESIAN_POINT ( 'NONE',  ( 0.3095370825347224519, -4.681152801286072140, -12.91933430393612703 ) ) ;
#7172=CARTESIAN_POINT ( 'NONE',  ( 1.861706995891666105, -10.38589138506421072, -6.878962591851865760 ) ) ;
#7173=CARTESIAN_POINT ( 'NONE',  ( 0.3150692679895994996, -13.73846569174796883, -0.1531143455845980217 ) ) ;
#7176=CARTESIAN_POINT ( 'NONE',  ( 0.4384471787762814210, -3.577367180593642892, 13.39294437382617353 ) ) ;
#7178=ADVANCED_FACE ( 'NONE', ( #4537 ), #144, .F. ) ;
#7183=ORIENTED_EDGE ( 'NONE', *, *, #9709, .T. ) ;
#7186=ORIENTED_EDGE ( 'NONE', *, *, #7912, .F. ) ;
#7187=CARTESIAN_POINT ( 'NONE',  ( 8.438534575730034959, 5.688336279099046600, 3.845978796786057696 ) ) ;
#7188=EDGE_CURVE ( 'NONE', #14993, #11535, #14187, .T. ) ;
#7190=VERTEX_POINT ( 'NONE', #17729 ) ;
#7191=CARTESIAN_POINT ( 'NONE',  ( 2.002547531651519996, 0.6781519942171739812, 12.57989064830759851 ) ) ;
#7199=CARTESIAN_POINT ( 'NONE',  ( 16.56782317627811096, 0.008141063682853480823, -0.005492611183758445634 ) ) ;
#7209=CARTESIAN_POINT ( 'NONE',  ( 3.950837973638677170, 13.10350451991849141, -6.316429227969337923 ) ) ;
#7210=CARTESIAN_POINT ( 'NONE',  ( 2.002547531651519996, -11.75462648437098601, -4.532360870844453160 ) ) ;
#7211=FACE_OUTER_BOUND ( 'NONE', #9431, .T. ) ;
#7212=ORIENTED_EDGE ( 'NONE', *, *, #9685, .F. ) ;
#7214=FACE_OUTER_BOUND ( 'NONE', #14533, .T. ) ;
#7216=EDGE_CURVE ( 'NONE', #8524, #13924, #5086, .T. ) ;
#7223=DIRECTION ( 'NONE',  ( 0.7561779333270775005, -0.5081796452863246438, -0.4122479608995723299 ) ) ;
#7224=CARTESIAN_POINT ( 'NONE',  ( 0.8740764193769881008, 5.211550415969331773, -13.31469591265785901 ) ) ;
#7225=PRODUCT_DEFINITION_SHAPE ( 'NONE', 'NONE',  #6272 ) ;
#7227=CARTESIAN_POINT ( 'NONE',  ( 1.977436885027412439, 13.27782258182005748, -7.806953934146017460 ) ) ;
#7231=EDGE_LOOP ( 'NONE', ( #5136, #5586, #2383, #4823, #1059, #2826 ) ) ;
#7234=VERTEX_POINT ( 'NONE', #35 ) ;
#7237=EDGE_LOOP ( 'NONE', ( #1081, #1699, #12381, #7281 ) ) ;
#7240=( BOUNDED_SURFACE ( )  B_SPLINE_SURFACE ( 3, 1, ( 
 ( #2433, #1005 ),
 ( #5576, #16975 ),
 ( #6843, #15441 ),
 ( #18674, #2352 ) ),
 .UNSPECIFIED., .F., .F., .T. ) 
 B_SPLINE_SURFACE_WITH_KNOTS ( ( 4, 4 ),
 ( 2, 2 ),
 ( 0.000000000000000000, 1.000000000000000000 ),
 ( 0.000000000000000000, 1.000000000000000000 ),
 .UNSPECIFIED. ) 
 GEOMETRIC_REPRESENTATION_ITEM ( )  RATIONAL_B_SPLINE_SURFACE ( (
 ( 1.000000000000000000, 1.000000000000000000),
 ( 0.9933953342250436691, 0.8357391271907733676),
 ( 0.9933953342250436691, 0.8357391271907733676),
 ( 1.000000000000000000, 1.000000000000000000) ) ) 
 REPRESENTATION_ITEM ( '' )  SURFACE ( )  );
#7245=CARTESIAN_POINT ( 'NONE',  ( 16.56753206892534891, -0.001421777558676013808, 0.009389754735542241854 ) ) ;
#7247=CARTESIAN_POINT ( 'NONE',  ( 3.950837973638677170, 6.316429227969654114, -13.10350451991833687 ) ) ;
#7251=CARTESIAN_POINT ( 'NONE',  ( 1.977228804422749064, -1.488378900182820264, -15.33060379559159259 ) ) ;
#7256=ORIENTED_EDGE ( 'NONE', *, *, #2547, .T. ) ;
#7257=ORIENTED_EDGE ( 'NONE', *, *, #3891, .T. ) ;
#7258=ADVANCED_FACE ( 'NONE', ( #10944 ), #13806, .T. ) ;
#7260=EDGE_CURVE ( 'NONE', #349, #13704, #10457, .T. ) ;
#7262=EDGE_LOOP ( 'NONE', ( #11071, #6519, #16032, #6583 ) ) ;
#7263=CARTESIAN_POINT ( 'NONE',  ( 1.562796894703937678, 0.000000000000000000, 0.000000000000000000 ) ) ;
#7266=CARTESIAN_POINT ( 'NONE',  ( 1.846524061778021419, 11.71897913237549105, 4.180439405448364454 ) ) ;
#7269=ORIENTED_EDGE ( 'NONE', *, *, #16992, .F. ) ;
#7273=CARTESIAN_POINT ( 'NONE',  ( 0.3137051932979792457, -13.73004976592202375, 0.4596302728639276580 ) ) ;
#7274=CARTESIAN_POINT ( 'NONE',  ( 0.3095370825347224519, 8.444334731364007141, 10.84046130709061373 ) ) ;
#7276=CARTESIAN_POINT ( 'NONE',  ( 2.697797270744668463, 0.9169917281809109033, -13.26309265156976203 ) ) ;
#7277=( BOUNDED_SURFACE ( )  B_SPLINE_SURFACE ( 3, 1, ( 
 ( #15190, #13833 ),
 ( #15359, #13663 ),
 ( #10795, #930 ),
 ( #16618, #9358 ) ),
 .UNSPECIFIED., .F., .F., .F. ) 
 B_SPLINE_SURFACE_WITH_KNOTS ( ( 4, 4 ),
 ( 2, 2 ),
 ( 0.000000000000000000, 1.000000000000000000 ),
 ( 0.000000000000000000, 1.000000000000000000 ),
 .UNSPECIFIED. ) 
 GEOMETRIC_REPRESENTATION_ITEM ( )  RATIONAL_B_SPLINE_SURFACE ( (
 ( 1.000000000000000000, 1.000000000000000000),
 ( 0.7792777138730158093, 0.9689936506012928330),
 ( 0.7792777138730158093, 0.9689936506012928330),
 ( 1.000000000000000000, 1.000000000000000000) ) ) 
 REPRESENTATION_ITEM ( '' )  SURFACE ( )  );
#7281=ORIENTED_EDGE ( 'NONE', *, *, #4558, .T. ) ;
#7283=CARTESIAN_POINT ( 'NONE',  ( 16.56822296793089322, -0.008619100080558715279, 0.005339139727952894703 ) ) ;
#7285=ADVANCED_FACE ( 'NONE', ( #8164 ), #15414, .T. ) ;
#7292=DIRECTION ( 'NONE',  ( 0.000000000000000000, 0.000000000000000000, 1.000000000000000000 ) ) ;
#7294=B_SPLINE_CURVE_WITH_KNOTS ( 'NONE', 3,
 ( #14542, #17413, #7098, #2494, #17315, #4233 ),
 .UNSPECIFIED., .F., .F.,
 ( 4, 2, 4 ),
 ( 0.000000000000000000, 0.001656992708821696143, 0.003313985417643392287 ),
 .UNSPECIFIED. ) ;
#7301=CARTESIAN_POINT ( 'NONE',  ( 16.56872352241294521, 0.004564908236400220913, 0.009382111268606271176 ) ) ;
#7304=ORIENTED_EDGE ( 'NONE', *, *, #16141, .F. ) ;
#7309=ORIENTED_EDGE ( 'NONE', *, *, #2400, .F. ) ;
#7310=CARTESIAN_POINT ( 'NONE',  ( 16.56872352241294521, 0.007240717549633990044, -0.007512283835805476720 ) ) ;
#7311=EDGE_CURVE ( 'NONE', #3395, #10485, #5317, .T. ) ;
#7313=DIRECTION ( 'NONE',  ( -1.000000000000000000, -0.000000000000000000, -0.000000000000000000 ) ) ;
#7318=CARTESIAN_POINT ( 'NONE',  ( 0.8740779401506997282, 9.070947476926598085, 11.05257166392028267 ) ) ;
#7319=CARTESIAN_POINT ( 'NONE',  ( 16.58200780006414732, 0.004047297414159048250, -0.01041078477704050417 ) ) ;
#7325=ORIENTED_EDGE ( 'NONE', *, *, #2865, .F. ) ;
#7330=B_SPLINE_CURVE_WITH_KNOTS ( 'NONE', 3,
 ( #3304, #1789, #354, #6183, #10585, #17950 ),
 .UNSPECIFIED., .F., .F.,
 ( 4, 2, 4 ),
 ( 0.000000000000000000, 0.0001828790815886945087, 0.0003657581631773890174 ),
 .UNSPECIFIED. ) ;
#7333=B_SPLINE_CURVE_WITH_KNOTS ( 'NONE', 3,
 ( #18165, #1728, #3441, #9470, #10812, #595 ),
 .UNSPECIFIED., .F., .F.,
 ( 4, 2, 4 ),
 ( 3.436766974507050665E-17, 0.0001825746017570568534, 0.0003651492035140793376 ),
 .UNSPECIFIED. ) ;
#7338=B_SPLINE_CURVE_WITH_KNOTS ( 'NONE', 3,
 ( #5034, #14978, #9440, #12125, #7733, #17958 ),
 .UNSPECIFIED., .F., .F.,
 ( 4, 2, 4 ),
 ( 0.000000000000000000, 0.001657017934709840989, 0.003314035869419681979 ),
 .UNSPECIFIED. ) ;
#7340=CARTESIAN_POINT ( 'NONE',  ( 3.950837973638676281, 6.316429227969464932, 13.10350451991842569 ) ) ;
#7346=CARTESIAN_POINT ( 'NONE',  ( 2.002547531651519996, 6.845637710436341727, -10.57595306287284842 ) ) ;
#7350=CARTESIAN_POINT ( 'NONE',  ( 0.3720661004400040439, -11.58636699658209679, -7.524064345033593781 ) ) ;
#7355=( BOUNDED_SURFACE ( )  B_SPLINE_SURFACE ( 3, 1, ( 
 ( #2271, #15729 ),
 ( #5416, #9627 ),
 ( #8120, #12862 ),
 ( #5589, #6772 ) ),
 .UNSPECIFIED., .F., .F., .T. ) 
 B_SPLINE_SURFACE_WITH_KNOTS ( ( 4, 4 ),
 ( 2, 2 ),
 ( 0.000000000000000000, 1.000000000000000000 ),
 ( 0.000000000000000000, 1.000000000000000000 ),
 .UNSPECIFIED. ) 
 GEOMETRIC_REPRESENTATION_ITEM ( )  RATIONAL_B_SPLINE_SURFACE ( (
 ( 1.000000000000000000, 1.000000000000000000),
 ( 0.9933953342250436691, 0.8357391271907733676),
 ( 0.9933953342250436691, 0.8357391271907733676),
 ( 1.000000000000000000, 1.000000000000000000) ) ) 
 REPRESENTATION_ITEM ( '' )  SURFACE ( )  );
#7359=CARTESIAN_POINT ( 'NONE',  ( 16.56822296793089322, 0.008619100080558677116, -0.005339139727952955418 ) ) ;
#7360=ORIENTED_EDGE ( 'NONE', *, *, #4718, .T. ) ;
#7365=ORIENTED_EDGE ( 'NONE', *, *, #7703, .T. ) ;
#7370=ADVANCED_FACE ( 'NONE', ( #3567 ), #10010, .F. ) ;
#7372=EDGE_CURVE ( 'NONE', #6541, #13630, #1922, .T. ) ;
#7374=ORIENTED_EDGE ( 'NONE', *, *, #625, .F. ) ;
#7378=VERTEX_POINT ( 'NONE', #5459 ) ;
#7379=CARTESIAN_POINT ( 'NONE',  ( 0.3137051932979792457, 8.442169467527008919, -10.83767969834794087 ) ) ;
#7384=ORIENTED_EDGE ( 'NONE', *, *, #8086, .F. ) ;
#7385=CARTESIAN_POINT ( 'NONE',  ( 1.846138399168762101, -4.238866729160323032, -11.69739621335926394 ) ) ;
#7387=LINE ( 'NONE', #3054, #5757 ) ;
#7391=EDGE_CURVE ( 'NONE', #4602, #18903, #10789, .T. ) ;
#7396=CARTESIAN_POINT ( 'NONE',  ( 1.861706995891675653, 0.5394761475745838419, 12.44571539481144207 ) ) ;
#7398=CARTESIAN_POINT ( 'NONE',  ( 1.959212340397962882, -12.53706137681889210, -0.6675998551413099280 ) ) ;
#7401=CARTESIAN_POINT ( 'NONE',  ( 3.950837973638668288, 0.000000000000000000, 0.000000000000000000 ) ) ;
#7402=B_SPLINE_CURVE_WITH_KNOTS ( 'NONE', 3,
 ( #16705, #9617, #12128, #3789, #652, #3415 ),
 .UNSPECIFIED., .F., .F.,
 ( 4, 2, 4 ),
 ( 0.000000000000000000, 0.001500839035891550054, 0.003001678071783100109 ),
 .UNSPECIFIED. ) ;
#7405=CARTESIAN_POINT ( 'NONE',  ( 0.3095370825347224519, -7.700448427571953580, 11.38092634279625770 ) ) ;
#7406=ORIENTED_EDGE ( 'NONE', *, *, #5834, .T. ) ;
#7407=CARTESIAN_POINT ( 'NONE',  ( 1.959212340397945562, 3.239239832449027467, 12.12975361829676579 ) ) ;
#7408=AXIS2_PLACEMENT_3D ( 'NONE', #10264, #7313, #6253 ) ;
#7410=CARTESIAN_POINT ( 'NONE',  ( 2.705023505549866147, 7.115606223895331262, -11.23800170568049062 ) ) ;
#7411=B_SPLINE_CURVE_WITH_KNOTS ( 'NONE', 3,
 ( #2914, #18794, #10299, #18695, #15738, #7150 ),
 .UNSPECIFIED., .F., .F.,
 ( 4, 2, 4 ),
 ( 0.000000000000000000, 0.0001828790815886944003, 0.0003657581631773888006 ),
 .UNSPECIFIED. ) ;
#7412=CARTESIAN_POINT ( 'NONE',  ( 1.254009781011257374, 12.44229282923036628, 7.789615163754328719 ) ) ;
#7413=CARTESIAN_POINT ( 'NONE',  ( 16.57210152137263393, -0.01453130299868521901, -0.0006600038696347544425 ) ) ;
#7415=CARTESIAN_POINT ( 'NONE',  ( 16.56822296793089322, -0.009385634690641594599, -0.003834730849370937035 ) ) ;
#7418=CARTESIAN_POINT ( 'NONE',  ( 0.4862570985993235340, -3.580942890621579444, -13.44146924561384537 ) ) ;
#7424=CARTESIAN_POINT ( 'NONE',  ( 1.847034903785822690, -11.90269060117936739, 3.625649561595261083 ) ) ;
#7425=ORIENTED_EDGE ( 'NONE', *, *, #1125, .T. ) ;
#7428=ORIENTED_EDGE ( 'NONE', *, *, #6341, .F. ) ;
#7445=DIRECTION ( 'NONE',  ( -0.7635533937278216055, 0.6453904417649387604, -0.02138673900302117195 ) ) ;
#7447=CARTESIAN_POINT ( 'NONE',  ( 0.3142011359265305948, -8.382042760265827397, -10.88514493056451471 ) ) ;
#7448=EDGE_LOOP ( 'NONE', ( #14016, #12356, #13851, #13700 ) ) ;
#7452=CARTESIAN_POINT ( 'NONE',  ( 3.950837973638677170, 13.10350451991849141, -6.316429227969337923 ) ) ;
#7455=CARTESIAN_POINT ( 'NONE',  ( 2.353870697619110608, -10.00946331859657334, -8.216087327473042379 ) ) ;
#7464=CARTESIAN_POINT ( 'NONE',  ( 2.636624412717099908, 14.46769361191384817, -6.973567714910368309 ) ) ;
#7465=( NAMED_UNIT ( * ) SI_UNIT ( $, .STERADIAN. ) SOLID_ANGLE_UNIT ( ) );
#7467=CARTESIAN_POINT ( 'NONE',  ( 16.56753206892534891, -0.006760771273035160941, 0.006669401563385170262 ) ) ;
#7470=CARTESIAN_POINT ( 'NONE',  ( 2.636624412714994037, -14.46769361191274328, -6.973567714907344950 ) ) ;
#7472=ORIENTED_EDGE ( 'NONE', *, *, #11876, .T. ) ;
#7473=CARTESIAN_POINT ( 'NONE',  ( 0.3150686449036038672, 7.951193823202562072, -11.20479228691389118 ) ) ;
#7476=VERTEX_POINT ( 'NONE', #4702 ) ;
#7487=ORIENTED_EDGE ( 'NONE', *, *, #16581, .F. ) ;
#7489=DIRECTION ( 'NONE',  ( 0.000000000000000000, 0.000000000000000000, 1.000000000000000000 ) ) ;
#7490=CARTESIAN_POINT ( 'NONE',  ( 2.636624412714236865, 0.000000000000000000, 0.000000000000000000 ) ) ;
#7494=ORIENTED_EDGE ( 'NONE', *, *, #625, .T. ) ;
#7495=CARTESIAN_POINT ( 'NONE',  ( 0.3137051932979757485, -7.698472063774552510, 11.37800749014128421 ) ) ;
#7498=ORIENTED_EDGE ( 'NONE', *, *, #404, .T. ) ;
#7504=EDGE_LOOP ( 'NONE', ( #7472, #17912, #4680, #10601 ) ) ;
#7508=CARTESIAN_POINT ( 'NONE',  ( 16.56872352241294521, 0.007240717549633888563, 0.007512283835804339609 ) ) ;
#7509=CARTESIAN_POINT ( 'NONE',  ( 1.254009781011254487, 14.64464726212552037, -1.011465182607978130 ) ) ;
#7514=CARTESIAN_POINT ( 'NONE',  ( 2.002547531651519996, 12.57989064830759496, -0.6781519942172177240 ) ) ;
#7518=CARTESIAN_POINT ( 'NONE',  ( 1.846138399168762989, 4.238866729160403857, 11.69739621335923729 ) ) ;
#7519=CARTESIAN_POINT ( 'NONE',  ( 16.56679352167444819, 0.008311568981097328460, -0.004162264567719685220 ) ) ;
#7522=CARTESIAN_POINT ( 'NONE',  ( 16.56753206892534891, 0.008432171035096382855, 0.004368917149004273269 ) ) ;
#7523=ORIENTED_EDGE ( 'NONE', *, *, #1778, .T. ) ;
#7528=EDGE_CURVE ( 'NONE', #2529, #1103, #957, .T. ) ;
#7529=DIRECTION ( 'NONE',  ( 0.000000000000000000, 0.000000000000000000, 1.000000000000000000 ) ) ;
#7536=B_SPLINE_CURVE_WITH_KNOTS ( 'NONE', 3,
 ( #5282, #13887, #804, #15145, #11038, #10948 ),
 .UNSPECIFIED., .F., .F.,
 ( 4, 2, 4 ),
 ( 0.000000000000000000, 0.001656992708822505175, 0.003313985417645010350 ),
 .UNSPECIFIED. ) ;
#7538=CARTESIAN_POINT ( 'NONE',  ( 3.074695600507531434, 11.23985886659412259, 10.75417554975680900 ) ) ;
#7540=ADVANCED_FACE ( 'NONE', ( #11195 ), #12056, .T. ) ;
#7542=CARTESIAN_POINT ( 'NONE',  ( 2.636624412715137922, -6.973567714907947135, 14.46769361191283920 ) ) ;
#7551=CARTESIAN_POINT ( 'NONE',  ( 1.918921323896210840, 9.738309537478938793, 7.860085869556105109 ) ) ;
#7555=CARTESIAN_POINT ( 'NONE',  ( 0.3939875929385635578, -11.57636969881029110, -7.545068896001335013 ) ) ;
#7557=CARTESIAN_POINT ( 'NONE',  ( 1.846138399168762989, 11.95493567637850774, 3.446241763653039580 ) ) ;
#7564=CARTESIAN_POINT ( 'NONE',  ( 0.3151930723728440520, 13.04315954105015152, 4.318364831037635021 ) ) ;
#7565=B_SPLINE_CURVE_WITH_KNOTS ( 'NONE', 3,
 ( #11410, #12740, #8268, #9961, #13991, #5385, #18295, #5292, #16955, #4044, #11320, #12553, #4142 ),
 .UNSPECIFIED., .F., .F.,
 ( 4, 3, 3, 3, 4 ),
 ( 2.168404344971008868E-18, 0.0002299780670421057124, 0.0004599561239687910961, 0.0006896788984287892561, 0.0009194956271626406052 ),
 .UNSPECIFIED. ) ;
#7568=CARTESIAN_POINT ( 'NONE',  ( 16.57778382496167424, 0.001819584982831895037, 0.01482878558584693578 ) ) ;
#7576=CARTESIAN_POINT ( 'NONE',  ( 1.977436885025838142, -14.12046670317529440, -6.153171729168441573 ) ) ;
#7577=CARTESIAN_POINT ( 'NONE',  ( 2.002547531651520885, 10.57595306287292480, 6.845637710436228929 ) ) ;
#7587=CARTESIAN_POINT ( 'NONE',  ( 16.56872352241294521, -0.01033355228142402750, 0.001442253899401767583 ) ) ;
#7589=CARTESIAN_POINT ( 'NONE',  ( 0.3307726912345213544, -10.76786801061213161, 8.558645027434234720 ) ) ;
#7596=CARTESIAN_POINT ( 'NONE',  ( 16.56822296793089322, -0.006547366384935564970, 0.007741272030791060237 ) ) ;
#7597=CARTESIAN_POINT ( 'NONE',  ( 0.3137051932979792457, 11.37800749014131263, 7.698472063774513430 ) ) ;
#7600=CARTESIAN_POINT ( 'NONE',  ( 16.57778382496167424, 0.01092721432668994352, 0.01018821665058780926 ) ) ;
#7604=ORIENTED_EDGE ( 'NONE', *, *, #434, .T. ) ;
#7611=CARTESIAN_POINT ( 'NONE',  ( 8.522092701127531811, -5.397361180353110299, -4.388629235579637466 ) ) ;
#7612=B_SPLINE_CURVE_WITH_KNOTS ( 'NONE', 3,
 ( #18839, #5827, #7001, #11672 ),
 .UNSPECIFIED., .F., .F.,
 ( 4, 4 ),
 ( 0.000000000000000000, 0.002004993803842712932 ),
 .UNSPECIFIED. ) ;
#7614=LINE ( 'NONE', #2065, #6282 ) ;
#7615=B_SPLINE_CURVE_WITH_KNOTS ( 'NONE', 3,
 ( #10863, #16686, #3388, #3587, #545, #15245 ),
 .UNSPECIFIED., .F., .F.,
 ( 4, 2, 4 ),
 ( 1.084202172485504434E-19, 0.0002017457492448070664, 0.0004034914984896140243 ),
 .UNSPECIFIED. ) ;
#7617=CARTESIAN_POINT ( 'NONE',  ( 0.4754618798421167414, -8.775436892861188554, 10.80499583390510132 ) ) ;
#7622=CARTESIAN_POINT ( 'NONE',  ( 1.846955891736117072, -11.74973605926567188, 4.094751675596655538 ) ) ;
#7627=ORIENTED_EDGE ( 'NONE', *, *, #11637, .T. ) ;
#7628=ORIENTED_EDGE ( 'NONE', *, *, #13219, .T. ) ;
#7636=CARTESIAN_POINT ( 'NONE',  ( 0.3058872367615226295, 0.6080468242582872662, -13.72992299905059177 ) ) ;
#7638=CARTESIAN_POINT ( 'NONE',  ( 1.847247051441591514, 12.44188156437794390, 0.1676840720645733362 ) ) ;
#7642=CARTESIAN_POINT ( 'NONE',  ( 16.56822296793089322, 0.002414375228568836022, 0.009847136207495320662 ) ) ;
#7643=EDGE_CURVE ( 'NONE', #16490, #4199, #13760, .T. ) ;
#7648=ORIENTED_EDGE ( 'NONE', *, *, #7117, .T. ) ;
#7650=B_SPLINE_CURVE_WITH_KNOTS ( 'NONE', 3,
 ( #10717, #16820, #5154, #6417, #15006, #3722 ),
 .UNSPECIFIED., .F., .F.,
 ( 4, 2, 4 ),
 ( 4.878909776184769953E-19, 0.001657017934711441055, 0.003314035869422881676 ),
 .UNSPECIFIED. ) ;
#7651=EDGE_LOOP ( 'NONE', ( #7116, #14089, #8920, #6676 ) ) ;
#7652=DIRECTION ( 'NONE',  ( 0.000000000000000000, 0.000000000000000000, 1.000000000000000000 ) ) ;
#7653=CARTESIAN_POINT ( 'NONE',  ( 16.56872352241294521, 0.001442253899401220278, -0.01033355228142500415 ) ) ;
#7655=CARTESIAN_POINT ( 'NONE',  ( 2.697797270744671128, 10.19107313879056953, 8.537712152180894520 ) ) ;
#7657=ORIENTED_EDGE ( 'NONE', *, *, #14202, .F. ) ;
#7661=CARTESIAN_POINT ( 'NONE',  ( 0.3137051932979775248, -0.4596302728638797519, -13.73004976592202553 ) ) ;
#7663=FILL_AREA_STYLE ('',( #14907 ) ) ;
#7669=DIRECTION ( 'NONE',  ( 0.7635533937278216055, 0.6071939193889560604, 0.2197766120036526161 ) ) ;
#7670=VERTEX_POINT ( 'NONE', #5707 ) ;
#7677=EDGE_LOOP ( 'NONE', ( #3193, #7384, #18364, #9362 ) ) ;
#7681=FACE_OUTER_BOUND ( 'NONE', #15058, .T. ) ;
#7684=EDGE_LOOP ( 'NONE', ( #1956, #8939, #775, #2181 ) ) ;
#7686=CARTESIAN_POINT ( 'NONE',  ( 2.002547531651519996, 12.17374746633578475, 3.242439124566693476 ) ) ;
#7691=ORIENTED_EDGE ( 'NONE', *, *, #18650, .F. ) ;
#7692=CARTESIAN_POINT ( 'NONE',  ( 0.4862570985993235340, -13.89016912371016943, -0.7479633556563904939 ) ) ;
#7694=CARTESIAN_POINT ( 'NONE',  ( 0.3145734862173260038, -4.535879238195024143, 12.96846406299304988 ) ) ;
#7697=VERTEX_POINT ( 'NONE', #11941 ) ;
#7698=AXIS2_PLACEMENT_3D ( 'NONE', #14253, #9752, #9666 ) ;
#7703=EDGE_CURVE ( 'NONE', #12288, #17352, #956, .T. ) ;
#7707=CARTESIAN_POINT ( 'NONE',  ( 0.3151930723728439410, 4.172946285306569969, 13.09040889075571990 ) ) ;
#7710=CARTESIAN_POINT ( 'NONE',  ( 16.58200780006414732, 0.01080144354108992025, -0.002844973367390922145 ) ) ;
#7712=FACE_OUTER_BOUND ( 'NONE', #9976, .T. ) ;
#7713=CARTESIAN_POINT ( 'NONE',  ( 2.320520222539219635, -3.126729907238178896, -15.43440824796753930 ) ) ;
#7714=CARTESIAN_POINT ( 'NONE',  ( 0.3142014840576498047, 7.762239086932858356, 11.33546131209465102 ) ) ;
#7716=CARTESIAN_POINT ( 'NONE',  ( 1.847247051441591514, -11.88474976472815214, 3.685275815977142599 ) ) ;
#7717=CARTESIAN_POINT ( 'NONE',  ( 0.3137051932979792457, 0.4596302728641686874, -13.73004976592201487 ) ) ;
#7720=EDGE_LOOP ( 'NONE', ( #13264, #11664, #14159, #15234 ) ) ;
#7721=ORIENTED_EDGE ( 'NONE', *, *, #15101, .T. ) ;
#7723=ADVANCED_FACE ( 'NONE', ( #89 ), #5386, .F. ) ;
#7725=CARTESIAN_POINT ( 'NONE',  ( 1.846138399168762101, -12.43476674860266940, 0.4167076046095114505 ) ) ;
#7727=CARTESIAN_POINT ( 'NONE',  ( 3.512766787570769544, 10.87507422923904166, -10.40533104696121214 ) ) ;
#7730=CARTESIAN_POINT ( 'NONE',  ( 3.950837973638668288, 0.000000000000000000, 0.000000000000000000 ) ) ;
#7733=CARTESIAN_POINT ( 'NONE',  ( 2.320521194581858460, 15.43440938316986610, 3.126729093672275805 ) ) ;
#7734=CARTESIAN_POINT ( 'NONE',  ( 0.3095370825347224519, 0.4597470195090193057, 13.73357284481724960 ) ) ;
#7750=ORIENTED_EDGE ( 'NONE', *, *, #14203, .F. ) ;
#7755=CARTESIAN_POINT ( 'NONE',  ( 1.847034903785822468, -10.19974412751570014, 7.126331315909236075 ) ) ;
#7756=( BOUNDED_SURFACE ( )  B_SPLINE_SURFACE ( 3, 1, ( 
 ( #18111, #5013 ),
 ( #15242, #16683 ),
 ( #2156, #2499 ),
 ( #6918, #987 ) ),
 .UNSPECIFIED., .F., .F., .T. ) 
 B_SPLINE_SURFACE_WITH_KNOTS ( ( 4, 4 ),
 ( 2, 2 ),
 ( 0.000000000000000000, 1.000000000000000000 ),
 ( 0.000000000000000000, 1.000000000000000000 ),
 .UNSPECIFIED. ) 
 GEOMETRIC_REPRESENTATION_ITEM ( )  RATIONAL_B_SPLINE_SURFACE ( (
 ( 1.000000000000000000, 1.000000000000000000),
 ( 0.9933953342250438912, 0.8357391271907739227),
 ( 0.9933953342250438912, 0.8357391271907739227),
 ( 1.000000000000000000, 1.000000000000000000) ) ) 
 REPRESENTATION_ITEM ( '' )  SURFACE ( )  );
#7758=CARTESIAN_POINT ( 'NONE',  ( 8.438534575730034959, 0.2320579683290127926, 6.862570336891076650 ) ) ;
#7761=CARTESIAN_POINT ( 'NONE',  ( 2.320521194582656044, -11.60169518685945356, 10.64885423995117542 ) ) ;
#7762=CARTESIAN_POINT ( 'NONE',  ( 1.562796894703937678, 0.000000000000000000, 2.500000000000000000 ) ) ;
#7763=ORIENTED_EDGE ( 'NONE', *, *, #1125, .F. ) ;
#7764=CARTESIAN_POINT ( 'NONE',  ( 3.950837973638676281, -14.41405733518061716, 1.958075594453740687 ) ) ;
#7765=CARTESIAN_POINT ( 'NONE',  ( 0.3939875929385612263, 10.75308190953755982, -8.678227324501007089 ) ) ;
#7770=CARTESIAN_POINT ( 'NONE',  ( 2.123976203522053741, 7.899625852120402136, -13.47898556379304580 ) ) ;
#7771=CARTESIAN_POINT ( 'NONE',  ( 16.56872352241294521, -0.007240717549633941472, -0.007512283835804289302 ) ) ;
#7773=CARTESIAN_POINT ( 'NONE',  ( 0.4384471787762838635, -10.76632603192792459, 8.732395932355645485 ) ) ;
#7774=CARTESIAN_POINT ( 'NONE',  ( 1.847372867223022519, 10.12831093686732586, -7.228345833872643844 ) ) ;
#7775=CONICAL_SURFACE ( 'NONE', #17509, 14.54644660717763927, 0.8559913436420816257 ) ;
#7777=ORIENTED_EDGE ( 'NONE', *, *, #17094, .F. ) ;
#7778=ORIENTED_EDGE ( 'NONE', *, *, #3886, .F. ) ;
#7782=CARTESIAN_POINT ( 'NONE',  ( 1.846138399168762101, 10.30487220521580305, -6.971848976710897539 ) ) ;
#7784=FACE_OUTER_BOUND ( 'NONE', #13289, .T. ) ;
#7786=CARTESIAN_POINT ( 'NONE',  ( 16.56872352241294521, 0.01033355228142401709, -0.001442253899401843694 ) ) ;
#7787=( BOUNDED_SURFACE ( )  B_SPLINE_SURFACE ( 3, 1, ( 
 ( #7245, #9804 ),
 ( #15634, #2536 ),
 ( #14217, #1113 ),
 ( #6965, #12776 ) ),
 .UNSPECIFIED., .F., .F., .T. ) 
 B_SPLINE_SURFACE_WITH_KNOTS ( ( 4, 4 ),
 ( 2, 2 ),
 ( 0.000000000000000000, 1.000000000000000000 ),
 ( 0.000000000000000000, 1.000000000000000000 ),
 .UNSPECIFIED. ) 
 GEOMETRIC_REPRESENTATION_ITEM ( )  RATIONAL_B_SPLINE_SURFACE ( (
 ( 1.000000000000000000, 1.000000000000000000),
 ( 0.9933953342250436691, 0.8357391271907733676),
 ( 0.9933953342250436691, 0.8357391271907733676),
 ( 1.000000000000000000, 1.000000000000000000) ) ) 
 REPRESENTATION_ITEM ( '' )  SURFACE ( )  );
#7788=CARTESIAN_POINT ( 'NONE',  ( 2.320520222537495680, -11.60169517779343096, -10.64885284335084847 ) ) ;
#7798=CIRCLE ( 'NONE', #17545, 16.06066017081991149 ) ;
#7800=B_SPLINE_CURVE_WITH_KNOTS ( 'NONE', 3,
 ( #11013, #11105, #9562, #6796, #15119, #15393 ),
 .UNSPECIFIED., .F., .F.,
 ( 4, 2, 4 ),
 ( 1.946286347258496500E-18, 0.0002017457492448080964, 0.0004034914984896142412 ),
 .UNSPECIFIED. ) ;
#7801=CARTESIAN_POINT ( 'NONE',  ( 0.4384471787762834749, 13.84291427302851574, -0.7363690479466810102 ) ) ;
#7802=CARTESIAN_POINT ( 'NONE',  ( 0.3137051932979757485, -7.698472063774552510, 11.37800749014128421 ) ) ;
#7803=B_SPLINE_CURVE_WITH_KNOTS ( 'NONE', 3,
 ( #16304, #17446, #11807, #5769, #2799, #7518 ),
 .UNSPECIFIED., .F., .F.,
 ( 4, 2, 4 ),
 ( 3.332294980281255979E-17, 0.0001825746017570583984, 0.0003651492035140835118 ),
 .UNSPECIFIED. ) ;
#7807=CARTESIAN_POINT ( 'NONE',  ( 0.4862570985993235340, 0.7479633556564388996, -13.89016912371016765 ) ) ;
#7810=CARTESIAN_POINT ( 'NONE',  ( 1.847372867223025183, 7.398914411685134418, -10.00438561114516034 ) ) ;
#7811=VECTOR ( 'NONE', #4773, 1000.000000000000227 ) ;
#7812=LINE ( 'NONE', #16774, #9376 ) ;
#7813=EDGE_CURVE ( 'NONE', #18612, #16214, #7119, .T. ) ;
#7815=LINE ( 'NONE', #5116, #5099 ) ;
#7817=VERTEX_POINT ( 'NONE', #16719 ) ;
#7824=CARTESIAN_POINT ( 'NONE',  ( 1.847247051441592403, -12.44188156437794035, -0.1676840720646602112 ) ) ;
#7825=CARTESIAN_POINT ( 'NONE',  ( 3.664313757352960721, 14.16986885736091750, 1.627055439596312159 ) ) ;
#7826=CARTESIAN_POINT ( 'NONE',  ( 3.950837973638676281, -6.888253895133199300, -12.81214529934982949 ) ) ;
#7833=CARTESIAN_POINT ( 'NONE',  ( 2.123976203522053297, -15.26039569100261950, 3.347755036805843076 ) ) ;
#7838=VECTOR ( 'NONE', #18284, 1000.000000000000000 ) ;
#7842=CARTESIAN_POINT ( 'NONE',  ( 1.846955891736119293, 3.593597880662512623, -11.91257079808164576 ) ) ;
#7853=CARTESIAN_POINT ( 'NONE',  ( 3.512766787570921867, 14.81029789862138912, 2.682019731918403593 ) ) ;
#7857=ORIENTED_EDGE ( 'NONE', *, *, #10761, .F. ) ;
#7859=CARTESIAN_POINT ( 'NONE',  ( 2.320520222537155064, -14.32454429810361951, -6.542539914240126819 ) ) ;
#7860=CARTESIAN_POINT ( 'NONE',  ( 1.846138399168762101, 11.95493567637855392, -3.446241763652874379 ) ) ;
#7872=ORIENTED_EDGE ( 'NONE', *, *, #11705, .F. ) ;
#7873=CARTESIAN_POINT ( 'NONE',  ( 2.747332970342022840, 7.555624153089857131, -14.49942876448584173 ) ) ;
#7876=CARTESIAN_POINT ( 'NONE',  ( 0.8740779401508861346, -14.27348745891575987, 0.8420120399581260129 ) ) ;
#7882=EDGE_CURVE ( 'NONE', #6956, #9697, #5958, .T. ) ;
#7884=ADVANCED_FACE ( 'NONE', ( #8478 ), #2115, .F. ) ;
#7894=ORIENTED_EDGE ( 'NONE', *, *, #2025, .T. ) ;
#7904=AXIS2_PLACEMENT_3D ( 'NONE', #14860, #18871, #14473 ) ;
#7905=CARTESIAN_POINT ( 'NONE',  ( 0.3308579732647025096, 12.88563776947746398, 4.812490080619245880 ) ) ;
#7907=CARTESIAN_POINT ( 'NONE',  ( 2.002547531651519996, -6.845637710436264456, 10.57595306287289638 ) ) ;
#7909=( BOUNDED_SURFACE ( )  B_SPLINE_SURFACE ( 3, 1, ( 
 ( #14950, #16197 ),
 ( #431, #1483 ),
 ( #6261, #14566 ),
 ( #7319, #40 ) ),
 .UNSPECIFIED., .F., .F., .T. ) 
 B_SPLINE_SURFACE_WITH_KNOTS ( ( 4, 4 ),
 ( 2, 2 ),
 ( 0.000000000000000000, 1.000000000000000000 ),
 ( 0.000000000000000000, 1.000000000000000000 ),
 .UNSPECIFIED. ) 
 GEOMETRIC_REPRESENTATION_ITEM ( )  RATIONAL_B_SPLINE_SURFACE ( (
 ( 1.000000000000000000, 1.000000000000000000),
 ( 0.7792777138730160313, 0.9689936506012927220),
 ( 0.7792777138730160313, 0.9689936506012927220),
 ( 1.000000000000000000, 1.000000000000000000) ) ) 
 REPRESENTATION_ITEM ( '' )  SURFACE ( )  );
#7912=EDGE_CURVE ( 'NONE', #12351, #12889, #16476, .T. ) ;
#7915=VERTEX_POINT ( 'NONE', #5500 ) ;
#7922=CARTESIAN_POINT ( 'NONE',  ( 1.959283090834839314, 9.750336807931262229, -7.909254450748897547 ) ) ;
#7923=EDGE_CURVE ( 'NONE', #7190, #4602, #8471, .T. ) ;
#7925=CARTESIAN_POINT ( 'NONE',  ( 2.320520222538070776, 1.795797593769018485, -15.64520721754711730 ) ) ;
#7927=CARTESIAN_POINT ( 'NONE',  ( 8.438534575730034959, 6.862570336891075762, 0.2320579683290369954 ) ) ;
#7929=ADVANCED_FACE ( 'NONE', ( #18597 ), #7355, .F. ) ;
#7935=ORIENTED_EDGE ( 'NONE', *, *, #6491, .F. ) ;
#7938=CARTESIAN_POINT ( 'NONE',  ( 8.438534575730034959, -3.845978796785994192, -5.688336279099088344 ) ) ;
#7939=CARTESIAN_POINT ( 'NONE',  ( 2.002547531651519996, -0.6781519942172617998, 12.57989064830759318 ) ) ;
#7940=CARTESIAN_POINT ( 'NONE',  ( 1.847412631396502913, -7.278870946904175909, -10.09191835241971269 ) ) ;
#7946=CARTESIAN_POINT ( 'NONE',  ( 1.845755665166725068, -0.4784952423729416648, 12.43231320373360838 ) ) ;
#7947=B_SPLINE_CURVE_WITH_KNOTS ( 'NONE', 3,
 ( #3803, #15553, #1021, #10993, #12501, #17086, #18247, #14115, #6863, #668, #8214, #3990, #5330 ),
 .UNSPECIFIED., .F., .F.,
 ( 4, 3, 3, 3, 4 ),
 ( 1.734723475976807094E-18, 0.0002299804304191480130, 0.0004599608082120234913, 0.0006467586077648008244, 0.0008336169836825994828 ),
 .UNSPECIFIED. ) ;
#7953=DIRECTION ( 'NONE',  ( -1.000000000000000000, -0.000000000000000000, -0.000000000000000000 ) ) ;
#7956=CARTESIAN_POINT ( 'NONE',  ( 0.4862570985993235340, 0.7479633556564388996, -13.89016912371016765 ) ) ;
#7957=ORIENTED_EDGE ( 'NONE', *, *, #9685, .T. ) ;
#7962=CARTESIAN_POINT ( 'NONE',  ( 3.664313757352976708, 5.926151963190554817, -12.97355833021534011 ) ) ;
#7968=CARTESIAN_POINT ( 'NONE',  ( 0.4862570985993235340, -8.769551628660655851, -10.79774104611382946 ) ) ;
#7969=CARTESIAN_POINT ( 'NONE',  ( 2.002547531651519996, 7.942910686618173344, 9.778737580845726640 ) ) ;
#7971=CARTESIAN_POINT ( 'NONE',  ( 0.3137051932979792457, 11.37800749014142276, -7.698472063774345564 ) ) ;
#7973=CARTESIAN_POINT ( 'NONE',  ( 1.845755665166725068, 10.33920510797153369, -6.920419570228236950 ) ) ;
#7989=VECTOR ( 'NONE', #3505, 1000.000000000000227 ) ;
#7992=CARTESIAN_POINT ( 'NONE',  ( 0.3132635586635976188, -7.641727604903970850, 11.41586812343486912 ) ) ;
#7993=CARTESIAN_POINT ( 'NONE',  ( 0.3095370825347234511, -3.806662003783320980, -13.20347358821918426 ) ) ;
#7997=CARTESIAN_POINT ( 'NONE',  ( 0.4754618798421162973, -12.98792082933648118, 5.007009103465200894 ) ) ;
#8001=CARTESIAN_POINT ( 'NONE',  ( 16.58200780006414732, -0.01041078477703985539, 0.004047297414157853025 ) ) ;
#8013=CARTESIAN_POINT ( 'NONE',  ( 3.950837973638675393, -14.31366178983251380, -2.591948120961955926 ) ) ;
#8016=CARTESIAN_POINT ( 'NONE',  ( 3.950837973638675393, 2.591948120961804936, 14.31366178983254578 ) ) ;
#8019=B_SPLINE_CURVE_WITH_KNOTS ( 'NONE', 3,
 ( #18774, #5488, #15815, #15531 ),
 .UNSPECIFIED., .F., .F.,
 ( 4, 4 ),
 ( 1.811104479740059440E-17, 0.003005512676784850932 ),
 .UNSPECIFIED. ) ;
#8021=VERTEX_POINT ( 'NONE', #2722 ) ;
#8022=ORIENTED_EDGE ( 'NONE', *, *, #5472, .F. ) ;
#8034=ADVANCED_FACE ( 'NONE', ( #4560 ), #9301, .F. ) ;
#8041=ORIENTED_EDGE ( 'NONE', *, *, #12824, .F. ) ;
#8043=CARTESIAN_POINT ( 'NONE',  ( 1.847247051441592625, 11.88474976472817701, -3.685275815977066216 ) ) ;
#8045=CARTESIAN_POINT ( 'NONE',  ( 16.56822296793089322, 0.0007467251401288622394, -0.01011126603341004279 ) ) ;
#8049=CARTESIAN_POINT ( 'NONE',  ( 0.3095370825347233956, 11.38092634279628967, 7.700448427571912724 ) ) ;
#8052=ORIENTED_EDGE ( 'NONE', *, *, #13261, .T. ) ;
#8054=DIRECTION ( 'NONE',  ( 0.000000000000000000, 0.000000000000000000, 1.000000000000000000 ) ) ;
#8055=CARTESIAN_POINT ( 'NONE',  ( 0.4862570985993235340, -13.89016912371018186, 0.7479633556561964269 ) ) ;
#8058=VECTOR ( 'NONE', #18724, 1000.000000000000114 ) ;
#8059=EDGE_CURVE ( 'NONE', #2148, #1614, #8938, .T. ) ;
#8080=CARTESIAN_POINT ( 'NONE',  ( 16.56872352241294521, -0.004907101719994693724, 0.009207754980063731845 ) ) ;
#8081=CARTESIAN_POINT ( 'NONE',  ( 2.636624412717099908, 11.60464335004051861, -11.10302021258208249 ) ) ;
#8082=( BOUNDED_SURFACE ( )  B_SPLINE_SURFACE ( 3, 1, ( 
 ( #6629, #16936 ),
 ( #8158, #10741 ),
 ( #13973, #15498 ),
 ( #2141, #18280 ) ),
 .UNSPECIFIED., .F., .F., .T. ) 
 B_SPLINE_SURFACE_WITH_KNOTS ( ( 4, 4 ),
 ( 2, 2 ),
 ( 0.000000000000000000, 1.000000000000000000 ),
 ( 0.000000000000000000, 1.000000000000000000 ),
 .UNSPECIFIED. ) 
 GEOMETRIC_REPRESENTATION_ITEM ( )  RATIONAL_B_SPLINE_SURFACE ( (
 ( 1.000000000000000000, 1.000000000000000000),
 ( 0.7792777138730158093, 0.9689936506012928330),
 ( 0.7792777138730158093, 0.9689936506012928330),
 ( 1.000000000000000000, 1.000000000000000000) ) ) 
 REPRESENTATION_ITEM ( '' )  SURFACE ( )  );
#8086=EDGE_CURVE ( 'NONE', #15500, #5687, #6880, .T. ) ;
#8092=VERTEX_POINT ( 'NONE', #1981 ) ;
#8093=B_SPLINE_CURVE_WITH_KNOTS ( 'NONE', 3,
 ( #4370, #18890, #2640, #1212, #5597, #11545, #7057, #5790, #11636, #10003, #2818, #17364, #4280 ),
 .UNSPECIFIED., .F., .F.,
 ( 4, 3, 3, 3, 4 ),
 ( 3.878959614448864246E-18, 0.0002299780670421063358, 0.0004599561239687880061, 0.0006896788984287903403, 0.0009194956271626402800 ),
 .UNSPECIFIED. ) ;
#8095=VERTEX_POINT ( 'NONE', #16420 ) ;
#8096=CARTESIAN_POINT ( 'NONE',  ( 0.4384471787762818096, 0.7363690479466327155, 13.84291427302852462 ) ) ;
#8100=LINE ( 'NONE', #646, #1369 ) ;
#8103=B_SPLINE_CURVE_WITH_KNOTS ( 'NONE', 3,
 ( #17669, #14976, #16328, #11832, #12124, #13160, #4759, #17562, #12023, #4372 ),
 .UNSPECIFIED., .F., .F.,
 ( 4, 3, 3, 4 ),
 ( 0.0004168119862248656667, 0.0004599608082120252802, 0.0006467586077648016917, 0.0008336169836825988323 ),
 .UNSPECIFIED. ) ;
#8105=CARTESIAN_POINT ( 'NONE',  ( 0.3095370825347233956, 10.84046130709070610, -8.444334731363889901 ) ) ;
#8110=ORIENTED_EDGE ( 'NONE', *, *, #13914, .T. ) ;
#8112=ORIENTED_EDGE ( 'NONE', *, *, #18263, .T. ) ;
#8113=ORIENTED_EDGE ( 'NONE', *, *, #17820, .F. ) ;
#8120=CARTESIAN_POINT ( 'NONE',  ( 16.56822296793089322, 0.005339139727952666586, -0.008619100080559792543 ) ) ;
#8121=CARTESIAN_POINT ( 'NONE',  ( 1.846138399168762101, 12.43476674860266584, 0.4167076046095977149 ) ) ;
#8122=CARTESIAN_POINT ( 'NONE',  ( 16.56872352241294521, -0.001821578298044716857, -0.01027347319884440967 ) ) ;
#8125=CARTESIAN_POINT ( 'NONE',  ( 0.3939822652208137543, 11.57634296752778802, -7.545099438011897419 ) ) ;
#8127=CARTESIAN_POINT ( 'NONE',  ( 2.320520222538102306, -7.743191299716920106, -13.71278186123380927 ) ) ;
#8133=EDGE_LOOP ( 'NONE', ( #15633, #17277 ) ) ;
#8134=VERTEX_POINT ( 'NONE', #555 ) ;
#8139=CARTESIAN_POINT ( 'NONE',  ( 1.846822687350019310, -3.566003975885607691, -11.92063725419902731 ) ) ;
#8150=CARTESIAN_POINT ( 'NONE',  ( 1.254009781011991898, 3.563484327698415388, -14.24044713813362151 ) ) ;
#8158=CARTESIAN_POINT ( 'NONE',  ( 16.57778382496167424, -0.01482878558584568157, -0.001819584982832054632 ) ) ;
#8159=CARTESIAN_POINT ( 'NONE',  ( 0.3142014840576518586, -3.879477880151352753, -13.17932813834298678 ) ) ;
#8160=ORIENTED_EDGE ( 'NONE', *, *, #7882, .F. ) ;
#8162=CARTESIAN_POINT ( 'NONE',  ( 2.636624412715137922, 2.161493821597615828, 15.91454522070216093 ) ) ;
#8164=FACE_OUTER_BOUND ( 'NONE', #12701, .T. ) ;
#8172=CARTESIAN_POINT ( 'NONE',  ( 1.861628059977341598, 12.44564375541077617, 0.5393144007390715533 ) ) ;
#8181=CARTESIAN_POINT ( 'NONE',  ( 16.56753206892534891, 0.006760771273035115839, -0.006669401563385219701 ) ) ;
#8184=ORIENTED_EDGE ( 'NONE', *, *, #10894, .T. ) ;
#8189=EDGE_CURVE ( 'NONE', #16119, #13313, #1428, .T. ) ;
#8193=CARTESIAN_POINT ( 'NONE',  ( 1.845755665166725068, 6.920419570228353301, 10.33920510797145909 ) ) ;
#8198=CARTESIAN_POINT ( 'NONE',  ( 0.4754618798421167414, -13.45049478164062329, 3.583352865732619463 ) ) ;
#8202=ORIENTED_EDGE ( 'NONE', *, *, #13309, .T. ) ;
#8204=CARTESIAN_POINT ( 'NONE',  ( 2.636624412714236865, 15.91454522070173638, 2.161493821596668585 ) ) ;
#8205=B_SPLINE_CURVE_WITH_KNOTS ( 'NONE', 3,
 ( #5260, #16831, #16925, #3736, #4986, #15486, #9563, #7774, #9286, #15394, #3832, #6714, #4015 ),
 .UNSPECIFIED., .F., .F.,
 ( 4, 3, 3, 3, 4 ),
 ( 3.127317220692750759E-18, 0.0002299804304191474438, 0.0004599608082120254971, 0.0006467586077648028843, 0.0008336169836825993744 ),
 .UNSPECIFIED. ) ;
#8213=EDGE_CURVE ( 'NONE', #5002, #11053, #12368, .T. ) ;
#8214=CARTESIAN_POINT ( 'NONE',  ( 1.846822687350021974, -11.74004266906801774, -4.121816957446323038 ) ) ;
#8227=CARTESIAN_POINT ( 'NONE',  ( 3.950837973638675393, -10.51028938476224894, 10.05648675950122595 ) ) ;
#8230=ORIENTED_EDGE ( 'NONE', *, *, #2079, .F. ) ;
#8231=CARTESIAN_POINT ( 'NONE',  ( 1.847034903785823134, -3.625649561595226888, -11.90269060117937627 ) ) ;
#8232=B_SPLINE_CURVE_WITH_KNOTS ( 'NONE', 3,
 ( #13802, #4837, #16684, #6456 ),
 .UNSPECIFIED., .F., .F.,
 ( 4, 4 ),
 ( 0.000000000000000000, 0.002004993803842881200 ),
 .UNSPECIFIED. ) ;
#8235=CARTESIAN_POINT ( 'NONE',  ( 3.353306896162453477, 9.252610477110421172, -10.44017738170046528 ) ) ;
#8237=LINE ( 'NONE', #14056, #11284 ) ;
#8238=CARTESIAN_POINT ( 'NONE',  ( 1.959283090834841090, -12.12982544407802799, -3.239245055717093091 ) ) ;
#8239=CARTESIAN_POINT ( 'NONE',  ( 0.3145734862173260038, -12.96846406299303212, -4.535879238195068552 ) ) ;
#8240=CARTESIAN_POINT ( 'NONE',  ( 0.3150690434770172521, -0.1531837610934980720, 13.73846430619029491 ) ) ;
#8242=AXIS2_PLACEMENT_3D ( 'NONE', #6705, #17017, #16739 ) ;
#8246=CARTESIAN_POINT ( 'NONE',  ( 2.002547531651519996, 9.778737580845815458, -7.942910686618064986 ) ) ;
#8247=DIRECTION ( 'NONE',  ( -1.000000000000000000, -0.000000000000000000, -0.000000000000000000 ) ) ;
#8248=ORIENTED_EDGE ( 'NONE', *, *, #13337, .T. ) ;
#8250=ADVANCED_FACE ( 'NONE', ( #4492 ), #15876, .F. ) ;
#8251=CARTESIAN_POINT ( 'NONE',  ( 0.3142014840576500267, -10.88517824918537080, -8.382000553815572630 ) ) ;
#8252=CARTESIAN_POINT ( 'NONE',  ( 0.3151930723728477157, -4.172946285306481151, -13.09040889075574476 ) ) ;
#8254=ORIENTED_EDGE ( 'NONE', *, *, #10930, .T. ) ;
#8258=CARTESIAN_POINT ( 'NONE',  ( 1.846138399168762101, -0.4167076046094680408, -12.43476674860266940 ) ) ;
#8263=EDGE_CURVE ( 'NONE', #8687, #9475, #10122, .T. ) ;
#8264=EDGE_CURVE ( 'NONE', #12585, #11870, #9612, .T. ) ;
#8268=CARTESIAN_POINT ( 'NONE',  ( 0.3145734862173208413, -13.15783074029281963, 3.953068532979947314 ) ) ;
#8272=FACE_OUTER_BOUND ( 'NONE', #18568, .T. ) ;
#8273=ORIENTED_EDGE ( 'NONE', *, *, #16139, .F. ) ;
#8276=ORIENTED_EDGE ( 'NONE', *, *, #1004, .T. ) ;
#8281=CARTESIAN_POINT ( 'NONE',  ( 1.342453679581834924, 7.902645620902447376, 12.51077660954468662 ) ) ;
#8283=CARTESIAN_POINT ( 'NONE',  ( 0.4384471787762828088, -12.93784327393176881, 4.978024343488995918 ) ) ;
#8295=CARTESIAN_POINT ( 'NONE',  ( 16.56872352241294521, -0.01033355228142500762, -0.001442253899401184716 ) ) ;
#8298=CARTESIAN_POINT ( 'NONE',  ( 2.320521194581854463, 13.71278319227944920, 7.743190876766304243 ) ) ;
#8301=CARTESIAN_POINT ( 'NONE',  ( 3.950837973638676281, 2.591948120962007884, -14.31366178983250670 ) ) ;
#8303=CARTESIAN_POINT ( 'NONE',  ( 1.342453679581834924, -3.649820028552833051, 14.34050741580205823 ) ) ;
#8305=CARTESIAN_POINT ( 'NONE',  ( 16.57210152137263393, 0.003862718596009277316, 0.01402404281922923004 ) ) ;
#8307=CARTESIAN_POINT ( 'NONE',  ( 0.4384471787762814765, 4.978024343489044767, 12.93784327393174571 ) ) ;
#8309=ORIENTED_EDGE ( 'NONE', *, *, #8671, .F. ) ;
#8313=ORIENTED_EDGE ( 'NONE', *, *, #8834, .F. ) ;
#8314=EDGE_CURVE ( 'NONE', #5315, #306, #12040, .T. ) ;
#8320=CARTESIAN_POINT ( 'NONE',  ( 2.705023505549863039, 13.27418276223636084, -0.8488853074253436271 ) ) ;
#8321=B_SPLINE_CURVE_WITH_KNOTS ( 'NONE', 3,
 ( #3709, #18243, #16989, #6401, #663, #10797 ),
 .UNSPECIFIED., .F., .F.,
 ( 4, 2, 4 ),
 ( 8.673617379884035472E-19, 0.001500839035891552223, 0.003001678071783103578 ),
 .UNSPECIFIED. ) ;
#8325=CARTESIAN_POINT ( 'NONE',  ( 2.002547531651519996, 7.942910686618313676, -9.778737580845612953 ) ) ;
#8327=DIRECTION ( 'NONE',  ( -1.000000000000000000, -0.000000000000000000, -0.000000000000000000 ) ) ;
#8328=CARTESIAN_POINT ( 'NONE',  ( 0.3145729642390373559, -13.15786090015081555, -3.952965287571249764 ) ) ;
#8331=B_SPLINE_CURVE_WITH_KNOTS ( 'NONE', 3,
 ( #9318, #15147, #432, #7905, #16401, #4732 ),
 .UNSPECIFIED., .F., .F.,
 ( 4, 2, 4 ),
 ( 4.016409351050315258E-17, 0.0002014099069817277545, 0.0004028198139634153394 ),
 .UNSPECIFIED. ) ;
#8332=SURFACE_STYLE_FILL_AREA ( #1050 ) ;
#8339=CARTESIAN_POINT ( 'NONE',  ( 0.3150692679895970572, -4.099798979280757649, -13.11337225490256664 ) ) ;
#8343=CARTESIAN_POINT ( 'NONE',  ( 16.57210152137263393, -0.003862718596009374894, -0.01402404281922920576 ) ) ;
#8348=CARTESIAN_POINT ( 'NONE',  ( 1.846613052777651198, -9.862487290071051405, 7.585914669018136713 ) ) ;
#8349=EDGE_CURVE ( 'NONE', #17715, #11214, #17874, .T. ) ;
#8352=( BOUNDED_SURFACE ( )  B_SPLINE_SURFACE ( 3, 1, ( 
 ( #7522, #17276 ),
 ( #13339, #12878 ),
 ( #15845, #3190 ),
 ( #346, #17646 ) ),
 .UNSPECIFIED., .F., .F., .T. ) 
 B_SPLINE_SURFACE_WITH_KNOTS ( ( 4, 4 ),
 ( 2, 2 ),
 ( 0.000000000000000000, 1.000000000000000000 ),
 ( 0.000000000000000000, 1.000000000000000000 ),
 .UNSPECIFIED. ) 
 GEOMETRIC_REPRESENTATION_ITEM ( )  RATIONAL_B_SPLINE_SURFACE ( (
 ( 1.000000000000000000, 1.000000000000000000),
 ( 0.9593108457356467333, 0.9995965569486454649),
 ( 0.9593108457356467333, 0.9995965569486454649),
 ( 1.000000000000000000, 1.000000000000000000) ) ) 
 REPRESENTATION_ITEM ( '' )  SURFACE ( )  );
#8356=CARTESIAN_POINT ( 'NONE',  ( 0.3095370825347224519, 10.84046130709070788, -8.444334731363888125 ) ) ;
#8359=CARTESIAN_POINT ( 'NONE',  ( 0.3148213771069364175, 11.24846294176323447, -7.888490156175093304 ) ) ;
#8364=ORIENTED_EDGE ( 'NONE', *, *, #8735, .F. ) ;
#8365=EDGE_LOOP ( 'NONE', ( #3894, #17351, #2001, #17258 ) ) ;
#8370=CARTESIAN_POINT ( 'NONE',  ( 0.3307726912345239634, -12.88561780039862015, 4.812300915532924606 ) ) ;
#8376=( BOUNDED_SURFACE ( )  B_SPLINE_SURFACE ( 3, 1, ( 
 ( #7508, #17827 ),
 ( #3376, #1865 ),
 ( #15144, #13511 ),
 ( #17732, #16195 ) ),
 .UNSPECIFIED., .F., .F., .T. ) 
 B_SPLINE_SURFACE_WITH_KNOTS ( ( 4, 4 ),
 ( 2, 2 ),
 ( 0.000000000000000000, 1.000000000000000000 ),
 ( 0.000000000000000000, 1.000000000000000000 ),
 .UNSPECIFIED. ) 
 GEOMETRIC_REPRESENTATION_ITEM ( )  RATIONAL_B_SPLINE_SURFACE ( (
 ( 1.000000000000000000, 1.000000000000000000),
 ( 0.9933953342250438912, 0.8357391271907739227),
 ( 0.9933953342250438912, 0.8357391271907739227),
 ( 1.000000000000000000, 1.000000000000000000) ) ) 
 REPRESENTATION_ITEM ( '' )  SURFACE ( )  );
#8381=CARTESIAN_POINT ( 'NONE',  ( 16.56753206892534891, -0.008490833999798956880, -0.004253784598196145433 ) ) ;
#8382=CARTESIAN_POINT ( 'NONE',  ( 0.4754618798421162973, 13.89949764182682657, 0.7484603771384912285 ) ) ;
#8386=CARTESIAN_POINT ( 'NONE',  ( 3.950837973638668288, 0.000000000000000000, 0.000000000000000000 ) ) ;
#8395=CARTESIAN_POINT ( 'NONE',  ( 1.847372867223022963, -3.945260592619128204, 11.80112642014553614 ) ) ;
#8396=EDGE_LOOP ( 'NONE', ( #10238, #11352, #1165, #3057 ) ) ;
#8400=ORIENTED_EDGE ( 'NONE', *, *, #10518, .T. ) ;
#8402=VECTOR ( 'NONE', #13270, 1000.000000000000114 ) ;
#8405=DIRECTION ( 'NONE',  ( 0.000000000000000000, 0.000000000000000000, 1.000000000000000000 ) ) ;
#8412=CARTESIAN_POINT ( 'NONE',  ( 0.3150686449036029235, -13.73846184595214304, 0.1533607327085267646 ) ) ;
#8414=CARTESIAN_POINT ( 'NONE',  ( 16.57210152137263393, 0.0006600038696346007027, -0.01453130299868522768 ) ) ;
#8418=CARTESIAN_POINT ( 'NONE',  ( 0.3095370825347233956, -10.84046130709064393, 8.444334731363969837 ) ) ;
#8420=ORIENTED_EDGE ( 'NONE', *, *, #3209, .T. ) ;
#8424=EDGE_LOOP ( 'NONE', ( #17771, #9102, #12652, #16137, #14259, #3295 ) ) ;
#8425=CARTESIAN_POINT ( 'NONE',  ( 0.3142011359265305392, 3.879426116491875742, -13.17934269988453977 ) ) ;
#8430=B_SPLINE_CURVE_WITH_KNOTS ( 'NONE', 3,
 ( #11401, #2862, #5377, #15881, #13010, #17220, #18844, #4133, #15787, #4036 ),
 .UNSPECIFIED., .F., .F.,
 ( 4, 3, 3, 4 ),
 ( 0.0004597478348665241538, 0.0004599561239687906082, 0.0006896788984287882803, 0.0009194956271626397379 ),
 .UNSPECIFIED. ) ;
#8431=LINE ( 'NONE', #1354, #12203 ) ;
#8437=VERTEX_POINT ( 'NONE', #17082 ) ;
#8442=CARTESIAN_POINT ( 'NONE',  ( 3.950837973638676281, -12.81214529934970336, -6.888253895133431115 ) ) ;
#8445=ORIENTED_EDGE ( 'NONE', *, *, #12873, .T. ) ;
#8457=B_SPLINE_CURVE_WITH_KNOTS ( 'NONE', 3,
 ( #2893, #16110, #1489, #13139 ),
 .UNSPECIFIED., .F., .F.,
 ( 4, 4 ),
 ( 2.006682199098010609E-17, 0.003005512676784846595 ),
 .UNSPECIFIED. ) ;
#8468=CARTESIAN_POINT ( 'NONE',  ( 16.57778382496167424, -0.01306626476309294925, 0.007244066302946726259 ) ) ;
#8469=CARTESIAN_POINT ( 'NONE',  ( 0.4754618798421171855, 5.007009103465246191, 12.98792082933646519 ) ) ;
#8470=VERTEX_POINT ( 'NONE', #16806 ) ;
#8471=B_SPLINE_CURVE_WITH_KNOTS ( 'NONE', 3,
 ( #4077, #17165, #14307, #14212, #17080, #15630 ),
 .UNSPECIFIED., .F., .F.,
 ( 4, 2, 4 ),
 ( 0.000000000000000000, 0.001500839035891552223, 0.003001678071783104446 ),
 .UNSPECIFIED. ) ;
#8476=B_SPLINE_CURVE_WITH_KNOTS ( 'NONE', 3,
 ( #6595, #5150, #15373, #6316 ),
 .UNSPECIFIED., .F., .F.,
 ( 4, 4 ),
 ( 1.974081779422029518E-17, 0.003005512676784849631 ),
 .UNSPECIFIED. ) ;
#8478=FACE_OUTER_BOUND ( 'NONE', #18150, .T. ) ;
#8484=CARTESIAN_POINT ( 'NONE',  ( 0.8740779401510758717, -0.8420120399581221271, -14.27348745891595172 ) ) ;
#8488=CARTESIAN_POINT ( 'NONE',  ( 3.950837973638676281, -12.81214529934979929, 6.888253895133251703 ) ) ;
#8489=DIRECTION ( 'NONE',  ( -0.7561779333270775005, -0.5491072561318312006, -0.3559159372837374935 ) ) ;
#8494=VECTOR ( 'NONE', #12537, 1000.000000000000114 ) ;
#8497=CARTESIAN_POINT ( 'NONE',  ( 3.950837973638675393, 6.888253895133479965, -12.81214529934967672 ) ) ;
#8500=VERTEX_POINT ( 'NONE', #10900 ) ;
#8508=CARTESIAN_POINT ( 'NONE',  ( 1.562796894703937678, 1.488975241814732168E-15, 12.15840553252917289 ) ) ;
#8509=CARTESIAN_POINT ( 'NONE',  ( 3.512766787570762439, -10.40533104696141997, 10.87507422923886224 ) ) ;
#8512=B_SPLINE_CURVE_WITH_KNOTS ( 'NONE', 3,
 ( #1693, #11730, #17560, #10298 ),
 .UNSPECIFIED., .F., .F.,
 ( 4, 4 ),
 ( 1.684670163748776910E-17, 0.003005512676784852233 ),
 .UNSPECIFIED. ) ;
#8517=ORIENTED_EDGE ( 'NONE', *, *, #16832, .F. ) ;
#8520=ADVANCED_FACE ( 'NONE', ( #5325 ), #15763, .F. ) ;
#8522=DIRECTION ( 'NONE',  ( -0.7561779333270775005, 0.1688126975276644792, -0.6322161072786924851 ) ) ;
#8524=VERTEX_POINT ( 'NONE', #15363 ) ;
#8527=CARTESIAN_POINT ( 'NONE',  ( 0.4862570985993252548, 3.580942890621670482, 13.44146924561382583 ) ) ;
#8531=CARTESIAN_POINT ( 'NONE',  ( 1.846138399168762989, 11.95493567637850774, 3.446241763653039580 ) ) ;
#8532=ORIENTED_EDGE ( 'NONE', *, *, #16501, .F. ) ;
#8536=CARTESIAN_POINT ( 'NONE',  ( 1.847168016377985778, 0.1868244120189564983, 12.44137401948661115 ) ) ;
#8540=CARTESIAN_POINT ( 'NONE',  ( 1.254009781011695468, -14.24044713813331597, -3.563484327698402510 ) ) ;
#8543=EDGE_CURVE ( 'NONE', #5397, #14601, #250, .T. ) ;
#8546=CARTESIAN_POINT ( 'NONE',  ( 16.56679352167444819, 0.004162264567718796174, -0.008311568981097996328 ) ) ;
#8548=ORIENTED_EDGE ( 'NONE', *, *, #8059, .F. ) ;
#8549=B_SPLINE_CURVE_WITH_KNOTS ( 'NONE', 3,
 ( #9144, #8761, #13149, #60, #11720, #1885 ),
 .UNSPECIFIED., .F., .F.,
 ( 4, 2, 4 ),
 ( 8.673617379884035472E-19, 0.0001828790815886942919, 0.0003657581631773877164 ),
 .UNSPECIFIED. ) ;
#8550=CARTESIAN_POINT ( 'NONE',  ( 1.977228804421386821, 10.21522664410325021, 11.52787183731143017 ) ) ;
#8552=CARTESIAN_POINT ( 'NONE',  ( 16.56782317627811096, 0.002708056627498641941, 0.009439921864426896805 ) ) ;
#8558=CARTESIAN_POINT ( 'NONE',  ( 1.342453679581834924, 5.476372339890016150, 13.74702459364886487 ) ) ;
#8561=EDGE_LOOP ( 'NONE', ( #14363, #10166, #17766, #13829 ) ) ;
#8562=ORIENTED_EDGE ( 'NONE', *, *, #15010, .T. ) ;
#8565=LINE ( 'NONE', #1399, #4414 ) ;
#8571=LINE ( 'NONE', #12961, #18134 ) ;
#8584=ORIENTED_EDGE ( 'NONE', *, *, #11096, .T. ) ;
#8586=CARTESIAN_POINT ( 'NONE',  ( 0.4754618798421162973, -3.583352865732763792, 13.45049478164058776 ) ) ;
#8595=CARTESIAN_POINT ( 'NONE',  ( 2.002547531651519996, 6.845637710436190737, 10.57595306287294612 ) ) ;
#8600=CARTESIAN_POINT ( 'NONE',  ( 0.3939875929385667219, -3.598491969338320384, 13.34133634968953785 ) ) ;
#8605=VERTEX_POINT ( 'NONE', #10189 ) ;
#8610=DIRECTION ( 'NONE',  ( -0.7635533937278214944, 0.5347026451755939602, 0.3620487483322503142 ) ) ;
#8620=DIRECTION ( 'NONE',  ( -1.000000000000000000, -0.000000000000000000, -0.000000000000000000 ) ) ;
#8621=ADVANCED_FACE ( 'NONE', ( #1207 ), #17583, .T. ) ;
#8622=( GEOMETRIC_REPRESENTATION_CONTEXT ( 3 ) GLOBAL_UNCERTAINTY_ASSIGNED_CONTEXT ( ( #15689 ) ) GLOBAL_UNIT_ASSIGNED_CONTEXT ( ( #6212, #3034, #7465 ) ) REPRESENTATION_CONTEXT ( 'NONE', 'WORKASPACE' ) );
#8624=EDGE_CURVE ( 'NONE', #12529, #5127, #8765, .T. ) ;
#8626=FACE_OUTER_BOUND ( 'NONE', #16779, .T. ) ;
#8627=CARTESIAN_POINT ( 'NONE',  ( 3.074695600507223681, -13.70113613813211195, -7.366518011946086908 ) ) ;
#8628=CARTESIAN_POINT ( 'NONE',  ( 0.4385251269669942498, 7.540955776459739468, 11.63205320541525900 ) ) ;
#8630=ORIENTED_EDGE ( 'NONE', *, *, #5052, .F. ) ;
#8633=ORIENTED_EDGE ( 'NONE', *, *, #13219, .F. ) ;
#8634=ORIENTED_EDGE ( 'NONE', *, *, #5662, .T. ) ;
#8635=CARTESIAN_POINT ( 'NONE',  ( 16.58200780006414732, -0.006043560077721639792, -0.009393638146079824613 ) ) ;
#8637=ORIENTED_EDGE ( 'NONE', *, *, #17611, .T. ) ;
#8642=CARTESIAN_POINT ( 'NONE',  ( 0.8740779401512712710, 11.05257166392075341, -9.070947476926923159 ) ) ;
#8644=ADVANCED_FACE ( 'NONE', ( #7140 ), #10530, .F. ) ;
#8645=CARTESIAN_POINT ( 'NONE',  ( 0.3137051932979809665, -3.805684345189881856, 13.20008686438104739 ) ) ;
#8649=CARTESIAN_POINT ( 'NONE',  ( 2.123976203522053741, 6.261444813538558307, 14.31368049382972529 ) ) ;
#8651=VERTEX_POINT ( 'NONE', #16514 ) ;
#8652=ORIENTED_EDGE ( 'NONE', *, *, #17188, .T. ) ;
#8653=EDGE_LOOP ( 'NONE', ( #12836, #11603, #10603, #13741 ) ) ;
#8656=CARTESIAN_POINT ( 'NONE',  ( 1.847168016377985333, 3.666915430942765397, -11.89018175117590559 ) ) ;
#8658=DIRECTION ( 'NONE',  ( -1.000000000000000000, -0.000000000000000000, -0.000000000000000000 ) ) ;
#8668=EDGE_CURVE ( 'NONE', #5097, #18549, #12762, .T. ) ;
#8669=LINE ( 'NONE', #13065, #14368 ) ;
#8671=EDGE_CURVE ( 'NONE', #13313, #5127, #14587, .T. ) ;
#8672=CARTESIAN_POINT ( 'NONE',  ( 1.847461586945727374, -3.813310247068524284, 11.84459954310609753 ) ) ;
#8673=ORIENTED_EDGE ( 'NONE', *, *, #2623, .T. ) ;
#8687=VERTEX_POINT ( 'NONE', #15065 ) ;
#8688=CARTESIAN_POINT ( 'NONE',  ( 16.56679352167444819, -0.008252760440870528930, -0.004277682826582232013 ) ) ;
#8689=LINE ( 'NONE', #2663, #15851 ) ;
#8690=CARTESIAN_POINT ( 'NONE',  ( 0.3142011359265340920, -13.73310835363014348, 0.3830873813805846240 ) ) ;
#8692=CARTESIAN_POINT ( 'NONE',  ( 0.3308579732647007887, -8.558831104906994725, 10.76782854710824111 ) ) ;
#8693=CARTESIAN_POINT ( 'NONE',  ( 1.847034903785822690, 7.126331315909270714, 10.19974412751566994 ) ) ;
#8698=ORIENTED_EDGE ( 'NONE', *, *, #9133, .T. ) ;
#8699=EDGE_CURVE ( 'NONE', #18618, #6956, #497, .T. ) ;
#8703=CARTESIAN_POINT ( 'NONE',  ( 0.3151926232592472954, 8.013596737356548871, -11.16039997398644879 ) ) ;
#8704=CARTESIAN_POINT ( 'NONE',  ( 0.4862570985993235340, -0.7479633556563419772, 13.89016912371017121 ) ) ;
#8705=B_SPLINE_CURVE_WITH_KNOTS ( 'NONE', 3,
 ( #4993, #11212, #2670, #12812, #15402, #14343 ),
 .UNSPECIFIED., .F., .F.,
 ( 4, 2, 4 ),
 ( 0.000000000000000000, 0.001656992708822831520, 0.003313985417645663040 ),
 .UNSPECIFIED. ) ;
#8712=ORIENTED_EDGE ( 'NONE', *, *, #9889, .T. ) ;
#8715=EDGE_CURVE ( 'NONE', #16337, #4624, #5, .T. ) ;
#8720=DIRECTION ( 'NONE',  ( -1.000000000000000000, -0.000000000000000000, -0.000000000000000000 ) ) ;
#8724=CARTESIAN_POINT ( 'NONE',  ( 1.846138399168762989, 4.238866729160403857, 11.69739621335923729 ) ) ;
#8729=ORIENTED_EDGE ( 'NONE', *, *, #16515, .T. ) ;
#8731=CARTESIAN_POINT ( 'NONE',  ( 16.57210152137263393, 0.003862718596009469003, -0.01402404281923040792 ) ) ;
#8733=CARTESIAN_POINT ( 'NONE',  ( 1.959283090834842200, -3.239245055717051791, 12.12982544407804220 ) ) ;
#8735=EDGE_CURVE ( 'NONE', #10624, #14167, #7330, .T. ) ;
#8736=CARTESIAN_POINT ( 'NONE',  ( 16.56782317627811096, -0.008141063682853446129, 0.005492611183758502880 ) ) ;
#8741=CARTESIAN_POINT ( 'NONE',  ( 0.3145734862173267810, 3.953068532979994831, 13.15783074029279831 ) ) ;
#8747=CARTESIAN_POINT ( 'NONE',  ( 0.3132642857406562342, -10.79548167658028213, -8.495623922778184678 ) ) ;
#8748=B_SPLINE_CURVE_WITH_KNOTS ( 'NONE', 3,
 ( #391, #3236, #9086, #17981, #6218, #4888 ),
 .UNSPECIFIED., .F., .F.,
 ( 4, 2, 4 ),
 ( 0.000000000000000000, 0.001656992708822033113, 0.003313985417644066227 ),
 .UNSPECIFIED. ) ;
#8751=CARTESIAN_POINT ( 'NONE',  ( 3.512766787570810845, 10.40533104696146083, -10.87507422923874856 ) ) ;
#8753=COLOUR_RGB ( '', 0.09019608, 0.27058824, 0.51372549) ;
#8756=ORIENTED_EDGE ( 'NONE', *, *, #18267, .T. ) ;
#8761=CARTESIAN_POINT ( 'NONE',  ( 1.845755665166725734, -11.97169564665393970, 3.386720041070682363 ) ) ;
#8763=CARTESIAN_POINT ( 'NONE',  ( 0.3095370825347224519, 13.73357284481724783, 0.4597470195090653799 ) ) ;
#8765=LINE ( 'NONE', #7051, #10579 ) ;
#8766=ORIENTED_EDGE ( 'NONE', *, *, #2727, .F. ) ;
#8769=VECTOR ( 'NONE', #16485, 1000.000000000000114 ) ;
#8770=CARTESIAN_POINT ( 'NONE',  ( 2.636624412714237309, 11.10302021257826866, 11.60464335004050973 ) ) ;
#8771=DIRECTION ( 'NONE',  ( -0.7635533937278216055, -0.6204116510013465424, -0.1790966170213987851 ) ) ;
#8781=CARTESIAN_POINT ( 'NONE',  ( 16.56872352241294521, 0.009382111268606257298, -0.004564908236400254740 ) ) ;
#8782=EDGE_CURVE ( 'NONE', #12877, #1860, #5018, .T. ) ;
#8785=CARTESIAN_POINT ( 'NONE',  ( 8.522092701127531811, -5.841710761610158009, 3.777034505568503064 ) ) ;
#8790=CARTESIAN_POINT ( 'NONE',  ( 3.664313757352971823, 7.012524439851495650, 12.42002390572628201 ) ) ;
#8798=CARTESIAN_POINT ( 'NONE',  ( 0.4862570985993235340, -11.67702470553370553, 7.559321496869385371 ) ) ;
#8803=ORIENTED_EDGE ( 'NONE', *, *, #18181, .T. ) ;
#8804=CARTESIAN_POINT ( 'NONE',  ( 0.3150692679895985560, 4.391039771493846722, -13.01874238516605331 ) ) ;
#8820=ORIENTED_EDGE ( 'NONE', *, *, #3651, .T. ) ;
#8821=FACE_OUTER_BOUND ( 'NONE', #17980, .T. ) ;
#8825=CARTESIAN_POINT ( 'NONE',  ( 16.56753206892534891, 0.008490833999798002782, -0.004253784598196794220 ) ) ;
#8827=CARTESIAN_POINT ( 'NONE',  ( 16.57210152137263393, -0.01136813053532154116, 0.009075239946109162070 ) ) ;
#8831=VERTEX_POINT ( 'NONE', #914 ) ;
#8834=EDGE_CURVE ( 'NONE', #5568, #17620, #10750, .T. ) ;
#8838=UNCERTAINTY_MEASURE_WITH_UNIT (LENGTH_MEASURE( 1.000000000000000082E-05 ), #13694, 'distance_accuracy_value', 'NONE');
#8840=CARTESIAN_POINT ( 'NONE',  ( 0.3095370825347224519, -0.4597470195089233824, -13.73357284481725316 ) ) ;
#8845=CARTESIAN_POINT ( 'NONE',  ( 0.3150692679895987780, 13.73846569174797061, 0.1531143455845020152 ) ) ;
#8846=EDGE_CURVE ( 'NONE', #8095, #2099, #5918, .T. ) ;
#8852=CYLINDRICAL_SURFACE ( 'NONE', #11405, 2.500000000000000000 ) ;
#8862=CARTESIAN_POINT ( 'NONE',  ( 3.074695600507765025, 15.30693405987741684, -2.772091048738999142 ) ) ;
#8867=ORIENTED_EDGE ( 'NONE', *, *, #16587, .F. ) ;
#8869=ORIENTED_EDGE ( 'NONE', *, *, #16854, .T. ) ;
#8874=CARTESIAN_POINT ( 'NONE',  ( 16.56679352167444819, 0.009190982326619719436, 0.001390132774594471984 ) ) ;
#8881=CARTESIAN_POINT ( 'NONE',  ( 1.977228804423517117, 14.12033626431153444, -6.152949558602713864 ) ) ;
#8882=EDGE_CURVE ( 'NONE', #17181, #15162, #9702, .T. ) ;
#8899=DIRECTION ( 'NONE',  ( 0.7561779333270775005, 0.1688126975276512953, 0.6322161072786960379 ) ) ;
#8906=EDGE_CURVE ( 'NONE', #2339, #16009, #7029, .T. ) ;
#8907=CARTESIAN_POINT ( 'NONE',  ( 0.4754618798421162973, -13.45049478164057177, -3.583352865732810866 ) ) ;
#8910=EDGE_CURVE ( 'NONE', #13343, #137, #5981, .T. ) ;
#8912=CARTESIAN_POINT ( 'NONE',  ( 0.3150686449036039227, -7.951193823202478583, 11.20479228691394979 ) ) ;
#8914=ORIENTED_EDGE ( 'NONE', *, *, #12222, .T. ) ;
#8920=ORIENTED_EDGE ( 'NONE', *, *, #6572, .T. ) ;
#8921=EDGE_CURVE ( 'NONE', #11883, #14584, #9651, .T. ) ;
#8924=B_SPLINE_CURVE_WITH_KNOTS ( 'NONE', 3,
 ( #2885, #38, #7412, #15548, #8298, #11266 ),
 .UNSPECIFIED., .F., .F.,
 ( 4, 2, 4 ),
 ( 1.084202172485504434E-19, 0.001657017934709843158, 0.003314035869419686316 ),
 .UNSPECIFIED. ) ;
#8927=CARTESIAN_POINT ( 'NONE',  ( 0.3151928479966097374, 0.000000000000000000, -13.73922861026898623 ) ) ;
#8931=CARTESIAN_POINT ( 'NONE',  ( 0.3095370825347224519, -10.84046130709064570, 8.444334731363969837 ) ) ;
#8933=CARTESIAN_POINT ( 'NONE',  ( 1.847380140988740260, -11.79969976631074680, 3.949801494731721263 ) ) ;
#8935=VERTEX_POINT ( 'NONE', #1191 ) ;
#8936=VECTOR ( 'NONE', #717, 1000.000000000000000 ) ;
#8938=B_SPLINE_CURVE_WITH_KNOTS ( 'NONE', 3,
 ( #13055, #259, #17553, #7340 ),
 .UNSPECIFIED., .F., .F.,
 ( 4, 4 ),
 ( 1.524041208624749586E-16, 0.002004993803842462265 ),
 .UNSPECIFIED. ) ;
#8939=ORIENTED_EDGE ( 'NONE', *, *, #15150, .F. ) ;
#8941=B_SPLINE_CURVE_WITH_KNOTS ( 'NONE', 3,
 ( #7379, #13189, #201, #7087, #6034, #4600, #17397, #8703, #7473, #11767, #12998, #18833, #10425 ),
 .UNSPECIFIED., .F., .F.,
 ( 4, 3, 3, 3, 4 ),
 ( 2.453269466693398698E-18, 0.0002299780670421020532, 0.0004599561239687888735, 0.0006896788984287890393, 0.0009194956271626411473 ),
 .UNSPECIFIED. ) ;
#8945=CARTESIAN_POINT ( 'NONE',  ( 0.3137051932979775248, 0.4596302728639756197, 13.73004976592202198 ) ) ;
#8951=CARTESIAN_POINT ( 'NONE',  ( 2.636624412714237309, 15.91454522070173638, -2.161493821596664144 ) ) ;
#8957=CARTESIAN_POINT ( 'NONE',  ( 16.56753206892534891, 0.004253784598196760393, 0.008490833999798020129 ) ) ;
#8959=( BOUNDED_SURFACE ( )  B_SPLINE_SURFACE ( 3, 1, ( 
 ( #6624, #16477 ),
 ( #4905, #786 ),
 ( #4813, #12442 ),
 ( #4715, #10545 ) ),
 .UNSPECIFIED., .F., .F., .T. ) 
 B_SPLINE_SURFACE_WITH_KNOTS ( ( 4, 4 ),
 ( 2, 2 ),
 ( 0.000000000000000000, 1.000000000000000000 ),
 ( 0.000000000000000000, 1.000000000000000000 ),
 .UNSPECIFIED. ) 
 GEOMETRIC_REPRESENTATION_ITEM ( )  RATIONAL_B_SPLINE_SURFACE ( (
 ( 1.000000000000000000, 1.000000000000000000),
 ( 0.9933953342250438912, 0.8357391271907739227),
 ( 0.9933953342250438912, 0.8357391271907739227),
 ( 1.000000000000000000, 1.000000000000000000) ) ) 
 REPRESENTATION_ITEM ( '' )  SURFACE ( )  );
#8967=CARTESIAN_POINT ( 'NONE',  ( 3.664313757352975820, -10.50730552161225972, -9.645155442698879256 ) ) ;
#8975=ADVANCED_FACE ( 'NONE', ( #15807 ), #2886, .F. ) ;
#8978=CARTESIAN_POINT ( 'NONE',  ( 1.918921323896324083, 11.69058285425790977, 4.466082741316246718 ) ) ;
#8979=CARTESIAN_POINT ( 'NONE',  ( 2.636624412715137922, 2.161493821597615828, 15.91454522070216093 ) ) ;
#8981=B_SPLINE_CURVE_WITH_KNOTS ( 'NONE', 3,
 ( #4979, #3638, #5163, #9472, #10919, #10816, #11193, #683, #2466, #8231, #8139, #14132, #18261 ),
 .UNSPECIFIED., .F., .F.,
 ( 4, 3, 3, 3, 4 ),
 ( 8.673617379884035472E-19, 0.0002299804304191491514, 0.0004599608082120254429, 0.0006467586077648011496, 0.0008336169836825998080 ),
 .UNSPECIFIED. ) ;
#8986=CARTESIAN_POINT ( 'NONE',  ( 3.950837973638676281, 12.81214529934975310, 6.888253895133341409 ) ) ;
#8987=ORIENTED_EDGE ( 'NONE', *, *, #17186, .T. ) ;
#8989=CARTESIAN_POINT ( 'NONE',  ( 16.56679352167444819, -0.004162264567718857756, 0.008311568981097966838 ) ) ;
#8996=( BOUNDED_SURFACE ( )  B_SPLINE_SURFACE ( 3, 1, ( 
 ( #6120, #17783 ),
 ( #3333, #3230 ),
 ( #9080, #9267 ),
 ( #15097, #1819 ) ),
 .UNSPECIFIED., .F., .F., .T. ) 
 B_SPLINE_SURFACE_WITH_KNOTS ( ( 4, 4 ),
 ( 2, 2 ),
 ( 0.000000000000000000, 1.000000000000000000 ),
 ( 0.000000000000000000, 1.000000000000000000 ),
 .UNSPECIFIED. ) 
 GEOMETRIC_REPRESENTATION_ITEM ( )  RATIONAL_B_SPLINE_SURFACE ( (
 ( 1.000000000000000000, 1.000000000000000000),
 ( 0.9933953342250436691, 0.8357391271907733676),
 ( 0.9933953342250436691, 0.8357391271907733676),
 ( 1.000000000000000000, 1.000000000000000000) ) ) 
 REPRESENTATION_ITEM ( '' )  SURFACE ( )  );
#8999=EDGE_CURVE ( 'NONE', #12864, #3512, #16440, .T. ) ;
#9001=CARTESIAN_POINT ( 'NONE',  ( 2.636624412714236865, 0.000000000000000000, 0.000000000000000000 ) ) ;
#9003=CARTESIAN_POINT ( 'NONE',  ( 0.3307726912345216319, -13.74203354050372283, 0.5948952607472158816 ) ) ;
#9011=CARTESIAN_POINT ( 'NONE',  ( 0.4384471787762856398, 11.63197976518328680, 7.540925784514595165 ) ) ;
#9017=AXIS2_PLACEMENT_3D ( 'NONE', #9636, #11178, #855 ) ;
#9026=ADVANCED_FACE ( 'NONE', ( #11700 ), #11194, .T. ) ;
#9030=CARTESIAN_POINT ( 'NONE',  ( 0.8740779401512095426, 7.708543377337996994, -12.04241618260087776 ) ) ;
#9032=CARTESIAN_POINT ( 'NONE',  ( 0.4862570985993252548, 3.580942890621670482, 13.44146924561382583 ) ) ;
#9033=FACE_OUTER_BOUND ( 'NONE', #13596, .T. ) ;
#9038=CARTESIAN_POINT ( 'NONE',  ( 0.3308579732646986238, -7.595989242675048381, -11.46737410776362509 ) ) ;
#9040=CARTESIAN_POINT ( 'NONE',  ( 1.562796894703937678, 1.635200584729765362E-15, 12.15840553252917289 ) ) ;
#9041=ORIENTED_EDGE ( 'NONE', *, *, #17001, .F. ) ;
#9045=ORIENTED_EDGE ( 'NONE', *, *, #9217, .F. ) ;
#9046=CARTESIAN_POINT ( 'NONE',  ( 0.3151928479966097374, 1.775918418904422640E-15, 13.73922861026898623 ) ) ;
#9048=CARTESIAN_POINT ( 'NONE',  ( 1.847372867223026294, -12.44269075185938611, -0.1054171785007791406 ) ) ;
#9049=CARTESIAN_POINT ( 'NONE',  ( 0.4862570985993235340, 13.89016912371017476, 0.7479633556562934604 ) ) ;
#9052=DIRECTION ( 'NONE',  ( 0.000000000000000000, 0.000000000000000000, 1.000000000000000000 ) ) ;
#9053=CARTESIAN_POINT ( 'NONE',  ( 0.3095370825347234511, 13.20347358821919848, -3.806662003783274795 ) ) ;
#9054=CARTESIAN_POINT ( 'NONE',  ( 1.847412631396503579, 12.44294644888238999, 0.04315047898439477309 ) ) ;
#9069=DIRECTION ( 'NONE',  ( -1.000000000000000000, -0.000000000000000000, -0.000000000000000000 ) ) ;
#9075=ORIENTED_EDGE ( 'NONE', *, *, #18497, .T. ) ;
#9080=CARTESIAN_POINT ( 'NONE',  ( 16.56822296793089322, -0.009385634690642031749, 0.003834730849371980905 ) ) ;
#9085=ORIENTED_EDGE ( 'NONE', *, *, #6224, .T. ) ;
#9086=CARTESIAN_POINT ( 'NONE',  ( 1.977436885025421809, 14.12046670317507058, 6.153171729167918436 ) ) ;
#9090=ORIENTED_EDGE ( 'NONE', *, *, #7311, .F. ) ;
#9095=CARTESIAN_POINT ( 'NONE',  ( 0.3137051932979792457, -12.91601973349266963, -4.679953077377624560 ) ) ;
#9098=CARTESIAN_POINT ( 'NONE',  ( 16.57778382496167424, -0.01092721432668986720, -0.01018821665058789253 ) ) ;
#9099=CARTESIAN_POINT ( 'NONE',  ( 0.3720661004400040439, 13.79610186261029980, -0.7231997263365288475 ) ) ;
#9102=ORIENTED_EDGE ( 'NONE', *, *, #9332, .F. ) ;
#9106=CARTESIAN_POINT ( 'NONE',  ( 16.57778382496167424, -0.01018821665058842162, -0.01092721432669105028 ) ) ;
#9110=VERTEX_POINT ( 'NONE', #11994 ) ;
#9112=EDGE_CURVE ( 'NONE', #10941, #10024, #17788, .T. ) ;
#9119=ORIENTED_EDGE ( 'NONE', *, *, #3071, .T. ) ;
#9123=ORIENTED_EDGE ( 'NONE', *, *, #5834, .F. ) ;
#9126=LINE ( 'NONE', #7611, #17612 ) ;
#9129=CARTESIAN_POINT ( 'NONE',  ( 2.747332970342022840, -7.289199830147006232, -14.63517873738954655 ) ) ;
#9133=EDGE_CURVE ( 'NONE', #10024, #17449, #13445, .T. ) ;
#9138=CIRCLE ( 'NONE', #14927, 16.06066017081991149 ) ;
#9139=VERTEX_POINT ( 'NONE', #4831 ) ;
#9144=CARTESIAN_POINT ( 'NONE',  ( 1.846138399168762101, -11.95493567637852905, 3.446241763652952539 ) ) ;
#9149=CARTESIAN_POINT ( 'NONE',  ( 3.512766787570690497, 2.682019731918607430, -14.81029789862162893 ) ) ;
#9153=CARTESIAN_POINT ( 'NONE',  ( 0.3137051932979809665, 13.20008686438111312, -3.805684345189650042 ) ) ;
#9154=CARTESIAN_POINT ( 'NONE',  ( 1.846138399168762101, -7.646096044339961040, 9.815003036200383946 ) ) ;
#9157=ORIENTED_EDGE ( 'NONE', *, *, #16964, .F. ) ;
#9159=ADVANCED_FACE ( 'NONE', ( #3077 ), #2797, .F. ) ;
#9164=CARTESIAN_POINT ( 'NONE',  ( 2.636624412715435462, -15.80357026013316712, -2.862162146983298516 ) ) ;
#9165=CARTESIAN_POINT ( 'NONE',  ( 0.3095370825347224519, -12.91933430393604709, -4.681152801286295073 ) ) ;
#9166=CARTESIAN_POINT ( 'NONE',  ( 0.4862570985993235340, -13.44146924561383827, 3.580942890621619412 ) ) ;
#9173=CARTESIAN_POINT ( 'NONE',  ( 16.58200780006414732, 0.007066318000004704822, 0.008650561019685554590 ) ) ;
#9181=LINE ( 'NONE', #16734, #2338 ) ;
#9184=EDGE_LOOP ( 'NONE', ( #13871, #12656, #10965, #16752 ) ) ;
#9188=( BOUNDED_SURFACE ( )  B_SPLINE_SURFACE ( 3, 1, ( 
 ( #5615, #6985 ),
 ( #11468, #14606 ),
 ( #15856, #16042 ),
 ( #4205, #12797 ) ),
 .UNSPECIFIED., .F., .F., .T. ) 
 B_SPLINE_SURFACE_WITH_KNOTS ( ( 4, 4 ),
 ( 2, 2 ),
 ( 0.000000000000000000, 1.000000000000000000 ),
 ( 0.000000000000000000, 1.000000000000000000 ),
 .UNSPECIFIED. ) 
 GEOMETRIC_REPRESENTATION_ITEM ( )  RATIONAL_B_SPLINE_SURFACE ( (
 ( 1.000000000000000000, 1.000000000000000000),
 ( 0.7792777138730160313, 0.9689936506012927220),
 ( 0.7792777138730160313, 0.9689936506012927220),
 ( 1.000000000000000000, 1.000000000000000000) ) ) 
 REPRESENTATION_ITEM ( '' )  SURFACE ( )  );
#9190=CARTESIAN_POINT ( 'NONE',  ( 16.58200780006414732, -0.004047297414157817463, -0.01041078477703986926 ) ) ;
#9192=CARTESIAN_POINT ( 'NONE',  ( 16.56679352167444819, -0.006526964904753006572, -0.006618561353599182288 ) ) ;
#9195=EDGE_CURVE ( 'NONE', #8605, #16257, #13985, .T. ) ;
#9197=CARTESIAN_POINT ( 'NONE',  ( 1.918918678667044908, -6.832809802519085096, 10.48466773720559608 ) ) ;
#9199=FACE_OUTER_BOUND ( 'NONE', #18790, .T. ) ;
#9201=VERTEX_POINT ( 'NONE', #628 ) ;
#9204=CARTESIAN_POINT ( 'NONE',  ( 0.4754618798421171855, -7.564402563418553882, 11.68486377711963797 ) ) ;
#9206=ORIENTED_EDGE ( 'NONE', *, *, #2727, .T. ) ;
#9217=EDGE_CURVE ( 'NONE', #8021, #1012, #7536, .T. ) ;
#9220=CARTESIAN_POINT ( 'NONE',  ( 0.4754618798421167414, 5.007009103465430044, -12.98792082933639058 ) ) ;
#9222=B_SPLINE_CURVE_WITH_KNOTS ( 'NONE', 3,
 ( #3065, #418, #16484, #4622, #3367, #12081, #18005, #13211, #8912, #10550, #17913, #14739, #7495 ),
 .UNSPECIFIED., .F., .F.,
 ( 4, 3, 3, 3, 4 ),
 ( 3.878959614448864246E-18, 0.0002299780670421047908, 0.0004599561239687891445, 0.0006896788984287886056, 0.0009194956271626397379 ),
 .UNSPECIFIED. ) ;
#9223=CARTESIAN_POINT ( 'NONE',  ( 1.562796894703937678, 0.000000000000000000, 0.000000000000000000 ) ) ;
#9224=( BOUNDED_SURFACE ( )  B_SPLINE_SURFACE ( 3, 1, ( 
 ( #4770, #10404 ),
 ( #477, #11844 ),
 ( #4867, #10700 ),
 ( #7653, #5902 ) ),
 .UNSPECIFIED., .F., .F., .F. ) 
 B_SPLINE_SURFACE_WITH_KNOTS ( ( 4, 4 ),
 ( 2, 2 ),
 ( 0.000000000000000000, 1.000000000000000000 ),
 ( 0.000000000000000000, 1.000000000000000000 ),
 .UNSPECIFIED. ) 
 GEOMETRIC_REPRESENTATION_ITEM ( )  RATIONAL_B_SPLINE_SURFACE ( (
 ( 1.000000000000000000, 1.000000000000000000),
 ( 0.9933953342250436691, 0.8357391271907733676),
 ( 0.9933953342250436691, 0.8357391271907733676),
 ( 1.000000000000000000, 1.000000000000000000) ) ) 
 REPRESENTATION_ITEM ( '' )  SURFACE ( )  );
#9225=CARTESIAN_POINT ( 'NONE',  ( 1.847168016377982669, 7.161712042621604546, -10.17509564929251020 ) ) ;
#9230=EDGE_LOOP ( 'NONE', ( #8, #17889, #4039, #16889 ) ) ;
#9231=ORIENTED_EDGE ( 'NONE', *, *, #16587, .T. ) ;
#9236=CARTESIAN_POINT ( 'NONE',  ( 2.697797270744668463, -12.33058466479264936, -4.970631985779717432 ) ) ;
#9239=EDGE_CURVE ( 'NONE', #16984, #6765, #18220, .T. ) ;
#9244=DIRECTION ( 'NONE',  ( 0.000000000000000000, 0.000000000000000000, 1.000000000000000000 ) ) ;
#9246=CARTESIAN_POINT ( 'NONE',  ( 0.3137051932979809665, 10.83767969834803324, 8.442169467526891680 ) ) ;
#9247=CARTESIAN_POINT ( 'NONE',  ( 8.522092701127531811, -0.3779863304870734741, -6.946128462138600135 ) ) ;
#9248=FACE_OUTER_BOUND ( 'NONE', #18172, .T. ) ;
#9261=CARTESIAN_POINT ( 'NONE',  ( 0.4862570985993235340, 3.580942890621860109, -13.44146924561377254 ) ) ;
#9263=EDGE_CURVE ( 'NONE', #5420, #7234, #15237, .T. ) ;
#9264=CARTESIAN_POINT ( 'NONE',  ( 0.3148208552358988666, 13.13564827777588917, 4.026279359288469806 ) ) ;
#9267=CARTESIAN_POINT ( 'NONE',  ( 0.3720661004400037664, 12.89739157014192550, 4.951033743989683877 ) ) ;
#9269=CARTESIAN_POINT ( 'NONE',  ( 0.4862570985993235340, 8.769551628660890330, -10.79774104611363761 ) ) ;
#9270=CARTESIAN_POINT ( 'NONE',  ( 0.3151928479966097374, 0.000000000000000000, -13.73922861026898623 ) ) ;
#9274=ORIENTED_EDGE ( 'NONE', *, *, #17142, .F. ) ;
#9278=CARTESIAN_POINT ( 'NONE',  ( 0.4862570985993235340, 10.79774104611385965, -8.769551628660616771 ) ) ;
#9283=LINE ( 'NONE', #2032, #6938 ) ;
#9285=CARTESIAN_POINT ( 'NONE',  ( 0.3132635586635981184, -8.495712071659319520, -10.79541209008113256 ) ) ;
#9286=CARTESIAN_POINT ( 'NONE',  ( 1.847247051441589960, 10.16425585218611083, -7.177495230324590025 ) ) ;
#9297=CARTESIAN_POINT ( 'NONE',  ( 1.342453679581834924, -11.38190519890846453, -9.456403821038923851 ) ) ;
#9299=CARTESIAN_POINT ( 'NONE',  ( 3.950837973638676281, 13.10350451991840615, 6.316429227969512894 ) ) ;
#9301=( BOUNDED_SURFACE ( )  B_SPLINE_SURFACE ( 3, 1, ( 
 ( #11441, #14393 ),
 ( #1300, #14582 ),
 ( #1500, #1400 ),
 ( #2811, #8763 ) ),
 .UNSPECIFIED., .F., .F., .T. ) 
 B_SPLINE_SURFACE_WITH_KNOTS ( ( 4, 4 ),
 ( 2, 2 ),
 ( 0.000000000000000000, 1.000000000000000000 ),
 ( 0.000000000000000000, 1.000000000000000000 ),
 .UNSPECIFIED. ) 
 GEOMETRIC_REPRESENTATION_ITEM ( )  RATIONAL_B_SPLINE_SURFACE ( (
 ( 1.000000000000000000, 1.000000000000000000),
 ( 0.9593108457356467333, 0.9995965569486454649),
 ( 0.9593108457356467333, 0.9995965569486454649),
 ( 1.000000000000000000, 1.000000000000000000) ) ) 
 REPRESENTATION_ITEM ( '' )  SURFACE ( )  );
#9308=DIRECTION ( 'NONE',  ( 0.000000000000000000, 0.000000000000000000, 1.000000000000000000 ) ) ;
#9309=ORIENTED_EDGE ( 'NONE', *, *, #4609, .F. ) ;
#9311=LINE ( 'NONE', #15143, #6411 ) ;
#9318=CARTESIAN_POINT ( 'NONE',  ( 0.4862570985993252548, 12.97920246947879441, 5.003653737315533867 ) ) ;
#9319=CARTESIAN_POINT ( 'NONE',  ( 2.002547531651519996, -0.6781519942170860515, -12.57989064830760206 ) ) ;
#9321=CARTESIAN_POINT ( 'NONE',  ( 0.3308579732647032867, -11.46737410776358779, 7.595989242675092790 ) ) ;
#9323=ORIENTED_EDGE ( 'NONE', *, *, #4445, .T. ) ;
#9324=VECTOR ( 'NONE', #18198, 1000.000000000000000 ) ;
#9326=CARTESIAN_POINT ( 'NONE',  ( 1.847461586945730261, 7.286856109515200686, -10.08650590720928619 ) ) ;
#9329=CARTESIAN_POINT ( 'NONE',  ( 1.847372867223024295, -11.86627781945711568, 3.744745203533932365 ) ) ;
#9330=LINE ( 'NONE', #18301, #6931 ) ;
#9331=ORIENTED_EDGE ( 'NONE', *, *, #5354, .F. ) ;
#9332=EDGE_CURVE ( 'NONE', #17964, #3017, #8430, .T. ) ;
#9335=ORIENTED_EDGE ( 'NONE', *, *, #5861, .T. ) ;
#9336=VERTEX_POINT ( 'NONE', #12735 ) ;
#9340=CARTESIAN_POINT ( 'NONE',  ( 1.847168016377981559, -12.44137401948661648, 0.1868244120189130053 ) ) ;
#9342=CARTESIAN_POINT ( 'NONE',  ( 1.918918678667045352, 9.738328798462491775, -7.860057224348732774 ) ) ;
#9349=ORIENTED_EDGE ( 'NONE', *, *, #8846, .F. ) ;
#9352=ORIENTED_EDGE ( 'NONE', *, *, #10158, .F. ) ;
#9354=EDGE_CURVE ( 'NONE', #13704, #17922, #7294, .T. ) ;
#9358=CARTESIAN_POINT ( 'NONE',  ( 0.4754618798421171855, 11.68486377711966639, 7.564402563418515690 ) ) ;
#9359=CARTESIAN_POINT ( 'NONE',  ( 1.846138399168762101, -7.646096044339819819, -9.815003036200495856 ) ) ;
#9362=ORIENTED_EDGE ( 'NONE', *, *, #15381, .F. ) ;
#9366=CARTESIAN_POINT ( 'NONE',  ( 1.845755665166726844, 11.67596932341234250, 4.296872077620717434 ) ) ;
#9373=FACE_OUTER_BOUND ( 'NONE', #12562, .T. ) ;
#9376=VECTOR ( 'NONE', #2240, 1000.000000000000114 ) ;
#9379=EDGE_CURVE ( 'NONE', #14747, #16257, #15698, .T. ) ;
#9383=CARTESIAN_POINT ( 'NONE',  ( 3.353306896162456585, 5.573563251762281290, -12.78841260990232165 ) ) ;
#9386=ORIENTED_EDGE ( 'NONE', *, *, #3071, .F. ) ;
#9387=CARTESIAN_POINT ( 'NONE',  ( 16.56679352167444819, -0.008252760440870216679, 0.004277682826583264174 ) ) ;
#9388=FACE_OUTER_BOUND ( 'NONE', #14870, .T. ) ;
#9389=CARTESIAN_POINT ( 'NONE',  ( 1.845755665166724846, -11.67596932341231231, -4.296872077620800034 ) ) ;
#9392=CARTESIAN_POINT ( 'NONE',  ( 0.3137051932979792457, -7.698472063774386420, -11.37800749014139612 ) ) ;
#9399=CARTESIAN_POINT ( 'NONE',  ( 0.3150686449036074754, -11.20479228691391604, -7.951193823202520328 ) ) ;
#9405=CARTESIAN_POINT ( 'NONE',  ( 2.697797270744668019, -7.053988368581781465, -11.26906156738834675 ) ) ;
#9408=CARTESIAN_POINT ( 'NONE',  ( 0.3058872367615230181, 13.24582953854925371, 3.664492643742809364 ) ) ;
#9412=CARTESIAN_POINT ( 'NONE',  ( 3.512766787570729576, 7.127386085303022867, -13.25664064834469613 ) ) ;
#9417=CARTESIAN_POINT ( 'NONE',  ( 1.861706995891666105, 3.332865258614144732, -12.00328602385076593 ) ) ;
#9422=CARTESIAN_POINT ( 'NONE',  ( 1.918918678667074440, 12.49849921341423276, -0.6348738215465657975 ) ) ;
#9425=VERTEX_POINT ( 'NONE', #4611 ) ;
#9431=EDGE_LOOP ( 'NONE', ( #10205, #2530, #9075, #1493 ) ) ;
#9432=B_SPLINE_CURVE_WITH_KNOTS ( 'NONE', 3,
 ( #18349, #15387, #3823, #9383, #7962, #866 ),
 .UNSPECIFIED., .F., .F.,
 ( 4, 2, 4 ),
 ( 0.000000000000000000, 0.001500839035891551355, 0.003001678071783102711 ),
 .UNSPECIFIED. ) ;
#9434=CARTESIAN_POINT ( 'NONE',  ( 0.3145729642390391323, 11.29233589755992639, 7.825496023201352180 ) ) ;
#9440=CARTESIAN_POINT ( 'NONE',  ( 1.254009781011253821, 14.24044713813288254, 3.563484327698356324 ) ) ;
#9442=B_SPLINE_CURVE_WITH_KNOTS ( 'NONE', 3,
 ( #2192, #7946, #9725, #3528, #2107, #667 ),
 .UNSPECIFIED., .F., .F.,
 ( 4, 2, 4 ),
 ( 5.421010862427522170E-20, 0.0001828790815886950779, 0.0003657581631773901016 ),
 .UNSPECIFIED. ) ;
#9448=ORIENTED_EDGE ( 'NONE', *, *, #8910, .F. ) ;
#9449=B_SPLINE_CURVE_WITH_KNOTS ( 'NONE', 3,
 ( #10323, #16151, #3033, #8881, #1620, #7464 ),
 .UNSPECIFIED., .F., .F.,
 ( 4, 2, 4 ),
 ( 7.047314121155778821E-19, 0.001657017934712349183, 0.003314035869424697932 ),
 .UNSPECIFIED. ) ;
#9451=CARTESIAN_POINT ( 'NONE',  ( 1.342453679581834924, 12.51077660954477189, -7.902645620902311485 ) ) ;
#9455=CARTESIAN_POINT ( 'NONE',  ( 0.3132635586635996727, 13.21855946425836592, 3.740017578711807289 ) ) ;
#9456=EDGE_LOOP ( 'NONE', ( #13976, #8712, #11857, #9119 ) ) ;
#9468=CARTESIAN_POINT ( 'NONE',  ( 1.846524061778019421, 11.93805390544205913, -3.506196582970981357 ) ) ;
#9469=ORIENTED_EDGE ( 'NONE', *, *, #700, .F. ) ;
#9470=CARTESIAN_POINT ( 'NONE',  ( 1.861706995891668326, 11.66987142852990189, -4.359009869687124450 ) ) ;
#9471=ORIENTED_EDGE ( 'NONE', *, *, #1262, .F. ) ;
#9472=CARTESIAN_POINT ( 'NONE',  ( 1.847168016377986000, -4.022276579849877187, -11.77471791462002670 ) ) ;
#9475=VERTEX_POINT ( 'NONE', #406 ) ;
#9476=CARTESIAN_POINT ( 'NONE',  ( 1.847372867223025406, -7.398914411685061587, 10.00438561114521185 ) ) ;
#9478=CARTESIAN_POINT ( 'NONE',  ( 1.846138399168762101, -11.69739621335919111, -4.238866729160527314 ) ) ;
#9480=ADVANCED_FACE ( 'NONE', ( #16073 ), #13195, .F. ) ;
#9482=EDGE_CURVE ( 'NONE', #31, #3117, #1352, .T. ) ;
#9484=CARTESIAN_POINT ( 'NONE',  ( 0.3720661004400040439, -10.73619472937708252, 8.694226082900557984 ) ) ;
#9486=ORIENTED_EDGE ( 'NONE', *, *, #13170, .F. ) ;
#9489=CARTESIAN_POINT ( 'NONE',  ( 1.959212340397942231, 12.12975361829680310, -3.239239832448903122 ) ) ;
#9492=ORIENTED_EDGE ( 'NONE', *, *, #4123, .T. ) ;
#9500=CARTESIAN_POINT ( 'NONE',  ( 2.320521194582656932, -14.32454473829943886, 6.542541239685230714 ) ) ;
#9504=CARTESIAN_POINT ( 'NONE',  ( 1.254255976357895763, -3.563435620217493494, -14.24071337840814166 ) ) ;
#9506=CARTESIAN_POINT ( 'NONE',  ( 0.3137051932979792457, 7.698472063774471685, 11.37800749014133928 ) ) ;
#9510=FACE_OUTER_BOUND ( 'NONE', #11819, .T. ) ;
#9514=ORIENTED_EDGE ( 'NONE', *, *, #9379, .F. ) ;
#9516=VERTEX_POINT ( 'NONE', #9658 ) ;
#9517=CARTESIAN_POINT ( 'NONE',  ( 0.3132635586635976188, 0.5277914263193109745, 13.72732610560088773 ) ) ;
#9523=CARTESIAN_POINT ( 'NONE',  ( 3.664313757352973600, -12.42002390572631221, 7.012524439851453906 ) ) ;
#9524=CARTESIAN_POINT ( 'NONE',  ( 2.705023505549862151, -12.88681800078730255, -3.294610156756031305 ) ) ;
#9531=ORIENTED_EDGE ( 'NONE', *, *, #6837, .T. ) ;
#9534=CARTESIAN_POINT ( 'NONE',  ( 3.664313757352971379, -1.627055439596372777, 14.16986885736092461 ) ) ;
#9535=CARTESIAN_POINT ( 'NONE',  ( 1.846822687350015757, -7.075150813727044685, -10.23524390843947529 ) ) ;
#9538=CARTESIAN_POINT ( 'NONE',  ( 16.56782317627811096, 0.0003415813796006246777, -0.009814734722107084502 ) ) ;
#9543=CARTESIAN_POINT ( 'NONE',  ( 2.636624412716061627, -7.605649742761058540, -14.14563173255469408 ) ) ;
#9545=CARTESIAN_POINT ( 'NONE',  ( 3.950837973638675393, -13.10350451991835818, -6.316429227969608817 ) ) ;
#9549=ORIENTED_EDGE ( 'NONE', *, *, #13607, .T. ) ;
#9556=VERTEX_POINT ( 'NONE', #7969 ) ;
#9560=CARTESIAN_POINT ( 'NONE',  ( 3.074695600507237891, -15.41438262616227739, 2.093687500611889352 ) ) ;
#9562=CARTESIAN_POINT ( 'NONE',  ( 0.3307726912345178572, 7.596084275799059427, -11.46720933246390572 ) ) ;
#9563=CARTESIAN_POINT ( 'NONE',  ( 1.847412631396500249, 10.09191835241973934, -7.278870946904142158 ) ) ;
#9566=VECTOR ( 'NONE', #10091, 1000.000000000000114 ) ;
#9567=CARTESIAN_POINT ( 'NONE',  ( 2.747332970342022840, -14.63517873738952524, 7.289199830147050641 ) ) ;
#9568=( BOUNDED_SURFACE ( )  B_SPLINE_SURFACE ( 3, 1, ( 
 ( #4595, #3135 ),
 ( #10418, #3607 ),
 ( #835, #5036 ),
 ( #1822, #16254 ) ),
 .UNSPECIFIED., .F., .F., .T. ) 
 B_SPLINE_SURFACE_WITH_KNOTS ( ( 4, 4 ),
 ( 2, 2 ),
 ( 0.000000000000000000, 1.000000000000000000 ),
 ( 0.000000000000000000, 1.000000000000000000 ),
 .UNSPECIFIED. ) 
 GEOMETRIC_REPRESENTATION_ITEM ( )  RATIONAL_B_SPLINE_SURFACE ( (
 ( 1.000000000000000000, 1.000000000000000000),
 ( 0.9593108457356467333, 0.9995965569486454649),
 ( 0.9593108457356467333, 0.9995965569486454649),
 ( 1.000000000000000000, 1.000000000000000000) ) ) 
 REPRESENTATION_ITEM ( '' )  SURFACE ( )  );
#9588=CARTESIAN_POINT ( 'NONE',  ( 3.950837973638676281, 1.958075594453990487, -14.41405733518058341 ) ) ;
#9595=CARTESIAN_POINT ( 'NONE',  ( 0.3170788640506440603, -4.392045232375903829, 13.02120094575826670 ) ) ;
#9600=ORIENTED_EDGE ( 'NONE', *, *, #9217, .T. ) ;
#9609=CARTESIAN_POINT ( 'NONE',  ( 16.56753206892534891, 0.001549402974394163733, 0.009369540855502535986 ) ) ;
#9612=CIRCLE ( 'NONE', #12069, 16.06066017081991149 ) ;
#9614=CARTESIAN_POINT ( 'NONE',  ( 0.3137051932979757485, 13.73004976592202020, -0.4596302728640235258 ) ) ;
#9615=CARTESIAN_POINT ( 'NONE',  ( 0.4862570985993235340, -7.559321496869339185, -11.67702470553373750 ) ) ;
#9617=CARTESIAN_POINT ( 'NONE',  ( 2.353870697619109720, 10.90705766126230536, -6.980654702310723714 ) ) ;
#9621=CIRCLE ( 'NONE', #13906, 14.54644660717763927 ) ;
#9624=B_SPLINE_CURVE_WITH_KNOTS ( 'NONE', 3,
 ( #5719, #11040, #15326, #897, #9500, #13089 ),
 .UNSPECIFIED., .F., .F.,
 ( 4, 2, 4 ),
 ( 1.305552300251627978E-18, 0.001657017934710633541, 0.003314035869421265781 ),
 .UNSPECIFIED. ) ;
#9626=EDGE_CURVE ( 'NONE', #13108, #1712, #1107, .T. ) ;
#9627=CARTESIAN_POINT ( 'NONE',  ( 0.3058872367615226295, -13.24582953854928036, 3.664492643742712108 ) ) ;
#9630=CARTESIAN_POINT ( 'NONE',  ( 16.57210152137263393, 0.01453130299868640209, -0.0006600038696348341314 ) ) ;
#9632=CARTESIAN_POINT ( 'NONE',  ( 16.56782317627811096, 0.0003415813796014688375, 0.009814734722106369796 ) ) ;
#9636=CARTESIAN_POINT ( 'NONE',  ( 2.636624412714236865, 0.000000000000000000, 0.000000000000000000 ) ) ;
#9651=CIRCLE ( 'NONE', #12108, 14.54644660717763927 ) ;
#9654=ORIENTED_EDGE ( 'NONE', *, *, #12824, .T. ) ;
#9658=CARTESIAN_POINT ( 'NONE',  ( 0.3137051932979792457, -8.442169467526928983, 10.83767969834800127 ) ) ;
#9660=VECTOR ( 'NONE', #11003, 1000.000000000000114 ) ;
#9661=B_SPLINE_CURVE_WITH_KNOTS ( 'NONE', 3,
 ( #1406, #16128, #7538, #18889 ),
 .UNSPECIFIED., .F., .F.,
 ( 4, 4 ),
 ( 0.000000000000000000, 0.002004993803841946618 ),
 .UNSPECIFIED. ) ;
#9666=DIRECTION ( 'NONE',  ( 0.000000000000000000, 0.000000000000000000, 1.000000000000000000 ) ) ;
#9669=CARTESIAN_POINT ( 'NONE',  ( 0.3095370825347224519, -11.38092634279622928, -7.700448427571997989 ) ) ;
#9671=CARTESIAN_POINT ( 'NONE',  ( 0.3145729642390400205, -11.29233589755986600, -7.825496023201434781 ) ) ;
#9675=LINE ( 'NONE', #12625, #7838 ) ;
#9679=CARTESIAN_POINT ( 'NONE',  ( 1.861706995891673433, -0.5394761475744983548, -12.44571539481144562 ) ) ;
#9681=CARTESIAN_POINT ( 'NONE',  ( 1.918918678667043354, 10.48466773720562273, 6.832809802519053122 ) ) ;
#9685=EDGE_CURVE ( 'NONE', #9139, #7697, #8205, .T. ) ;
#9688=( BOUNDED_SURFACE ( )  B_SPLINE_SURFACE ( 3, 1, ( 
 ( #6239, #4989 ),
 ( #4811, #1846 ),
 ( #9106, #17809 ),
 ( #6528, #4712 ) ),
 .UNSPECIFIED., .F., .F., .T. ) 
 B_SPLINE_SURFACE_WITH_KNOTS ( ( 4, 4 ),
 ( 2, 2 ),
 ( 0.000000000000000000, 1.000000000000000000 ),
 ( 0.000000000000000000, 1.000000000000000000 ),
 .UNSPECIFIED. ) 
 GEOMETRIC_REPRESENTATION_ITEM ( )  RATIONAL_B_SPLINE_SURFACE ( (
 ( 1.000000000000000000, 1.000000000000000000),
 ( 0.7792777138730160313, 0.9689936506012927220),
 ( 0.7792777138730160313, 0.9689936506012927220),
 ( 1.000000000000000000, 1.000000000000000000) ) ) 
 REPRESENTATION_ITEM ( '' )  SURFACE ( )  );
#9691=EDGE_CURVE ( 'NONE', #17807, #18257, #13201, .T. ) ;
#9692=CARTESIAN_POINT ( 'NONE',  ( 0.3058872367615226295, -12.87003593440624982, -4.821066432589462103 ) ) ;
#9695=LINE ( 'NONE', #6829, #2945 ) ;
#9696=CARTESIAN_POINT ( 'NONE',  ( 1.342453679581834924, -5.476372339890114738, 13.74702459364882401 ) ) ;
#9697=VERTEX_POINT ( 'NONE', #17290 ) ;
#9698=ORIENTED_EDGE ( 'NONE', *, *, #6572, .F. ) ;
#9699=ORIENTED_EDGE ( 'NONE', *, *, #13982, .F. ) ;
#9702=LINE ( 'NONE', #10967, #11784 ) ;
#9704=CARTESIAN_POINT ( 'NONE',  ( 16.56822296793089322, -0.006547366384936689071, -0.007741272030791150442 ) ) ;
#9705=CARTESIAN_POINT ( 'NONE',  ( 16.57210152137263393, -0.01361613799508957709, 0.005118120558002058063 ) ) ;
#9707=EDGE_CURVE ( 'NONE', #9813, #7378, #5238, .T. ) ;
#9709=EDGE_CURVE ( 'NONE', #2485, #1319, #3814, .T. ) ;
#9711=B_SPLINE_CURVE_WITH_KNOTS ( 'NONE', 3,
 ( #6475, #6665, #9149, #10880 ),
 .UNSPECIFIED., .F., .F.,
 ( 4, 4 ),
 ( 1.779952243785056044E-16, 0.002004993803842976610 ),
 .UNSPECIFIED. ) ;
#9712=CARTESIAN_POINT ( 'NONE',  ( 2.123976203522053297, 10.37815841598508371, -11.67822624909914175 ) ) ;
#9713=FACE_OUTER_BOUND ( 'NONE', #504, .T. ) ;
#9720=CARTESIAN_POINT ( 'NONE',  ( 2.123976203522053297, 13.47898556379324297, -7.899625852120059299 ) ) ;
#9725=CARTESIAN_POINT ( 'NONE',  ( 1.861628059977344263, -0.5393144007391119654, 12.44564375541076728 ) ) ;
#9726=CARTESIAN_POINT ( 'NONE',  ( 0.4862570985993235340, 11.67702470553376060, -7.559321496869298329 ) ) ;
#9733=ORIENTED_EDGE ( 'NONE', *, *, #5672, .T. ) ;
#9734=ADVANCED_FACE ( 'NONE', ( #9934 ), #9896, .F. ) ;
#9737=AXIS2_PLACEMENT_3D ( 'NONE', #2301, #8327, #15663 ) ;
#9742=CARTESIAN_POINT ( 'NONE',  ( 1.846138399168762101, -4.238866729160323032, -11.69739621335926394 ) ) ;
#9746=CARTESIAN_POINT ( 'NONE',  ( 0.4862570985993235340, 0.7479633556562450547, 13.89016912371017831 ) ) ;
#9748=CARTESIAN_POINT ( 'NONE',  ( 3.074695600507260984, -10.75417554975707013, 11.23985886659431621 ) ) ;
#9752=DIRECTION ( 'NONE',  ( -1.000000000000000000, -0.000000000000000000, -0.000000000000000000 ) ) ;
#9757=CARTESIAN_POINT ( 'NONE',  ( 1.977436885025011470, 11.52792723756289206, 10.21547824869447219 ) ) ;
#9761=CARTESIAN_POINT ( 'NONE',  ( 16.57778382496167424, 0.001819584982831899374, -0.01482878558584570412 ) ) ;
#9765=CARTESIAN_POINT ( 'NONE',  ( 1.846138399168762989, 10.30487220521570357, 6.971848976711047641 ) ) ;
#9767=CARTESIAN_POINT ( 'NONE',  ( 1.846138399168762101, -9.815003036200465658, 7.646096044339859787 ) ) ;
#9784=( BOUNDED_SURFACE ( )  B_SPLINE_SURFACE ( 3, 1, ( 
 ( #4995, #2854 ),
 ( #17306, #3937 ),
 ( #14153, #17399 ),
 ( #11217, #14438 ) ),
 .UNSPECIFIED., .F., .F., .T. ) 
 B_SPLINE_SURFACE_WITH_KNOTS ( ( 4, 4 ),
 ( 2, 2 ),
 ( 0.000000000000000000, 1.000000000000000000 ),
 ( 0.000000000000000000, 1.000000000000000000 ),
 .UNSPECIFIED. ) 
 GEOMETRIC_REPRESENTATION_ITEM ( )  RATIONAL_B_SPLINE_SURFACE ( (
 ( 1.000000000000000000, 1.000000000000000000),
 ( 0.9593108457356467333, 0.9995965569486454649),
 ( 0.9593108457356467333, 0.9995965569486454649),
 ( 1.000000000000000000, 1.000000000000000000) ) ) 
 REPRESENTATION_ITEM ( '' )  SURFACE ( )  );
#9787=CARTESIAN_POINT ( 'NONE',  ( 3.950837973638676281, -6.316429227969383220, -13.10350451991847009 ) ) ;
#9790=CARTESIAN_POINT ( 'NONE',  ( 1.342453679581834924, 0.9602753779832786662, -14.76648944001038188 ) ) ;
#9800=CARTESIAN_POINT ( 'NONE',  ( 16.56753206892534891, 0.001549402974393146101, -0.009369540855502138735 ) ) ;
#9802=CARTESIAN_POINT ( 'NONE',  ( 2.123976203522053297, -3.347755036805797779, -15.26039569100262838 ) ) ;
#9804=CARTESIAN_POINT ( 'NONE',  ( 0.3095370825347234511, 8.444334731364163460, -10.84046130709049294 ) ) ;
#9813=VERTEX_POINT ( 'NONE', #13086 ) ;
#9819=ADVANCED_FACE ( 'NONE', ( #1435 ), #15166, .F. ) ;
#9821=ORIENTED_EDGE ( 'NONE', *, *, #13673, .T. ) ;
#9823=CARTESIAN_POINT ( 'NONE',  ( 3.512766787570980931, 13.55823433651926280, 6.535475144496921907 ) ) ;
#9826=B_SPLINE_CURVE_WITH_KNOTS ( 'NONE', 3,
 ( #5272, #11116, #15499, #2399, #6809, #14068 ),
 .UNSPECIFIED., .F., .F.,
 ( 4, 2, 4 ),
 ( 0.000000000000000000, 0.0001828790815886940750, 0.0003657581631773881500 ),
 .UNSPECIFIED. ) ;
#9833=CARTESIAN_POINT ( 'NONE',  ( 2.636624412716062960, -2.161493821598612808, -15.91454522070331912 ) ) ;
#9836=LINE ( 'NONE', #2477, #9853 ) ;
#9840=CARTESIAN_POINT ( 'NONE',  ( 0.3170788640506441158, -11.20690911610897800, -7.952793437297696499 ) ) ;
#9842=ORIENTED_EDGE ( 'NONE', *, *, #13607, .F. ) ;
#9845=B_SPLINE_CURVE_WITH_KNOTS ( 'NONE', 3,
 ( #6413, #2373, #7853, #12242 ),
 .UNSPECIFIED., .F., .F.,
 ( 4, 4 ),
 ( 7.039312503357838248E-16, 0.002004993803841917561 ),
 .UNSPECIFIED. ) ;
#9847=DIRECTION ( 'NONE',  ( -1.000000000000000000, -0.000000000000000000, -0.000000000000000000 ) ) ;
#9851=CARTESIAN_POINT ( 'NONE',  ( 2.002547531651519996, 7.942910686618313676, -9.778737580845612953 ) ) ;
#9853=VECTOR ( 'NONE', #1051, 1000.000000000000227 ) ;
#9857=CARTESIAN_POINT ( 'NONE',  ( 16.56822296793089322, 0.009385634690642057770, -0.003834730849371914118 ) ) ;
#9858=ORIENTED_EDGE ( 'NONE', *, *, #13692, .F. ) ;
#9859=CARTESIAN_POINT ( 'NONE',  ( 1.846613052777650976, 0.3401093050881815461, 12.43780859207239864 ) ) ;
#9860=CARTESIAN_POINT ( 'NONE',  ( 1.846138399168762101, -0.4167076046094680408, -12.43476674860266940 ) ) ;
#9872=CARTESIAN_POINT ( 'NONE',  ( 3.950837973638675393, -10.05648675950118509, -10.51028938476228980 ) ) ;
#9873=EDGE_CURVE ( 'NONE', #381, #12288, #4009, .T. ) ;
#9875=ORIENTED_EDGE ( 'NONE', *, *, #12678, .T. ) ;
#9876=ADVANCED_FACE ( 'NONE', ( #12705 ), #11869, .F. ) ;
#9879=CARTESIAN_POINT ( 'NONE',  ( 1.847380140988742703, -10.13114603776191380, -7.224522571381438496 ) ) ;
#9881=CARTESIAN_POINT ( 'NONE',  ( 2.320521194582656488, -7.743190876766163022, 13.71278319228045284 ) ) ;
#9887=CARTESIAN_POINT ( 'NONE',  ( 16.57778382496167424, 0.01306626476309378365, 0.007244066302947740205 ) ) ;
#9888=CARTESIAN_POINT ( 'NONE',  ( 1.846138399168762101, 6.971848976711159551, -10.30487220521562541 ) ) ;
#9889=EDGE_CURVE ( 'NONE', #349, #11883, #15489, .T. ) ;
#9896=( BOUNDED_SURFACE ( )  B_SPLINE_SURFACE ( 3, 1, ( 
 ( #6797, #2751 ),
 ( #15762, #18443 ),
 ( #8414, #4212 ),
 ( #15863, #11201 ) ),
 .UNSPECIFIED., .F., .F., .T. ) 
 B_SPLINE_SURFACE_WITH_KNOTS ( ( 4, 4 ),
 ( 2, 2 ),
 ( 0.000000000000000000, 1.000000000000000000 ),
 ( 0.000000000000000000, 1.000000000000000000 ),
 .UNSPECIFIED. ) 
 GEOMETRIC_REPRESENTATION_ITEM ( )  RATIONAL_B_SPLINE_SURFACE ( (
 ( 1.000000000000000000, 1.000000000000000000),
 ( 0.7792777138730158093, 0.9689936506012928330),
 ( 0.7792777138730158093, 0.9689936506012928330),
 ( 1.000000000000000000, 1.000000000000000000) ) ) 
 REPRESENTATION_ITEM ( '' )  SURFACE ( )  );
#9898=CARTESIAN_POINT ( 'NONE',  ( 2.636624412714994037, -14.46769361191274328, -6.973567714907344950 ) ) ;
#9900=B_SPLINE_CURVE_WITH_KNOTS ( 'NONE', 3,
 ( #8488, #2730, #6867, #14499 ),
 .UNSPECIFIED., .F., .F.,
 ( 4, 4 ),
 ( 0.000000000000000000, 0.002004993803842703825 ),
 .UNSPECIFIED. ) ;
#9901=CARTESIAN_POINT ( 'NONE',  ( 3.950837973638668288, 0.000000000000000000, 0.000000000000000000 ) ) ;
#9904=FACE_OUTER_BOUND ( 'NONE', #14674, .T. ) ;
#9913=ADVANCED_FACE ( 'NONE', ( #11196 ), #15725, .T. ) ;
#9916=CIRCLE ( 'NONE', #6889, 16.06066017081991149 ) ;
#9918=ORIENTED_EDGE ( 'NONE', *, *, #8668, .T. ) ;
#9919=CARTESIAN_POINT ( 'NONE',  ( 2.636624412715999011, 2.161493821598055920, -15.91454522070273647 ) ) ;
#9924=DIRECTION ( 'NONE',  ( 0.000000000000000000, 0.000000000000000000, 1.000000000000000000 ) ) ;
#9934=FACE_OUTER_BOUND ( 'NONE', #12499, .T. ) ;
#9936=EDGE_CURVE ( 'NONE', #3961, #6426, #3407, .T. ) ;
#9940=EDGE_CURVE ( 'NONE', #13630, #10260, #12976, .T. ) ;
#9941=CARTESIAN_POINT ( 'NONE',  ( 16.57210152137263393, -0.01453130299868639515, 0.0006600038696349324685 ) ) ;
#9944=FACE_OUTER_BOUND ( 'NONE', #18210, .T. ) ;
#9956=ORIENTED_EDGE ( 'NONE', *, *, #3093, .F. ) ;
#9961=CARTESIAN_POINT ( 'NONE',  ( 0.3148213771069329203, -13.13560149728604109, 4.026433757158931925 ) ) ;
#9962=CARTESIAN_POINT ( 'NONE',  ( 2.002547531651519996, 12.17374746633582561, -3.242439124566524278 ) ) ;
#9965=VERTEX_POINT ( 'NONE', #18582 ) ;
#9966=CARTESIAN_POINT ( 'NONE',  ( 1.977228804422197062, -15.04020501276157518, -3.321884655131998265 ) ) ;
#9968=ORIENTED_EDGE ( 'NONE', *, *, #3408, .F. ) ;
#9972=CARTESIAN_POINT ( 'NONE',  ( 0.3095370825347224519, -8.444334731364081748, 10.84046130709055689 ) ) ;
#9976=EDGE_LOOP ( 'NONE', ( #2844, #16762, #1421, #14525 ) ) ;
#9977=EDGE_CURVE ( 'NONE', #10089, #10024, #15617, .T. ) ;
#9980=CARTESIAN_POINT ( 'NONE',  ( 0.4754618798421162973, -0.7484603771385398563, 13.89949764182682301 ) ) ;
#9986=CARTESIAN_POINT ( 'NONE',  ( 2.636624412715137922, -15.91454522070252153, 2.161493821597598508 ) ) ;
#9988=ADVANCED_FACE ( 'NONE', ( #16974 ), #13816, .F. ) ;
#9989=EDGE_CURVE ( 'NONE', #12131, #7670, #11174, .T. ) ;
#9992=VERTEX_POINT ( 'NONE', #15811 ) ;
#9993=ORIENTED_EDGE ( 'NONE', *, *, #11617, .F. ) ;
#9998=ORIENTED_EDGE ( 'NONE', *, *, #16515, .F. ) ;
#10003=CARTESIAN_POINT ( 'NONE',  ( 0.3148208552358952028, -10.97826876274317875, 8.260375059853302560 ) ) ;
#10004=CONICAL_SURFACE ( 'NONE', #1783, 14.54644660717763927, 0.8559913436420816257 ) ;
#10008=CARTESIAN_POINT ( 'NONE',  ( 1.847034903785829574, -4.063013886994788493, 11.76058231742743665 ) ) ;
#10010=( BOUNDED_SURFACE ( )  B_SPLINE_SURFACE ( 3, 1, ( 
 ( #3751, #15410 ),
 ( #9761, #7093 ),
 ( #8343, #11307 ),
 ( #15679, #13004 ) ),
 .UNSPECIFIED., .F., .F., .T. ) 
 B_SPLINE_SURFACE_WITH_KNOTS ( ( 4, 4 ),
 ( 2, 2 ),
 ( 0.000000000000000000, 1.000000000000000000 ),
 ( 0.000000000000000000, 1.000000000000000000 ),
 .UNSPECIFIED. ) 
 GEOMETRIC_REPRESENTATION_ITEM ( )  RATIONAL_B_SPLINE_SURFACE ( (
 ( 1.000000000000000000, 1.000000000000000000),
 ( 0.7792777138730158093, 0.9689936506012928330),
 ( 0.7792777138730158093, 0.9689936506012928330),
 ( 1.000000000000000000, 1.000000000000000000) ) ) 
 REPRESENTATION_ITEM ( '' )  SURFACE ( )  );
#10018=ORIENTED_EDGE ( 'NONE', *, *, #17191, .F. ) ;
#10024=VERTEX_POINT ( 'NONE', #2708 ) ;
#10029=CARTESIAN_POINT ( 'NONE',  ( 0.3137051932979792457, -13.20008686438103140, -3.805684345189927154 ) ) ;
#10030=CARTESIAN_POINT ( 'NONE',  ( 0.3132635586635994507, -3.740017578711855695, 13.21855946425835882 ) ) ;
#10036=DIRECTION ( 'NONE',  ( 0.7561779333270775005, 0.6106991889125038542, 0.2350349629540249285 ) ) ;
#10039=ORIENTED_EDGE ( 'NONE', *, *, #3886, .T. ) ;
#10043=CARTESIAN_POINT ( 'NONE',  ( 1.847168016377981781, 10.17509564929258836, 7.161712042621497076 ) ) ;
#10051=VECTOR ( 'NONE', #18619, 1000.000000000000000 ) ;
#10057=B_SPLINE_CURVE_WITH_KNOTS ( 'NONE', 3,
 ( #3746, #12266, #16754, #6352, #10650, #3659 ),
 .UNSPECIFIED., .F., .F.,
 ( 4, 2, 4 ),
 ( 3.229102830436655475E-17, 0.0001825746017570572058, 0.0003651492035140821565 ),
 .UNSPECIFIED. ) ;
#10061=CARTESIAN_POINT ( 'NONE',  ( 2.002547531651519996, 0.6781519942171739812, 12.57989064830759851 ) ) ;
#10062=CARTESIAN_POINT ( 'NONE',  ( 1.847247051441592625, 3.685275815977189673, 11.88474976472813971 ) ) ;
#10067=ORIENTED_EDGE ( 'NONE', *, *, #9239, .F. ) ;
#10076=CARTESIAN_POINT ( 'NONE',  ( 1.846955891736119071, -10.21904526726841311, -7.098901504650468652 ) ) ;
#10077=ADVANCED_FACE ( 'NONE', ( #17533 ), #17737, .F. ) ;
#10085=CARTESIAN_POINT ( 'NONE',  ( 16.58200780006414732, 0.01080144354108870768, 0.002844973367391462511 ) ) ;
#10089=VERTEX_POINT ( 'NONE', #7514 ) ;
#10091=DIRECTION ( 'NONE',  ( 0.7561779333270775005, -0.3559159372837316093, -0.5491072561318351974 ) ) ;
#10093=B_SPLINE_CURVE_WITH_KNOTS ( 'NONE', 3,
 ( #16730, #6692, #13941, #2374 ),
 .UNSPECIFIED., .F., .F.,
 ( 4, 4 ),
 ( 3.727890075251872641E-16, 0.002004993803842877297 ),
 .UNSPECIFIED. ) ;
#10097=EDGE_CURVE ( 'NONE', #11870, #5180, #17524, .T. ) ;
#10098=CARTESIAN_POINT ( 'NONE',  ( 2.636624412716062960, 6.973567714909310489, -14.46769361191320868 ) ) ;
#10099=CIRCLE ( 'NONE', #5222, 2.500000000000000000 ) ;
#10100=EDGE_CURVE ( 'NONE', #16664, #13997, #17061, .T. ) ;
#10103=CARTESIAN_POINT ( 'NONE',  ( 2.636624412716062960, -2.161493821598612808, -15.91454522070331912 ) ) ;
#10104=B_SPLINE_CURVE_WITH_KNOTS ( 'NONE', 3,
 ( #5444, #9560, #11102, #15661 ),
 .UNSPECIFIED., .F., .F.,
 ( 4, 4 ),
 ( 1.914591753770035818E-17, 0.002004993803842692549 ),
 .UNSPECIFIED. ) ;
#10108=DIRECTION ( 'NONE',  ( 0.000000000000000000, 0.000000000000000000, 1.000000000000000000 ) ) ;
#10109=VERTEX_POINT ( 'NONE', #13230 ) ;
#10116=ORIENTED_EDGE ( 'NONE', *, *, #5321, .F. ) ;
#10117=CARTESIAN_POINT ( 'NONE',  ( 2.002547531651521773, 9.778737580845699995, 7.942910686618207983 ) ) ;
#10120=CARTESIAN_POINT ( 'NONE',  ( 2.353870697619111496, -8.216087327473003299, 10.00946331859660710 ) ) ;
#10122=LINE ( 'NONE', #15946, #16947 ) ;
#10126=CARTESIAN_POINT ( 'NONE',  ( 0.3151930723728451622, -13.73922999529477451, -0.07645105377001075453 ) ) ;
#10128=CARTESIAN_POINT ( 'NONE',  ( 0.4862570985993235340, -8.769551628660812170, 10.79774104611370333 ) ) ;
#10137=VERTEX_POINT ( 'NONE', #1575 ) ;
#10141=ADVANCED_FACE ( 'NONE', ( #16108 ), #1362, .F. ) ;
#10142=CARTESIAN_POINT ( 'NONE',  ( 0.3142014840576516921, 4.608051180497103161, -12.94260032291123785 ) ) ;
#10144=ORIENTED_EDGE ( 'NONE', *, *, #17142, .T. ) ;
#10158=EDGE_CURVE ( 'NONE', #1652, #13434, #7614, .T. ) ;
#10161=CARTESIAN_POINT ( 'NONE',  ( 0.3095370825347224519, 4.681152801286160070, 12.91933430393609861 ) ) ;
#10164=B_SPLINE_CURVE_WITH_KNOTS ( 'NONE', 3,
 ( #13601, #519, #2313, #2223, #3658, #9299 ),
 .UNSPECIFIED., .F., .F.,
 ( 4, 2, 4 ),
 ( 0.000000000000000000, 0.001500839035891550922, 0.003001678071783101844 ),
 .UNSPECIFIED. ) ;
#10166=ORIENTED_EDGE ( 'NONE', *, *, #6712, .T. ) ;
#10167=CARTESIAN_POINT ( 'NONE',  ( 3.950837973638668288, 0.000000000000000000, 0.000000000000000000 ) ) ;
#10177=CARTESIAN_POINT ( 'NONE',  ( 0.3137051932979792457, -7.698472063774386420, -11.37800749014139612 ) ) ;
#10183=ORIENTED_EDGE ( 'NONE', *, *, #4315, .T. ) ;
#10187=CARTESIAN_POINT ( 'NONE',  ( 1.846524061778021419, 4.180439405448487911, -11.71897913237544664 ) ) ;
#10189=CARTESIAN_POINT ( 'NONE',  ( 0.4862570985993235340, 8.769551628660890330, -10.79774104611363761 ) ) ;
#10190=ORIENTED_EDGE ( 'NONE', *, *, #12726, .T. ) ;
#10192=CARTESIAN_POINT ( 'NONE',  ( 2.747332970342022840, -2.409922051470793747, 16.17136872824897864 ) ) ;
#10193=AXIS2_PLACEMENT_3D ( 'NONE', #5787, #1210, #17460 ) ;
#10199=CARTESIAN_POINT ( 'NONE',  ( 16.56782317627811096, 0.003357783021327817585, 0.009228812961908668469 ) ) ;
#10202=VERTEX_POINT ( 'NONE', #9319 ) ;
#10205=ORIENTED_EDGE ( 'NONE', *, *, #18181, .F. ) ;
#10207=ORIENTED_EDGE ( 'NONE', *, *, #3630, .T. ) ;
#10208=CARTESIAN_POINT ( 'NONE',  ( 1.846138399168762989, 9.815003036200414144, 7.646096044339929954 ) ) ;
#10211=EDGE_LOOP ( 'NONE', ( #7935, #8052, #1763, #12431 ) ) ;
#10212=DIRECTION ( 'NONE',  ( -1.000000000000000000, 0.000000000000000000, 0.000000000000000000 ) ) ;
#10218=EDGE_CURVE ( 'NONE', #9992, #5117, #9621, .T. ) ;
#10219=DIRECTION ( 'NONE',  ( -0.7561779333270775005, 0.03481510524964793324, 0.6534392409364820908 ) ) ;
#10221=( BOUNDED_SURFACE ( )  B_SPLINE_SURFACE ( 3, 1, ( 
 ( #17232, #4247 ),
 ( #11238, #9696 ),
 ( #11138, #3870 ),
 ( #15701, #17140 ) ),
 .UNSPECIFIED., .F., .F., .T. ) 
 B_SPLINE_SURFACE_WITH_KNOTS ( ( 4, 4 ),
 ( 2, 2 ),
 ( 0.000000000000000000, 1.000000000000000000 ),
 ( 0.000000000000000000, 1.000000000000000000 ),
 .UNSPECIFIED. ) 
 GEOMETRIC_REPRESENTATION_ITEM ( )  RATIONAL_B_SPLINE_SURFACE ( (
 ( 1.000000000000000000, 1.000000000000000000),
 ( 0.7792777138730160313, 0.9689936506012927220),
 ( 0.7792777138730160313, 0.9689936506012927220),
 ( 1.000000000000000000, 1.000000000000000000) ) ) 
 REPRESENTATION_ITEM ( '' )  SURFACE ( )  );
#10232=CARTESIAN_POINT ( 'NONE',  ( 0.8740779401507798863, 5.211551231203803702, 13.31469722824348878 ) ) ;
#10234=CARTESIAN_POINT ( 'NONE',  ( 16.56753206892534891, -0.006760771273035160941, 0.006669401563385170262 ) ) ;
#10235=ADVANCED_FACE ( 'NONE', ( #15148 ), #2688, .F. ) ;
#10236=ADVANCED_FACE ( 'NONE', ( #9033 ), #1997, .F. ) ;
#10237=CARTESIAN_POINT ( 'NONE',  ( 8.438534575730034959, 3.845978796786037268, 5.688336279099058146 ) ) ;
#10238=ORIENTED_EDGE ( 'NONE', *, *, #1804, .F. ) ;
#10239=CARTESIAN_POINT ( 'NONE',  ( 1.847372867223027404, 10.00438561114523850, 7.398914411685026060 ) ) ;
#10245=CARTESIAN_POINT ( 'NONE',  ( 1.254009781011619529, -3.563484327698362542, 14.24044713813325558 ) ) ;
#10246=DIRECTION ( 'NONE',  ( -0.7635533937278216055, -0.02138673900301441000, -0.6453904417649389824 ) ) ;
#10248=ADVANCED_FACE ( 'NONE', ( #18200, #3180 ), #1771, .F. ) ;
#10255=CARTESIAN_POINT ( 'NONE',  ( 0.4862570985993235340, 7.559321496869426227, 11.67702470553367711 ) ) ;
#10256=VECTOR ( 'NONE', #13482, 1000.000000000000227 ) ;
#10260=VERTEX_POINT ( 'NONE', #10565 ) ;
#10261=ORIENTED_EDGE ( 'NONE', *, *, #4469, .F. ) ;
#10263=ORIENTED_EDGE ( 'NONE', *, *, #6506, .T. ) ;
#10264=CARTESIAN_POINT ( 'NONE',  ( 2.636624412714236865, 0.000000000000000000, 0.000000000000000000 ) ) ;
#10266=FACE_OUTER_BOUND ( 'NONE', #7448, .T. ) ;
#10268=CARTESIAN_POINT ( 'NONE',  ( 0.3137051932979792457, 4.679953077377485116, 12.91601973349272114 ) ) ;
#10277=CARTESIAN_POINT ( 'NONE',  ( 0.3132642857406504611, -7.641821025099783782, -11.41580579227785464 ) ) ;
#10283=ORIENTED_EDGE ( 'NONE', *, *, #5395, .F. ) ;
#10291=CARTESIAN_POINT ( 'NONE',  ( 2.636624412716062071, -14.14563173255412742, -7.605649742760987486 ) ) ;
#10294=EDGE_CURVE ( 'NONE', #13957, #10109, #6887, .T. ) ;
#10298=CARTESIAN_POINT ( 'NONE',  ( 2.002547531651519996, -0.6781519942170860515, -12.57989064830760206 ) ) ;
#10299=CARTESIAN_POINT ( 'NONE',  ( 1.861628059977343597, -10.38573835516717381, 6.879051339207257421 ) ) ;
#10301=LINE ( 'NONE', #1798, #15383 ) ;
#10304=( BOUNDED_SURFACE ( )  B_SPLINE_SURFACE ( 3, 1, ( 
 ( #16208, #3290 ),
 ( #5977, #3092 ),
 ( #15749, #1220 ),
 ( #1878, #18703 ) ),
 .UNSPECIFIED., .F., .F., .T. ) 
 B_SPLINE_SURFACE_WITH_KNOTS ( ( 4, 4 ),
 ( 2, 2 ),
 ( 0.000000000000000000, 1.000000000000000000 ),
 ( 0.000000000000000000, 1.000000000000000000 ),
 .UNSPECIFIED. ) 
 GEOMETRIC_REPRESENTATION_ITEM ( )  RATIONAL_B_SPLINE_SURFACE ( (
 ( 1.000000000000000000, 1.000000000000000000),
 ( 0.7792777138730158093, 0.9689936506012928330),
 ( 0.7792777138730158093, 0.9689936506012928330),
 ( 1.000000000000000000, 1.000000000000000000) ) ) 
 REPRESENTATION_ITEM ( '' )  SURFACE ( )  );
#10308=EDGE_CURVE ( 'NONE', #17715, #12131, #15122, .T. ) ;
#10311=ORIENTED_EDGE ( 'NONE', *, *, #3733, .T. ) ;
#10314=CARTESIAN_POINT ( 'NONE',  ( 0.8740764193768836288, 9.070946295054209685, -11.05257066464527327 ) ) ;
#10315=CARTESIAN_POINT ( 'NONE',  ( 0.3170788640506441158, -13.11595226728154984, -4.100430649998100030 ) ) ;
#10317=CARTESIAN_POINT ( 'NONE',  ( 0.3170788640506441158, -4.392045232375722641, -13.02120094575832709 ) ) ;
#10322=CARTESIAN_POINT ( 'NONE',  ( 0.4754618798421171855, 0.7484603771384397142, 13.89949764182683012 ) ) ;
#10323=CARTESIAN_POINT ( 'NONE',  ( 0.4862570985993235340, 12.97920246947886191, -5.003653737315353567 ) ) ;
#10324=EDGE_CURVE ( 'NONE', #15826, #18802, #9624, .T. ) ;
#10327=ORIENTED_EDGE ( 'NONE', *, *, #2505, .T. ) ;
#10330=ORIENTED_EDGE ( 'NONE', *, *, #15690, .T. ) ;
#10331=EDGE_CURVE ( 'NONE', #5127, #11242, #5967, .T. ) ;
#10332=CARTESIAN_POINT ( 'NONE',  ( 0.3095370825347234511, 11.38092634279639803, -7.700448427571746635 ) ) ;
#10336=B_SPLINE_CURVE_WITH_KNOTS ( 'NONE', 3,
 ( #5634, #17308, #4317, #10043, #17401, #5732, #14347, #10239, #7092, #11584, #14440, #5928, #1251 ),
 .UNSPECIFIED., .F., .F.,
 ( 4, 3, 3, 3, 4 ),
 ( 2.453269466693398698E-18, 0.0002299804304191500187, 0.0004599608082120258223, 0.0006467586077648020170, 0.0008336169836825994828 ),
 .UNSPECIFIED. ) ;
#10341=CARTESIAN_POINT ( 'NONE',  ( 3.512766787570770433, -2.025881399556492823, 14.91422000116819113 ) ) ;
#10350=ORIENTED_EDGE ( 'NONE', *, *, #7083, .F. ) ;
#10353=B_SPLINE_CURVE_WITH_KNOTS ( 'NONE', 3,
 ( #2666, #10030, #15864, #8600, #7176, #14425 ),
 .UNSPECIFIED., .F., .F.,
 ( 4, 2, 4 ),
 ( 3.144186300207962859E-18, 0.0002017457492448088553, 0.0004034914984896145664 ),
 .UNSPECIFIED. ) ;
#10356=VERTEX_POINT ( 'NONE', #16454 ) ;
#10359=CARTESIAN_POINT ( 'NONE',  ( 0.4862570985993235340, 7.559321496869426227, 11.67702470553367711 ) ) ;
#10366=CARTESIAN_POINT ( 'NONE',  ( 0.3148208552358936485, 4.463611911212218786, 12.99355031785207260 ) ) ;
#10370=CARTESIAN_POINT ( 'NONE',  ( 16.56679352167444819, 0.001518074900131727951, 0.009170718284672568082 ) ) ;
#10376=CARTESIAN_POINT ( 'NONE',  ( 8.438534575730034959, 1.899950616255187352, 6.598402093327886853 ) ) ;
#10377=FACE_OUTER_BOUND ( 'NONE', #594, .T. ) ;
#10379=EDGE_CURVE ( 'NONE', #4341, #16993, #6214, .T. ) ;
#10381=ORIENTED_EDGE ( 'NONE', *, *, #695, .F. ) ;
#10383=CARTESIAN_POINT ( 'NONE',  ( 0.3151928479966097374, 6.943324946344315912E-05, 13.73922861026898623 ) ) ;
#10387=CARTESIAN_POINT ( 'NONE',  ( 0.4862570985993252548, 10.79774104611373353, 8.769551628660776643 ) ) ;
#10389=DIRECTION ( 'NONE',  ( -0.7635533937278214944, 0.6204116510013479857, 0.1790966170213943998 ) ) ;
#10390=CARTESIAN_POINT ( 'NONE',  ( 16.56822296793089322, -0.003834730849370904075, 0.009385634690641608477 ) ) ;
#10393=FACE_OUTER_BOUND ( 'NONE', #16245, .T. ) ;
#10394=CARTESIAN_POINT ( 'NONE',  ( 1.959212340397943120, -9.750290364083578964, -7.909199412631276793 ) ) ;
#10402=CARTESIAN_POINT ( 'NONE',  ( 16.56782317627811096, 0.007739510688078436902, -0.006045301465876656150 ) ) ;
#10404=CARTESIAN_POINT ( 'NONE',  ( 0.3095370825347234511, -11.38092634279634119, 7.700448427571834564 ) ) ;
#10407=CARTESIAN_POINT ( 'NONE',  ( 2.002547531651521773, 9.778737580845699995, 7.942910686618207983 ) ) ;
#10408=CARTESIAN_POINT ( 'NONE',  ( 2.636624412714236865, 0.000000000000000000, 0.000000000000000000 ) ) ;
#10415=( BOUNDED_SURFACE ( )  B_SPLINE_SURFACE ( 3, 1, ( 
 ( #6824, #2500 ),
 ( #12644, #9692 ),
 ( #9857, #3956 ),
 ( #15694, #15795 ) ),
 .UNSPECIFIED., .F., .F., .T. ) 
 B_SPLINE_SURFACE_WITH_KNOTS ( ( 4, 4 ),
 ( 2, 2 ),
 ( 0.000000000000000000, 1.000000000000000000 ),
 ( 0.000000000000000000, 1.000000000000000000 ),
 .UNSPECIFIED. ) 
 GEOMETRIC_REPRESENTATION_ITEM ( )  RATIONAL_B_SPLINE_SURFACE ( (
 ( 1.000000000000000000, 1.000000000000000000),
 ( 0.9933953342250436691, 0.8357391271907733676),
 ( 0.9933953342250436691, 0.8357391271907733676),
 ( 1.000000000000000000, 1.000000000000000000) ) ) 
 REPRESENTATION_ITEM ( '' )  SURFACE ( )  );
#10416=CARTESIAN_POINT ( 'NONE',  ( 16.58200780006414732, 0.006043560077721704844, 0.009393638146079782980 ) ) ;
#10418=CARTESIAN_POINT ( 'NONE',  ( 16.56679352167444819, 0.004162264567719650525, 0.008311568981097349276 ) ) ;
#10423=ORIENTED_EDGE ( 'NONE', *, *, #13199, .T. ) ;
#10425=CARTESIAN_POINT ( 'NONE',  ( 0.3137051932979757485, 7.698472063774634222, -11.37800749014122736 ) ) ;
#10427=EDGE_CURVE ( 'NONE', #8092, #12877, #17785, .T. ) ;
#10428=FACE_OUTER_BOUND ( 'NONE', #12159, .T. ) ;
#10429=ORIENTED_EDGE ( 'NONE', *, *, #9195, .F. ) ;
#10436=DIRECTION ( 'NONE',  ( 0.000000000000000000, 0.000000000000000000, 1.000000000000000000 ) ) ;
#10437=MANIFOLD_SOLID_BREP ( 'Bore', #834 ) ;
#10438=VERTEX_POINT ( 'NONE', #12046 ) ;
#10443=CARTESIAN_POINT ( 'NONE',  ( 16.56822296793089322, 0.005339139727952925060, 0.008619100080558696197 ) ) ;
#10444=CARTESIAN_POINT ( 'NONE',  ( 0.3307726912345234083, 11.46720933246398388, 7.596084275798933305 ) ) ;
#10447=ORIENTED_EDGE ( 'NONE', *, *, #6767, .T. ) ;
#10449=CARTESIAN_POINT ( 'NONE',  ( 0.3095370825347224519, 3.806662003783413351, 13.20347358821915940 ) ) ;
#10457=CIRCLE ( 'NONE', #5936, 16.06066017081991149 ) ;
#10464=CIRCLE ( 'NONE', #2221, 16.06066017081991149 ) ;
#10465=LINE ( 'NONE', #14755, #163 ) ;
#10466=CARTESIAN_POINT ( 'NONE',  ( 0.3720661004400040439, -7.524064345033547596, 11.58636699658212699 ) ) ;
#10470=CARTESIAN_POINT ( 'NONE',  ( 3.950837973638675393, -10.05648675950118509, -10.51028938476228980 ) ) ;
#10471=DIRECTION ( 'NONE',  ( -0.7561779333270775005, 0.6106991889125087392, -0.2350349629540122165 ) ) ;
#10481=CARTESIAN_POINT ( 'NONE',  ( 1.959212340397961327, 0.6675998551413537818, -12.53706137681889388 ) ) ;
#10483=CARTESIAN_POINT ( 'NONE',  ( 0.3939822652208105902, 13.80035637018652395, 0.7002900021918435636 ) ) ;
#10484=CARTESIAN_POINT ( 'NONE',  ( 2.636624412717099908, 11.60464335004051861, -11.10302021258208249 ) ) ;
#10485=VERTEX_POINT ( 'NONE', #15201 ) ;
#10486=CARTESIAN_POINT ( 'NONE',  ( 8.438534575730034959, 6.598402093327880635, 1.899950616255211111 ) ) ;
#10493=DIRECTION ( 'NONE',  ( -1.000000000000000000, -0.000000000000000000, -0.000000000000000000 ) ) ;
#10497=ORIENTED_EDGE ( 'NONE', *, *, #8882, .F. ) ;
#10498=EDGE_LOOP ( 'NONE', ( #6656, #15337, #9998, #1604 ) ) ;
#10513=CARTESIAN_POINT ( 'NONE',  ( 8.438534575730034959, -2.341351102130233119, -6.454982381540311565 ) ) ;
#10515=CARTESIAN_POINT ( 'NONE',  ( 1.861628059977342708, 11.66985327793199190, 4.358833901513087916 ) ) ;
#10517=CARTESIAN_POINT ( 'NONE',  ( 16.57210152137263393, -0.003862718596009370557, 0.01402404281923043221 ) ) ;
#10518=EDGE_CURVE ( 'NONE', #11623, #9992, #9845, .T. ) ;
#10519=CARTESIAN_POINT ( 'NONE',  ( 2.705023505549863039, 3.294610156756076602, -12.88681800078729189 ) ) ;
#10524=ORIENTED_EDGE ( 'NONE', *, *, #15998, .T. ) ;
#10528=CARTESIAN_POINT ( 'NONE',  ( 0.3308579732647026761, -12.88563776947742312, -4.812490080619330257 ) ) ;
#10530=( BOUNDED_SURFACE ( )  B_SPLINE_SURFACE ( 3, 1, ( 
 ( #12957, #5880 ),
 ( #1401, #18789 ),
 ( #5686, #18883 ),
 ( #5783, #11628 ) ),
 .UNSPECIFIED., .F., .F., .T. ) 
 B_SPLINE_SURFACE_WITH_KNOTS ( ( 4, 4 ),
 ( 2, 2 ),
 ( 0.000000000000000000, 1.000000000000000000 ),
 ( 0.000000000000000000, 1.000000000000000000 ),
 .UNSPECIFIED. ) 
 GEOMETRIC_REPRESENTATION_ITEM ( )  RATIONAL_B_SPLINE_SURFACE ( (
 ( 1.000000000000000000, 1.000000000000000000),
 ( 0.9933953342250436691, 0.8357391271907733676),
 ( 0.9933953342250436691, 0.8357391271907733676),
 ( 1.000000000000000000, 1.000000000000000000) ) ) 
 REPRESENTATION_ITEM ( '' )  SURFACE ( )  );
#10537=CARTESIAN_POINT ( 'NONE',  ( 0.4754618798421171855, 12.98792082933651493, -5.007009103465112076 ) ) ;
#10539=EDGE_CURVE ( 'NONE', #13630, #15469, #1339, .T. ) ;
#10541=EDGE_CURVE ( 'NONE', #15645, #11211, #8476, .T. ) ;
#10545=CARTESIAN_POINT ( 'NONE',  ( 0.3095370825347233956, 0.4597470195090213041, 13.73357284481724960 ) ) ;
#10549=ORIENTED_EDGE ( 'NONE', *, *, #2442, .T. ) ;
#10550=CARTESIAN_POINT ( 'NONE',  ( 0.3148208552358926493, -7.888357771040781508, 11.24855514421872726 ) ) ;
#10554=VERTEX_POINT ( 'NONE', #14120 ) ;
#10557=CARTESIAN_POINT ( 'NONE',  ( 16.58200780006414732, -0.0006320991582348829945, 0.01115192838421569070 ) ) ;
#10558=VERTEX_POINT ( 'NONE', #12870 ) ;
#10565=CARTESIAN_POINT ( 'NONE',  ( 3.950837973638676281, -6.316429227969383220, -13.10350451991847009 ) ) ;
#10572=CARTESIAN_POINT ( 'NONE',  ( 0.3151930723728450512, 13.73922999529477451, 0.07645105376991474799 ) ) ;
#10579=VECTOR ( 'NONE', #14583, 1000.000000000000000 ) ;
#10583=B_SPLINE_CURVE_WITH_KNOTS ( 'NONE', 3,
 ( #6136, #17800, #4701, #10528, #3247, #9095 ),
 .UNSPECIFIED., .F., .F.,
 ( 4, 2, 4 ),
 ( 4.225718824587268470E-17, 0.0002014099069817298145, 0.0004028198139634173993 ),
 .UNSPECIFIED. ) ;
#10585=CARTESIAN_POINT ( 'NONE',  ( 1.959212340397940899, -3.239239832448945755, -12.12975361829679066 ) ) ;
#10596=EDGE_CURVE ( 'NONE', #8651, #5950, #7058, .T. ) ;
#10600=CIRCLE ( 'NONE', #17287, 14.54644660717763927 ) ;
#10601=ORIENTED_EDGE ( 'NONE', *, *, #2923, .F. ) ;
#10603=ORIENTED_EDGE ( 'NONE', *, *, #10427, .F. ) ;
#10604=ORIENTED_EDGE ( 'NONE', *, *, #13107, .T. ) ;
#10610=CARTESIAN_POINT ( 'NONE',  ( 0.3132635586635977853, -11.41586812343484070, -7.641727604904016147 ) ) ;
#10615=CARTESIAN_POINT ( 'NONE',  ( 0.3307726912345230752, 3.680742887039495148, -13.25328329128662119 ) ) ;
#10616=CARTESIAN_POINT ( 'NONE',  ( 0.3142014840576536350, 12.94260032291128759, 4.608051180496968158 ) ) ;
#10621=ORIENTED_EDGE ( 'NONE', *, *, #2429, .T. ) ;
#10622=CARTESIAN_POINT ( 'NONE',  ( 2.636624412715137034, -11.60464335004055947, 11.10302021257951743 ) ) ;
#10624=VERTEX_POINT ( 'NONE', #12782 ) ;
#10626=EDGE_CURVE ( 'NONE', #5819, #10871, #2767, .T. ) ;
#10632=B_SPLINE_CURVE_WITH_KNOTS ( 'NONE', 3,
 ( #9767, #8348, #2590, #1918, #11948, #15198, #4969, #13671, #1718, #7755, #17689, #4881, #18064 ),
 .UNSPECIFIED., .F., .F.,
 ( 4, 3, 3, 3, 4 ),
 ( 8.673617379884035472E-19, 0.0002299804304191502627, 0.0004599608082120273944, 0.0006467586077648031012, 0.0008336169836825989407 ),
 .UNSPECIFIED. ) ;
#10635=CARTESIAN_POINT ( 'NONE',  ( 0.3095370825347224519, 13.20347358821919670, -3.806662003783277459 ) ) ;
#10636=CARTESIAN_POINT ( 'NONE',  ( 2.002547531651519996, 0.6781519942171739812, 12.57989064830759851 ) ) ;
#10639=ORIENTED_EDGE ( 'NONE', *, *, #1185, .T. ) ;
#10640=B_SPLINE_CURVE_WITH_KNOTS ( 'NONE', 3,
 ( #11996, #2064, #4834, #4924, #8240, #18356, #18020 ),
 .UNSPECIFIED., .F., .F.,
 ( 4, 3, 4 ),
 ( 3.198396408832238080E-18, 0.0002299780670421062274, 0.0004597478348664300451 ),
 .UNSPECIFIED. ) ;
#10649=CARTESIAN_POINT ( 'NONE',  ( 0.3148208552358935375, -4.026279359288518656, 13.13564827777588029 ) ) ;
#10650=CARTESIAN_POINT ( 'NONE',  ( 1.845756295923356438, -11.67600463554276224, 4.296776483139434610 ) ) ;
#10651=( BOUNDED_SURFACE ( )  B_SPLINE_SURFACE ( 3, 1, ( 
 ( #3046, #4791 ),
 ( #13288, #203 ),
 ( #8989, #17704 ),
 ( #3346, #1630 ) ),
 .UNSPECIFIED., .F., .F., .T. ) 
 B_SPLINE_SURFACE_WITH_KNOTS ( ( 4, 4 ),
 ( 2, 2 ),
 ( 0.000000000000000000, 1.000000000000000000 ),
 ( 0.000000000000000000, 1.000000000000000000 ),
 .UNSPECIFIED. ) 
 GEOMETRIC_REPRESENTATION_ITEM ( )  RATIONAL_B_SPLINE_SURFACE ( (
 ( 1.000000000000000000, 1.000000000000000000),
 ( 0.9593108457356467333, 0.9995965569486454649),
 ( 0.9593108457356467333, 0.9995965569486454649),
 ( 1.000000000000000000, 1.000000000000000000) ) ) 
 REPRESENTATION_ITEM ( '' )  SURFACE ( )  );
#10652=ORIENTED_EDGE ( 'NONE', *, *, #909, .F. ) ;
#10655=EDGE_CURVE ( 'NONE', #12889, #2783, #3704, .T. ) ;
#10659=CARTESIAN_POINT ( 'NONE',  ( 0.4754618798421167414, 10.80499583390513152, 8.775436892861154803 ) ) ;
#10660=ORIENTED_EDGE ( 'NONE', *, *, #16862, .T. ) ;
#10663=CARTESIAN_POINT ( 'NONE',  ( 1.254009781012255020, 7.789615163754674221, -12.44229282923133262 ) ) ;
#10666=CARTESIAN_POINT ( 'NONE',  ( 0.3720661004400037664, -4.951033743989731839, 12.89739157014191129 ) ) ;
#10667=CARTESIAN_POINT ( 'NONE',  ( 2.002547531651519996, -3.242439124566566910, -12.17374746633581495 ) ) ;
#10668=CARTESIAN_POINT ( 'NONE',  ( 0.3151930723728398331, 8.013866567350898862, 11.16020735774769435 ) ) ;
#10672=VECTOR ( 'NONE', #10246, 1000.000000000000114 ) ;
#10676=EDGE_CURVE ( 'NONE', #2096, #11053, #10301, .T. ) ;
#10677=EDGE_CURVE ( 'NONE', #18537, #1902, #14635, .T. ) ;
#10678=ORIENTED_EDGE ( 'NONE', *, *, #10218, .F. ) ;
#10683=CARTESIAN_POINT ( 'NONE',  ( 0.3132642857406529591, -13.72733058964894681, -0.5276792104583708509 ) ) ;
#10697=ORIENTED_EDGE ( 'NONE', *, *, #14086, .T. ) ;
#10700=CARTESIAN_POINT ( 'NONE',  ( 0.3720661004400037664, -11.58636699658219982, 7.524064345033424139 ) ) ;
#10705=ORIENTED_EDGE ( 'NONE', *, *, #8699, .F. ) ;
#10707=CARTESIAN_POINT ( 'NONE',  ( 0.4754618798421162973, -7.564402563418381575, -11.68486377711974811 ) ) ;
#10712=CARTESIAN_POINT ( 'NONE',  ( 2.636624412714236865, 0.000000000000000000, 0.000000000000000000 ) ) ;
#10717=CARTESIAN_POINT ( 'NONE',  ( 0.4862570985993235340, -8.769551628660655851, -10.79774104611382946 ) ) ;
#10720=CARTESIAN_POINT ( 'NONE',  ( 0.4754618798421162973, 11.68486377711977475, -7.564402563418339831 ) ) ;
#10724=ORIENTED_EDGE ( 'NONE', *, *, #10758, .T. ) ;
#10730=ORIENTED_EDGE ( 'NONE', *, *, #16141, .T. ) ;
#10731=ADVANCED_FACE ( 'NONE', ( #1511 ), #16403, .F. ) ;
#10737=ORIENTED_EDGE ( 'NONE', *, *, #12462, .T. ) ;
#10741=CARTESIAN_POINT ( 'NONE',  ( 2.123976203522053741, -1.531817366691644144, -15.54801196254788742 ) ) ;
#10750=B_SPLINE_CURVE_WITH_KNOTS ( 'NONE', 3,
 ( #11056, #5124, #2252, #12385, #12475, #12564 ),
 .UNSPECIFIED., .F., .F.,
 ( 4, 2, 4 ),
 ( 3.499941646806256644E-17, 0.0001825746017570586152, 0.0003651492035140799881 ),
 .UNSPECIFIED. ) ;
#10754=DIRECTION ( 'NONE',  ( 0.000000000000000000, 0.000000000000000000, 1.000000000000000000 ) ) ;
#10756=CARTESIAN_POINT ( 'NONE',  ( 1.918918678667046462, 7.860057224348842020, 9.738328798462404734 ) ) ;
#10757=CARTESIAN_POINT ( 'NONE',  ( 0.000000000000000000, 0.000000000000000000, 0.000000000000000000 ) ) ;
#10758=EDGE_CURVE ( 'NONE', #1712, #17181, #6457, .T. ) ;
#10761=EDGE_CURVE ( 'NONE', #11623, #1184, #10464, .T. ) ;
#10762=CARTESIAN_POINT ( 'NONE',  ( 1.977436885026506497, -3.321781585408274839, -15.04044112860335147 ) ) ;
#10763=CARTESIAN_POINT ( 'NONE',  ( 0.3137051932979757485, 8.442169467526850823, 10.83767969834806166 ) ) ;
#10765=CARTESIAN_POINT ( 'NONE',  ( 1.846138399168762101, -11.69739621335925328, 4.238866729160359448 ) ) ;
#10767=CARTESIAN_POINT ( 'NONE',  ( 16.57210152137263393, -0.005118120558001483002, 0.01361613799508852585 ) ) ;
#10769=ORIENTED_EDGE ( 'NONE', *, *, #18131, .F. ) ;
#10780=EDGE_CURVE ( 'NONE', #18854, #17057, #12110, .T. ) ;
#10784=EDGE_CURVE ( 'NONE', #4406, #16984, #13822, .T. ) ;
#10786=CARTESIAN_POINT ( 'NONE',  ( 1.846138399168762101, 7.646096044340033870, -9.815003036200328879 ) ) ;
#10789=B_SPLINE_CURVE_WITH_KNOTS ( 'NONE', 3,
 ( #1163, #1061, #2766, #4228 ),
 .UNSPECIFIED., .F., .F.,
 ( 4, 4 ),
 ( 0.000000000000000000, 0.002004993803841771411 ),
 .UNSPECIFIED. ) ;
#10790=ORIENTED_EDGE ( 'NONE', *, *, #623, .T. ) ;
#10791=ORIENTED_EDGE ( 'NONE', *, *, #7260, .T. ) ;
#10795=CARTESIAN_POINT ( 'NONE',  ( 16.57210152137263393, 0.005118120558001383255, -0.01361613799508856922 ) ) ;
#10796=CARTESIAN_POINT ( 'NONE',  ( 1.847168016377979116, -7.464000291196340342, -9.955470380986712442 ) ) ;
#10797=CARTESIAN_POINT ( 'NONE',  ( 3.950837973638676281, -6.316429227969562632, 13.10350451991838128 ) ) ;
#10801=CONICAL_SURFACE ( 'NONE', #2523, 16.06066017081991149, 0.7853981625000062694 ) ;
#10810=EDGE_CURVE ( 'NONE', #17093, #492, #15078, .T. ) ;
#10812=CARTESIAN_POINT ( 'NONE',  ( 1.845756295923357104, 11.67600463554279244, -4.296776483139357339 ) ) ;
#10816=CARTESIAN_POINT ( 'NONE',  ( 1.847461586945734480, -3.877048136045296634, -11.82388984758122596 ) ) ;
#10823=B_SPLINE_CURVE_WITH_KNOTS ( 'NONE', 3,
 ( #10470, #151, #11711, #16204 ),
 .UNSPECIFIED., .F., .F.,
 ( 4, 4 ),
 ( 2.117499858742978245E-17, 0.003005512676784849197 ),
 .UNSPECIFIED. ) ;
#10829=CARTESIAN_POINT ( 'NONE',  ( 1.861706995891665439, -6.878962591851823127, 10.38589138506424092 ) ) ;
#10830=ADVANCED_FACE ( 'NONE', ( #6294 ), #18337, .F. ) ;
#10836=ORIENTED_EDGE ( 'NONE', *, *, #17242, .T. ) ;
#10837=CARTESIAN_POINT ( 'NONE',  ( 1.861628059977341598, 12.00316790821106139, -3.332996951203504032 ) ) ;
#10850=CARTESIAN_POINT ( 'NONE',  ( 0.4862570985993252548, 5.003653737315486794, 12.97920246947881395 ) ) ;
#10861=CARTESIAN_POINT ( 'NONE',  ( 1.846138399168762101, 7.646096044340033870, -9.815003036200328879 ) ) ;
#10863=CARTESIAN_POINT ( 'NONE',  ( 0.3137051932979757485, 8.442169467526850823, 10.83767969834806166 ) ) ;
#10868=EDGE_CURVE ( 'NONE', #618, #13860, #14155, .T. ) ;
#10869=EDGE_LOOP ( 'NONE', ( #11098, #3275, #12974, #18286 ) ) ;
#10871=VERTEX_POINT ( 'NONE', #9153 ) ;
#10872=ORIENTED_EDGE ( 'NONE', *, *, #18361, .T. ) ;
#10877=CARTESIAN_POINT ( 'NONE',  ( 0.3148213771069381384, 10.97836617636225220, 8.260246460850757089 ) ) ;
#10880=CARTESIAN_POINT ( 'NONE',  ( 3.950837973638676281, 2.591948120962007884, -14.31366178983250670 ) ) ;
#10892=ORIENTED_EDGE ( 'NONE', *, *, #7083, .T. ) ;
#10894=EDGE_CURVE ( 'NONE', #14601, #11623, #7338, .T. ) ;
#10897=CARTESIAN_POINT ( 'NONE',  ( 16.56872352241294521, 0.001821578298043785094, -0.01027347319884367241 ) ) ;
#10900=CARTESIAN_POINT ( 'NONE',  ( 1.846138399168762989, 9.815003036200414144, 7.646096044339929954 ) ) ;
#10903=CARTESIAN_POINT ( 'NONE',  ( 0.4862570985993235340, 7.559321496869426227, 11.67702470553367711 ) ) ;
#10909=EDGE_CURVE ( 'NONE', #14561, #15826, #2968, .T. ) ;
#10911=CARTESIAN_POINT ( 'NONE',  ( 16.57210152137263393, 0.01136813053532075186, 0.009075239946108242667 ) ) ;
#10912=ORIENTED_EDGE ( 'NONE', *, *, #9112, .T. ) ;
#10913=CARTESIAN_POINT ( 'NONE',  ( 3.950837973638677170, 6.316429227969654114, -13.10350451991833687 ) ) ;
#10919=CARTESIAN_POINT ( 'NONE',  ( 1.847380140988743591, -3.949801494731685292, -11.79969976631075390 ) ) ;
#10927=CARTESIAN_POINT ( 'NONE',  ( 1.918918678667048461, -12.08296592096905187, -3.258447776119960615 ) ) ;
#10930=EDGE_CURVE ( 'NONE', #10260, #17138, #8019, .T. ) ;
#10936=CARTESIAN_POINT ( 'NONE',  ( 16.58200780006414732, 0.0006320991582349651770, -0.01115192838421568376 ) ) ;
#10937=CIRCLE ( 'NONE', #7904, 13.42403576283810906 ) ;
#10938=ORIENTED_EDGE ( 'NONE', *, *, #16449, .F. ) ;
#10939=CARTESIAN_POINT ( 'NONE',  ( 2.002547531651519996, 12.17374746633582561, -3.242439124566524278 ) ) ;
#10940=CARTESIAN_POINT ( 'NONE',  ( 1.846138399168762989, 11.95493567637850774, 3.446241763653039580 ) ) ;
#10941=VERTEX_POINT ( 'NONE', #9614 ) ;
#10944=FACE_OUTER_BOUND ( 'NONE', #14302, .T. ) ;
#10948=CARTESIAN_POINT ( 'NONE',  ( 0.4862570985993235340, -0.7479633556563419772, 13.89016912371017121 ) ) ;
#10951=CARTESIAN_POINT ( 'NONE',  ( 1.342453679581834924, 5.476372339890209773, -13.74702459364878315 ) ) ;
#10954=CARTESIAN_POINT ( 'NONE',  ( 0.3132642857406489623, -11.41580579227782444, 7.641821025099830855 ) ) ;
#10955=CARTESIAN_POINT ( 'NONE',  ( 16.56782317627811096, 0.009439921864426468329, 0.002708056627497651414 ) ) ;
#10956=CARTESIAN_POINT ( 'NONE',  ( 0.3137051932979809665, 3.805684345189785933, 13.20008686438107581 ) ) ;
#10960=DIRECTION ( 'NONE',  ( -0.7635533937278214944, 0.5095610256143914274, -0.3966532189476541514 ) ) ;
#10962=EDGE_LOOP ( 'NONE', ( #10429, #5875, #6396, #2699 ) ) ;
#10965=ORIENTED_EDGE ( 'NONE', *, *, #2025, .F. ) ;
#10967=CARTESIAN_POINT ( 'NONE',  ( 8.522092701127531811, -2.505958102592667824, 6.489356537178181838 ) ) ;
#10975=AXIS2_PLACEMENT_3D ( 'NONE', #9001, #4518, #10436 ) ;
#10976=CARTESIAN_POINT ( 'NONE',  ( 3.074695600507132198, -14.01296402267896823, -6.754521329825003306 ) ) ;
#10979=B_SPLINE_CURVE_WITH_KNOTS ( 'NONE', 3,
 ( #1968, #7713, #10762, #9504, #13519, #3385 ),
 .UNSPECIFIED., .F., .F.,
 ( 4, 2, 4 ),
 ( 0.000000000000000000, 0.001656992708823338926, 0.003313985417646677853 ),
 .UNSPECIFIED. ) ;
#10985=VECTOR ( 'NONE', #10212, 1000.000000000000000 ) ;
#10993=CARTESIAN_POINT ( 'NONE',  ( 1.847168016377984889, -11.89018175117591980, -3.666915430942724097 ) ) ;
#11003=DIRECTION ( 'NONE',  ( 0.7635533937278216055, 0.3966532189476633663, -0.5095610256143844330 ) ) ;
#11005=DIRECTION ( 'NONE',  ( 0.000000000000000000, 0.000000000000000000, 1.000000000000000000 ) ) ;
#11008=FACE_OUTER_BOUND ( 'NONE', #86, .T. ) ;
#11011=CARTESIAN_POINT ( 'NONE',  ( 1.846138399168762101, -6.971848976711082280, 10.30487220521567693 ) ) ;
#11012=CARTESIAN_POINT ( 'NONE',  ( 0.4385251269669947494, -13.39302348765811068, 3.577373010348662508 ) ) ;
#11013=CARTESIAN_POINT ( 'NONE',  ( 0.3137051932979757485, 7.698472063774634222, -11.37800749014122736 ) ) ;
#11015=AXIS2_PLACEMENT_3D ( 'NONE', #5376, #12364, #18197 ) ;
#11016=ADVANCED_FACE ( 'NONE', ( #11249 ), #7240, .F. ) ;
#11018=CARTESIAN_POINT ( 'NONE',  ( 0.4862570985993235340, 3.580942890621860109, -13.44146924561377254 ) ) ;
#11020=CARTESIAN_POINT ( 'NONE',  ( 16.56872352241294521, -0.009382111268607402216, -0.004564908236399935551 ) ) ;
#11022=VERTEX_POINT ( 'NONE', #8645 ) ;
#11023=CARTESIAN_POINT ( 'NONE',  ( 8.522092701127531811, 2.505958102592620751, 6.489356537178200490 ) ) ;
#11025=CARTESIAN_POINT ( 'NONE',  ( 0.3150692679895942816, -11.02465386701222805, -8.199139630396127032 ) ) ;
#11027=B_SPLINE_CURVE_WITH_KNOTS ( 'NONE', 3,
 ( #1948, #699, #13499, #3656 ),
 .UNSPECIFIED., .F., .F.,
 ( 4, 4 ),
 ( 1.734723475976807094E-17, 0.003005512676784844427 ),
 .UNSPECIFIED. ) ;
#11029=ORIENTED_EDGE ( 'NONE', *, *, #623, .F. ) ;
#11034=CARTESIAN_POINT ( 'NONE',  ( 1.845756295923359769, 10.33914852636104875, 6.920504327368230513 ) ) ;
#11038=CARTESIAN_POINT ( 'NONE',  ( 0.8740764193767192047, -0.8420116711622469552, 14.27348595579779911 ) ) ;
#11040=CARTESIAN_POINT ( 'NONE',  ( 0.8740779401508862456, -13.31469722824359891, 5.211551231203810808 ) ) ;
#11042=( BOUNDED_SURFACE ( )  B_SPLINE_SURFACE ( 3, 1, ( 
 ( #11020, #14340 ),
 ( #9941, #15770 ),
 ( #14062, #5452 ),
 ( #3932, #1153 ) ),
 .UNSPECIFIED., .F., .F., .T. ) 
 B_SPLINE_SURFACE_WITH_KNOTS ( ( 4, 4 ),
 ( 2, 2 ),
 ( 0.000000000000000000, 1.000000000000000000 ),
 ( 0.000000000000000000, 1.000000000000000000 ),
 .UNSPECIFIED. ) 
 GEOMETRIC_REPRESENTATION_ITEM ( )  RATIONAL_B_SPLINE_SURFACE ( (
 ( 1.000000000000000000, 1.000000000000000000),
 ( 0.7792777138730160313, 0.9689936506012927220),
 ( 0.7792777138730160313, 0.9689936506012927220),
 ( 1.000000000000000000, 1.000000000000000000) ) ) 
 REPRESENTATION_ITEM ( '' )  SURFACE ( )  );
#11044=CARTESIAN_POINT ( 'NONE',  ( 3.950837973638675393, -2.591948120961912849, 14.31366178983252446 ) ) ;
#11045=B_SPLINE_CURVE_WITH_KNOTS ( 'NONE', 3,
 ( #9269, #1530, #98, #5912, #11757, #4499 ),
 .UNSPECIFIED., .F., .F.,
 ( 4, 2, 4 ),
 ( 4.027530160694267299E-17, 0.0002014099069817290014, 0.0004028198139634177246 ),
 .UNSPECIFIED. ) ;
#11046=CARTESIAN_POINT ( 'NONE',  ( 16.56822296793089322, 0.009385634690641620620, 0.003834730849370876320 ) ) ;
#11053=VERTEX_POINT ( 'NONE', #13042 ) ;
#11056=CARTESIAN_POINT ( 'NONE',  ( 2.002547531651519996, -9.778737580845755062, 7.942910686618138705 ) ) ;
#11058=B_SPLINE_CURVE_WITH_KNOTS ( 'NONE', 3,
 ( #15518, #13995, #9422, #2074, #15333, #17053 ),
 .UNSPECIFIED., .F., .F.,
 ( 4, 2, 4 ),
 ( 5.421010862427522170E-19, 0.0001825746017570580189, 0.0003651492035141154957 ),
 .UNSPECIFIED. ) ;
#11062=CARTESIAN_POINT ( 'NONE',  ( 3.512766787570877902, 13.25664064834461264, 7.127386085302796381 ) ) ;
#11063=FACE_OUTER_BOUND ( 'NONE', #7231, .T. ) ;
#11071=ORIENTED_EDGE ( 'NONE', *, *, #6712, .F. ) ;
#11078=B_SPLINE_CURVE_WITH_KNOTS ( 'NONE', 3,
 ( #10128, #1239, #2841, #8692, #11661, #7079 ),
 .UNSPECIFIED., .F., .F.,
 ( 4, 2, 4 ),
 ( 4.023840028577795923E-17, 0.0002014099069817275377, 0.0004028198139634147973 ),
 .UNSPECIFIED. ) ;
#11086=CARTESIAN_POINT ( 'NONE',  ( 3.512766787570793969, 2.682019731918377836, 14.81029789862155255 ) ) ;
#11090=CARTESIAN_POINT ( 'NONE',  ( 0.3145729642390390768, 12.96842777670212676, -4.535980493004950986 ) ) ;
#11093=ORIENTED_EDGE ( 'NONE', *, *, #14523, .T. ) ;
#11096=EDGE_CURVE ( 'NONE', #15892, #9201, #14391, .T. ) ;
#11098=ORIENTED_EDGE ( 'NONE', *, *, #13421, .T. ) ;
#11101=ORIENTED_EDGE ( 'NONE', *, *, #9889, .F. ) ;
#11102=CARTESIAN_POINT ( 'NONE',  ( 3.512766787570752669, -14.91422000116822311, 2.025881399556336060 ) ) ;
#11105=CARTESIAN_POINT ( 'NONE',  ( 0.3132635586635982849, 7.641727604904055227, -11.41586812343481583 ) ) ;
#11107=CARTESIAN_POINT ( 'NONE',  ( 1.959283090834840202, 7.909254450749005017, 9.750336807931171634 ) ) ;
#11109=SURFACE_STYLE_USAGE ( .BOTH. , #7080 ) ;
#11110=CARTESIAN_POINT ( 'NONE',  ( 0.4862570985993235340, -0.7479633556561480212, -13.89016912371018186 ) ) ;
#11114=CARTESIAN_POINT ( 'NONE',  ( 3.950837973638675393, -6.888253895133384930, 12.81214529934972823 ) ) ;
#11115=CARTESIAN_POINT ( 'NONE',  ( 0.3151926232592488497, -11.16039997398647365, -8.013596737356504462 ) ) ;
#11116=CARTESIAN_POINT ( 'NONE',  ( 1.845755665166724846, 4.296872077620840891, -11.67596932341229987 ) ) ;
#11125=ADVANCED_FACE ( 'NONE', ( #14569 ), #3939, .F. ) ;
#11126=CARTESIAN_POINT ( 'NONE',  ( 1.959283090834841090, 6.829027319138399221, -10.53516775895152691 ) ) ;
#11129=CARTESIAN_POINT ( 'NONE',  ( 0.4384471787762798112, -7.540925784514636909, 11.63197976518326371 ) ) ;
#11130=CARTESIAN_POINT ( 'NONE',  ( 1.846955891736116184, 7.525208385419960067, 9.909315188408065467 ) ) ;
#11133=ORIENTED_EDGE ( 'NONE', *, *, #6278, .F. ) ;
#11138=CARTESIAN_POINT ( 'NONE',  ( 16.57778382496167424, -0.01466529584256786797, -0.002851818597093949692 ) ) ;
#11144=ORIENTED_EDGE ( 'NONE', *, *, #15998, .F. ) ;
#11151=CARTESIAN_POINT ( 'NONE',  ( 2.636624412716062960, -2.161493821598612808, -15.91454522070331912 ) ) ;
#11154=VECTOR ( 'NONE', #16345, 1000.000000000000114 ) ;
#11159=DIRECTION ( 'NONE',  ( 0.000000000000000000, 0.000000000000000000, 1.000000000000000000 ) ) ;
#11162=ORIENTED_EDGE ( 'NONE', *, *, #7643, .F. ) ;
#11165=ORIENTED_EDGE ( 'NONE', *, *, #4185, .T. ) ;
#11169=CARTESIAN_POINT ( 'NONE',  ( 3.950837973638677170, 10.51028938476232355, -10.05648675950114956 ) ) ;
#11174=B_SPLINE_CURVE_WITH_KNOTS ( 'NONE', 3,
 ( #5485, #8193, #12757, #6841, #11336, #18492 ),
 .UNSPECIFIED., .F., .F.,
 ( 4, 2, 4 ),
 ( 0.000000000000000000, 0.0001828790815886947255, 0.0003657581631773894511 ),
 .UNSPECIFIED. ) ;
#11177=CARTESIAN_POINT ( 'NONE',  ( 3.074695600507311610, 2.772091048739249164, 15.30693405987785916 ) ) ;
#11178=DIRECTION ( 'NONE',  ( -1.000000000000000000, -0.000000000000000000, -0.000000000000000000 ) ) ;
#11193=CARTESIAN_POINT ( 'NONE',  ( 1.847412631396507576, -3.804043368582581408, -11.84727953344286888 ) ) ;
#11194=CONICAL_SURFACE ( 'NONE', #16061, 14.54644660717763927, 0.8559913436420816257 ) ;
#11195=FACE_OUTER_BOUND ( 'NONE', #7237, .T. ) ;
#11196=FACE_OUTER_BOUND ( 'NONE', #7137, .T. ) ;
#11198=CARTESIAN_POINT ( 'NONE',  ( 1.254255976358459757, 14.24071337840876694, -3.563435620217374478 ) ) ;
#11200=CARTESIAN_POINT ( 'NONE',  ( 0.3137051932979792457, 8.442169467527008919, -10.83767969834794087 ) ) ;
#11201=CARTESIAN_POINT ( 'NONE',  ( 0.4754618798421171855, 13.45049478164060019, 3.583352865732718495 ) ) ;
#11211=VERTEX_POINT ( 'NONE', #7907 ) ;
#11212=CARTESIAN_POINT ( 'NONE',  ( 2.320520222537280297, -10.64885284335050741, 11.60169517779339898 ) ) ;
#11214=VERTEX_POINT ( 'NONE', #16405 ) ;
#11216=B_SPLINE_CURVE_WITH_KNOTS ( 'NONE', 3,
 ( #12151, #13675, #18068, #15374, #3433, #18336, #9270 ),
 .UNSPECIFIED., .F., .F.,
 ( 4, 3, 4 ),
 ( 3.198396408832238080E-18, 0.0002299780670421061460, 0.0004597478348665241538 ),
 .UNSPECIFIED. ) ;
#11217=CARTESIAN_POINT ( 'NONE',  ( 16.56753206892534891, 0.006669401563384923931, -0.006760771273036191367 ) ) ;
#11218=CARTESIAN_POINT ( 'NONE',  ( 0.4862570985993252548, 10.79774104611373353, 8.769551628660776643 ) ) ;
#11220=CARTESIAN_POINT ( 'NONE',  ( 8.522092701127531811, 6.946128462138595694, 0.3779863304871469154 ) ) ;
#11221=VECTOR ( 'NONE', #10471, 1000.000000000000000 ) ;
#11226=CARTESIAN_POINT ( 'NONE',  ( 1.846138399168762101, 6.971848976711159551, -10.30487220521562541 ) ) ;
#11231=FACE_OUTER_BOUND ( 'NONE', #12134, .T. ) ;
#11235=EDGE_CURVE ( 'NONE', #5038, #16664, #17932, .T. ) ;
#11236=ADVANCED_FACE ( 'NONE', ( #7712 ), #13715, .F. ) ;
#11238=CARTESIAN_POINT ( 'NONE',  ( 16.57210152137263393, -0.01214401161737629908, -0.008007331252333388036 ) ) ;
#11242=VERTEX_POINT ( 'NONE', #14953 ) ;
#11247=DIRECTION ( 'NONE',  ( 0.000000000000000000, 0.000000000000000000, 1.000000000000000000 ) ) ;
#11248=DIRECTION ( 'NONE',  ( 0.000000000000000000, 0.000000000000000000, 1.000000000000000000 ) ) ;
#11249=FACE_OUTER_BOUND ( 'NONE', #3514, .T. ) ;
#11253=CARTESIAN_POINT ( 'NONE',  ( 2.747332970342022840, 7.289199830147106596, 14.63517873738950037 ) ) ;
#11254=ADVANCED_FACE ( 'NONE', ( #12000 ), #4557, .F. ) ;
#11256=ADVANCED_FACE ( 'NONE', ( #631 ), #7756, .F. ) ;
#11259=ORIENTED_EDGE ( 'NONE', *, *, #1048, .T. ) ;
#11262=CARTESIAN_POINT ( 'NONE',  ( 3.950837973638668288, 0.000000000000000000, 0.000000000000000000 ) ) ;
#11264=CARTESIAN_POINT ( 'NONE',  ( 0.3720661004400040439, 4.951033743989640357, 12.89739157014194859 ) ) ;
#11266=CARTESIAN_POINT ( 'NONE',  ( 2.636624412714237309, 14.14563173255211126, 7.605649742762011556 ) ) ;
#11267=ORIENTED_EDGE ( 'NONE', *, *, #9709, .F. ) ;
#11269=CARTESIAN_POINT ( 'NONE',  ( 1.977436885025426250, 7.806953934146316776, 13.27782258181756880 ) ) ;
#11272=B_SPLINE_CURVE_WITH_KNOTS ( 'NONE', 3,
 ( #8595, #12890, #1235, #16148, #8790, #4108 ),
 .UNSPECIFIED., .F., .F.,
 ( 4, 2, 4 ),
 ( 4.336808689942017736E-19, 0.001500839035891552006, 0.003001678071783103578 ),
 .UNSPECIFIED. ) ;
#11273=CARTESIAN_POINT ( 'NONE',  ( 3.950837973638675393, -2.591948120961706792, -14.31366178983255466 ) ) ;
#11280=CARTESIAN_POINT ( 'NONE',  ( 16.58200780006414732, -0.002844973367390960309, -0.01080144354108991157 ) ) ;
#11283=CARTESIAN_POINT ( 'NONE',  ( 1.847412631396504246, -0.04315047898443813423, 12.44294644888238999 ) ) ;
#11284=VECTOR ( 'NONE', #14242, 1000.000000000000114 ) ;
#11289=ORIENTED_EDGE ( 'NONE', *, *, #12790, .F. ) ;
#11290=CARTESIAN_POINT ( 'NONE',  ( 0.4862570985993235340, 13.44146924561385958, -3.580942890621532371 ) ) ;
#11291=CARTESIAN_POINT ( 'NONE',  ( 1.977228804422632713, -13.27756617201330336, -7.806978995470745808 ) ) ;
#11296=FACE_OUTER_BOUND ( 'NONE', #3420, .T. ) ;
#11299=CARTESIAN_POINT ( 'NONE',  ( 8.522092701127531811, -6.722964936702084948, -1.786985377232103600 ) ) ;
#11303=B_SPLINE_CURVE_WITH_KNOTS ( 'NONE', 3,
 ( #11701, #9030, #10663, #17829, #1768, #13227 ),
 .UNSPECIFIED., .F., .F.,
 ( 4, 2, 4 ),
 ( 2.710505431213761085E-19, 0.001657017934712013297, 0.003314035869424026594 ),
 .UNSPECIFIED. ) ;
#11304=CARTESIAN_POINT ( 'NONE',  ( 0.4385251269669950269, -0.7363879510386354132, 13.84299131624729462 ) ) ;
#11307=CARTESIAN_POINT ( 'NONE',  ( 1.342453679581834924, 14.76648944001039254, -0.9602753779831244563 ) ) ;
#11311=LINE ( 'NONE', #11497, #2736 ) ;
#11312=CARTESIAN_POINT ( 'NONE',  ( 1.918921323896324749, 7.860085869556325378, -9.738309537478915701 ) ) ;
#11318=CARTESIAN_POINT ( 'NONE',  ( 0.4862570985993235340, -13.44146924561378498, -3.580942890621813923 ) ) ;
#11320=CARTESIAN_POINT ( 'NONE',  ( 0.3145729642390355241, -12.96842777670210189, 4.535980493005037140 ) ) ;
#11321=CARTESIAN_POINT ( 'NONE',  ( 8.438534575730034959, -0.2320579683290609485, 6.862570336891074874 ) ) ;
#11331=ORIENTED_EDGE ( 'NONE', *, *, #8189, .F. ) ;
#11335=CARTESIAN_POINT ( 'NONE',  ( 0.3095370825347234511, 4.681152801286343923, -12.91933430393602933 ) ) ;
#11336=CARTESIAN_POINT ( 'NONE',  ( 1.959212340397939123, 6.829000156128186561, 10.53510106265284563 ) ) ;
#11340=CARTESIAN_POINT ( 'NONE',  ( 2.747332970342022840, -11.45495994260709161, -11.66639548242820190 ) ) ;
#11341=B_SPLINE_CURVE_WITH_KNOTS ( 'NONE', 3,
 ( #15860, #1330, #2940, #7172, #1528, #12985 ),
 .UNSPECIFIED., .F., .F.,
 ( 4, 2, 4 ),
 ( 3.556447555475521540E-17, 0.0001825746017570587236, 0.0003651492035140818855 ),
 .UNSPECIFIED. ) ;
#11343=ORIENTED_EDGE ( 'NONE', *, *, #6109, .T. ) ;
#11344=ORIENTED_EDGE ( 'NONE', *, *, #12876, .F. ) ;
#11348=CARTESIAN_POINT ( 'NONE',  ( 3.353306896162457029, 13.62210141459500079, -3.007732942432275181 ) ) ;
#11352=ORIENTED_EDGE ( 'NONE', *, *, #17068, .F. ) ;
#11353=DIRECTION ( 'NONE',  ( 0.000000000000000000, 0.000000000000000000, 1.000000000000000000 ) ) ;
#11354=EDGE_CURVE ( 'NONE', #7378, #796, #1159, .T. ) ;
#11356=CARTESIAN_POINT ( 'NONE',  ( 2.123976203522053297, -1.531817366691861304, 15.54801196254786255 ) ) ;
#11359=CARTESIAN_POINT ( 'NONE',  ( 0.3095370825347234511, 3.806662003783410242, 13.20347358821915940 ) ) ;
#11368=CARTESIAN_POINT ( 'NONE',  ( 0.3058872367615230181, 8.562166468153717958, 10.75034008168919009 ) ) ;
#11377=FACE_OUTER_BOUND ( 'NONE', #16005, .T. ) ;
#11378=CARTESIAN_POINT ( 'NONE',  ( 3.950837973638676281, -1.958075594453890789, 14.41405733518059940 ) ) ;
#11380=CARTESIAN_POINT ( 'NONE',  ( 3.074695600508242421, -2.093687500613561348, -15.41438262616270194 ) ) ;
#11383=SHAPE_REPRESENTATION_RELATIONSHIP ( 'NONE' , 'NONE' ,  #18049, #556 ) ;
#11393=CARTESIAN_POINT ( 'NONE',  ( 0.3145729642390374670, 3.952965287571295949, -13.15786090015079957 ) ) ;
#11401=CARTESIAN_POINT ( 'NONE',  ( 0.3151928479966097374, 0.000000000000000000, -13.73922861026898623 ) ) ;
#11402=DIRECTION ( 'NONE',  ( 0.000000000000000000, 0.000000000000000000, 1.000000000000000000 ) ) ;
#11405=AXIS2_PLACEMENT_3D ( 'NONE', #11915, #5878, #7529 ) ;
#11410=CARTESIAN_POINT ( 'NONE',  ( 0.3137051932979809665, -13.20008686438108647, 3.805684345189735307 ) ) ;
#11411=CARTESIAN_POINT ( 'NONE',  ( 1.847426409206450959, -2.029922383240494730E-11, 12.44303504652081038 ) ) ;
#11412=CARTESIAN_POINT ( 'NONE',  ( 0.3170788640506441158, 11.02668139258453905, -8.200855617524412722 ) ) ;
#11415=CARTESIAN_POINT ( 'NONE',  ( 0.3137051932979775248, 10.83767969834815581, -8.442169467526731808 ) ) ;
#11418=ORIENTED_EDGE ( 'NONE', *, *, #10909, .F. ) ;
#11420=MECHANICAL_DESIGN_GEOMETRIC_PRESENTATION_REPRESENTATION('',(#14462),#8622);
#11423=ORIENTED_EDGE ( 'NONE', *, *, #6506, .F. ) ;
#11426=CARTESIAN_POINT ( 'NONE',  ( 0.3058872367615226295, -0.6080468242581913429, 13.72992299905059888 ) ) ;
#11428=CARTESIAN_POINT ( 'NONE',  ( 0.3132635586635958425, -12.89236642382225462, 4.743936529203192087 ) ) ;
#11433=ORIENTED_EDGE ( 'NONE', *, *, #13834, .T. ) ;
#11434=B_SPLINE_CURVE_WITH_KNOTS ( 'NONE', 3,
 ( #312, #17608, #7589, #117, #7773, #13395 ),
 .UNSPECIFIED., .F., .F.,
 ( 4, 2, 4 ),
 ( 0.000000000000000000, 0.0002017457492448075543, 0.0004034914984896151085 ),
 .UNSPECIFIED. ) ;
#11441=CARTESIAN_POINT ( 'NONE',  ( 16.56753206892534891, -0.008432171035096412345, -0.004368917149004214288 ) ) ;
#11446=CARTESIAN_POINT ( 'NONE',  ( 8.522092701127531811, -3.777034505568564349, 5.841710761610117153 ) ) ;
#11464=CARTESIAN_POINT ( 'NONE',  ( 0.4862570985993252548, 12.97920246947879441, 5.003653737315533867 ) ) ;
#11468=CARTESIAN_POINT ( 'NONE',  ( 16.57210152137263393, 0.0006600038696347836076, 0.01453130299868640209 ) ) ;
#11471=CARTESIAN_POINT ( 'NONE',  ( 0.3170788640506441158, 13.11595226728158003, 4.100430649998006771 ) ) ;
#11479=CARTESIAN_POINT ( 'NONE',  ( 0.3095370825347224519, 3.806662003783598536, -13.20347358821910433 ) ) ;
#11485=AXIS2_PLACEMENT_3D ( 'NONE', #9901, #8658, #12772 ) ;
#11486=CARTESIAN_POINT ( 'NONE',  ( 0.3308579732647026761, -0.5950689966505304795, 13.74211098745268522 ) ) ;
#11497=CARTESIAN_POINT ( 'NONE',  ( 8.522092701127531811, 1.786985377232031436, 6.722964936702105376 ) ) ;
#11499=CARTESIAN_POINT ( 'NONE',  ( 16.56822296793089322, 0.007741272030791174728, -0.006547366384936662183 ) ) ;
#11515=CARTESIAN_POINT ( 'NONE',  ( 2.636624412715384391, -11.60464335004044223, -11.10302021258006278 ) ) ;
#11520=DIRECTION ( 'NONE',  ( 0.000000000000000000, 0.000000000000000000, 1.000000000000000000 ) ) ;
#11523=CARTESIAN_POINT ( 'NONE',  ( 16.56872352241294521, 0.01033355228142401709, -0.001442253899401843694 ) ) ;
#11525=CARTESIAN_POINT ( 'NONE',  ( 1.959283090834838426, 3.239245055717136168, -12.12982544407801555 ) ) ;
#11530=( BOUNDED_SURFACE ( )  B_SPLINE_SURFACE ( 3, 1, ( 
 ( #14065, #9669 ),
 ( #6806, #9840 ),
 ( #970, #18452 ),
 ( #2575, #15495 ) ),
 .UNSPECIFIED., .F., .F., .T. ) 
 B_SPLINE_SURFACE_WITH_KNOTS ( ( 4, 4 ),
 ( 2, 2 ),
 ( 0.000000000000000000, 1.000000000000000000 ),
 ( 0.000000000000000000, 1.000000000000000000 ),
 .UNSPECIFIED. ) 
 GEOMETRIC_REPRESENTATION_ITEM ( )  RATIONAL_B_SPLINE_SURFACE ( (
 ( 1.000000000000000000, 1.000000000000000000),
 ( 0.9593108457356467333, 0.9995965569486454649),
 ( 0.9593108457356467333, 0.9995965569486454649),
 ( 1.000000000000000000, 1.000000000000000000) ) ) 
 REPRESENTATION_ITEM ( '' )  SURFACE ( )  );
#11535=VERTEX_POINT ( 'NONE', #18180 ) ;
#11536=CARTESIAN_POINT ( 'NONE',  ( 1.847461586945732703, 3.813310247068605552, -11.84459954310606378 ) ) ;
#11541=ADVANCED_FACE ( 'NONE', ( #16748 ), #9688, .F. ) ;
#11544=CARTESIAN_POINT ( 'NONE',  ( 16.56753206892534891, -0.006669401563384967299, 0.006760771273036151469 ) ) ;
#11545=CARTESIAN_POINT ( 'NONE',  ( 0.3151930723728477157, -11.16020735774772277, 8.013866567350856229 ) ) ;
#11550=CARTESIAN_POINT ( 'NONE',  ( 1.847247051441598176, -4.004229874809106526, 11.78111530882021185 ) ) ;
#11551=VERTEX_POINT ( 'NONE', #16375 ) ;
#11553=VERTEX_POINT ( 'NONE', #7971 ) ;
#11554=VERTEX_POINT ( 'NONE', #7686 ) ;
#11558=FACE_OUTER_BOUND ( 'NONE', #18070, .T. ) ;
#11559=CARTESIAN_POINT ( 'NONE',  ( 1.847380140988740926, 11.86779270755359050, 3.740232970470796392 ) ) ;
#11561=CARTESIAN_POINT ( 'NONE',  ( 0.3095370825347224519, -3.806662003783324089, -13.20347358821918249 ) ) ;
#11567=( BOUNDED_SURFACE ( )  B_SPLINE_SURFACE ( 3, 1, ( 
 ( #17175, #17467 ),
 ( #2820, #3994 ),
 ( #8305, #7151 ),
 ( #15640, #5694 ) ),
 .UNSPECIFIED., .F., .F., .T. ) 
 B_SPLINE_SURFACE_WITH_KNOTS ( ( 4, 4 ),
 ( 2, 2 ),
 ( 0.000000000000000000, 1.000000000000000000 ),
 ( 0.000000000000000000, 1.000000000000000000 ),
 .UNSPECIFIED. ) 
 GEOMETRIC_REPRESENTATION_ITEM ( )  RATIONAL_B_SPLINE_SURFACE ( (
 ( 1.000000000000000000, 1.000000000000000000),
 ( 0.7792777138730158093, 0.9689936506012928330),
 ( 0.7792777138730158093, 0.9689936506012928330),
 ( 1.000000000000000000, 1.000000000000000000) ) ) 
 REPRESENTATION_ITEM ( '' )  SURFACE ( )  );
#11568=CARTESIAN_POINT ( 'NONE',  ( 0.3148208552358935930, -13.13564827777586785, -4.026279359288564841 ) ) ;
#11569=EDGE_CURVE ( 'NONE', #11211, #1652, #15285, .T. ) ;
#11580=VERTEX_POINT ( 'NONE', #9392 ) ;
#11583=ORIENTED_EDGE ( 'NONE', *, *, #4126, .F. ) ;
#11584=CARTESIAN_POINT ( 'NONE',  ( 1.847034903785825577, 9.929438108952146180, 7.498375632854650696 ) ) ;
#11593=ADVANCED_FACE ( 'NONE', ( #13695 ), #1767, .F. ) ;
#11598=CARTESIAN_POINT ( 'NONE',  ( 1.847168016377985333, 4.022276579849959788, 11.77471791462000184 ) ) ;
#11602=ORIENTED_EDGE ( 'NONE', *, *, #4609, .T. ) ;
#11603=ORIENTED_EDGE ( 'NONE', *, *, #8782, .F. ) ;
#11606=CARTESIAN_POINT ( 'NONE',  ( 3.950837973638668288, 0.000000000000000000, 0.000000000000000000 ) ) ;
#11611=CARTESIAN_POINT ( 'NONE',  ( 16.56753206892534891, 0.004368917149005333185, 0.008432171035096464387 ) ) ;
#11614=CARTESIAN_POINT ( 'NONE',  ( 0.3308579732647013438, -3.680601586799781000, -13.25341063505879546 ) ) ;
#11615=CARTESIAN_POINT ( 'NONE',  ( 0.3137051932979792457, -10.83767969834796929, -8.442169467526971616 ) ) ;
#11617=EDGE_CURVE ( 'NONE', #11535, #11022, #9836, .T. ) ;
#11623=VERTEX_POINT ( 'NONE', #13964 ) ;
#11624=ORIENTED_EDGE ( 'NONE', *, *, #1070, .F. ) ;
#11628=CARTESIAN_POINT ( 'NONE',  ( 0.4754618798421162973, 10.80499583390512974, 8.775436892861156579 ) ) ;
#11636=CARTESIAN_POINT ( 'NONE',  ( 0.3150686449036064207, -11.02450593298024195, 8.199336701264503091 ) ) ;
#11637=EDGE_CURVE ( 'NONE', #18802, #17659, #4793, .T. ) ;
#11638=FACE_OUTER_BOUND ( 'NONE', #8396, .T. ) ;
#11639=CARTESIAN_POINT ( 'NONE',  ( 0.4754618798421162973, -11.68486377711960955, -7.564402563418597403 ) ) ;
#11642=( BOUNDED_SURFACE ( )  B_SPLINE_SURFACE ( 3, 1, ( 
 ( #17666, #4660 ),
 ( #10390, #16224 ),
 ( #3107, #14779 ),
 ( #266, #17759 ) ),
 .UNSPECIFIED., .F., .F., .T. ) 
 B_SPLINE_SURFACE_WITH_KNOTS ( ( 4, 4 ),
 ( 2, 2 ),
 ( 0.000000000000000000, 1.000000000000000000 ),
 ( 0.000000000000000000, 1.000000000000000000 ),
 .UNSPECIFIED. ) 
 GEOMETRIC_REPRESENTATION_ITEM ( )  RATIONAL_B_SPLINE_SURFACE ( (
 ( 1.000000000000000000, 1.000000000000000000),
 ( 0.9933953342250438912, 0.8357391271907739227),
 ( 0.9933953342250438912, 0.8357391271907739227),
 ( 1.000000000000000000, 1.000000000000000000) ) ) 
 REPRESENTATION_ITEM ( '' )  SURFACE ( )  );
#11643=CARTESIAN_POINT ( 'NONE',  ( 0.3137051932979792457, -7.698472063774386420, -11.37800749014139612 ) ) ;
#11645=ORIENTED_EDGE ( 'NONE', *, *, #1825, .T. ) ;
#11646=EDGE_LOOP ( 'NONE', ( #7721, #11418, #12672, #8532 ) ) ;
#11648=ORIENTED_EDGE ( 'NONE', *, *, #1729, .T. ) ;
#11650=ADVANCED_FACE ( 'NONE', ( #11296 ), #690, .F. ) ;
#11653=CARTESIAN_POINT ( 'NONE',  ( 3.664313757352970047, -9.645155442698829518, 10.50730552161229880 ) ) ;
#11655=CARTESIAN_POINT ( 'NONE',  ( 16.56679352167444819, 0.004277682826583292797, 0.008252760440870202802 ) ) ;
#11661=CARTESIAN_POINT ( 'NONE',  ( 0.3132642857406529591, -8.495623922778147374, 10.79548167658031588 ) ) ;
#11664=ORIENTED_EDGE ( 'NONE', *, *, #109, .F. ) ;
#11671=ORIENTED_EDGE ( 'NONE', *, *, #2206, .T. ) ;
#11672=CARTESIAN_POINT ( 'NONE',  ( 2.636624412715138366, -15.91454522070249311, -2.161493821597819665 ) ) ;
#11683=CARTESIAN_POINT ( 'NONE',  ( 2.636624412716902288, 7.605649742760546950, -14.14563173255513995 ) ) ;
#11698=CARTESIAN_POINT ( 'NONE',  ( 0.3307726912345211323, -0.5948952607471654774, -13.74203354050372461 ) ) ;
#11700=FACE_OUTER_BOUND ( 'NONE', #14229, .T. ) ;
#11701=CARTESIAN_POINT ( 'NONE',  ( 0.4862570985993235340, 7.559321496869593204, -11.67702470553357053 ) ) ;
#11705=EDGE_CURVE ( 'NONE', #1072, #13213, #6623, .T. ) ;
#11706=B_SPLINE_CURVE_WITH_KNOTS ( 'NONE', 3,
 ( #9506, #7714, #4839, #18024, #1969, #10668, #438, #6458, #12282, #15331, #4928, #12099, #10763 ),
 .UNSPECIFIED., .F., .F.,
 ( 4, 3, 3, 3, 4 ),
 ( 3.127317220692750759E-18, 0.0002299780670421087210, 0.0004599561239687931019, 0.0006896788984287912077, 0.0009194956271626412558 ),
 .UNSPECIFIED. ) ;
#11711=CARTESIAN_POINT ( 'NONE',  ( 2.705023505549866591, -8.489131503859701056, -10.24007717649589821 ) ) ;
#11712=VECTOR ( 'NONE', #4242, 1000.000000000000114 ) ;
#11718=EDGE_LOOP ( 'NONE', ( #16435, #16188, #11887, #15294 ) ) ;
#11719=VERTEX_POINT ( 'NONE', #11110 ) ;
#11720=CARTESIAN_POINT ( 'NONE',  ( 1.959212340397940899, -12.12975361829678178, 3.239239832448982170 ) ) ;
#11721=B_SPLINE_CURVE_WITH_KNOTS ( 'NONE', 3,
 ( #1649, #1950, #7694, #11884, #3166, #3267, #13407, #4818, #323, #10649, #6152, #11980, #17815 ),
 .UNSPECIFIED., .F., .F.,
 ( 4, 3, 3, 3, 4 ),
 ( 1.734723475976807094E-18, 0.0002299780670421052245, 0.0004599561239687887651, 0.0006896788984287890393, 0.0009194956271626402800 ),
 .UNSPECIFIED. ) ;
#11730=CARTESIAN_POINT ( 'NONE',  ( 3.377929128793396796, -1.296196549818846355, -13.92579934231097560 ) ) ;
#11734=CARTESIAN_POINT ( 'NONE',  ( 2.636624412714236865, 0.000000000000000000, 0.000000000000000000 ) ) ;
#11737=B_SPLINE_CURVE_WITH_KNOTS ( 'NONE', 3,
 ( #3895, #15544, #7842, #8656, #12860, #11536, #1014, #7048, #15920, #17455, #4362, #10187, #7138 ),
 .UNSPECIFIED., .F., .F.,
 ( 4, 3, 3, 3, 4 ),
 ( 1.734723475976806902E-18, 0.0002299804304191479859, 0.0004599608082120235455, 0.0006467586077647999570, 0.0008336169836825983986 ),
 .UNSPECIFIED. ) ;
#11739=ORIENTED_EDGE ( 'NONE', *, *, #13914, .F. ) ;
#11744=CARTESIAN_POINT ( 'NONE',  ( 2.636624412717099908, 14.46769361191384817, -6.973567714910368309 ) ) ;
#11747=CARTESIAN_POINT ( 'NONE',  ( 2.636624412716045196, 11.10302021257998994, -11.60464335004042447 ) ) ;
#11748=CARTESIAN_POINT ( 'NONE',  ( 16.56753206892534891, 0.006669401563385194548, 0.006760771273035138390 ) ) ;
#11751=ORIENTED_EDGE ( 'NONE', *, *, #462, .F. ) ;
#11757=CARTESIAN_POINT ( 'NONE',  ( 0.3132642857406526260, 8.495623922778223758, -10.79548167658025193 ) ) ;
#11761=ADVANCED_FACE ( 'NONE', ( #5722 ), #6518, .F. ) ;
#11767=CARTESIAN_POINT ( 'NONE',  ( 0.3148208552358927603, 7.888357771040864996, -11.24855514421867042 ) ) ;
#11770=CARTESIAN_POINT ( 'NONE',  ( 0.3148213771069373057, 4.463459503829174224, -12.99360322443197724 ) ) ;
#11771=B_SPLINE_CURVE_WITH_KNOTS ( 'NONE', 3,
 ( #9543, #8127, #16812, #12417, #760, #15462 ),
 .UNSPECIFIED., .F., .F.,
 ( 4, 2, 4 ),
 ( 0.000000000000000000, 0.001656992708823638600, 0.003313985417647277200 ),
 .UNSPECIFIED. ) ;
#11778=CARTESIAN_POINT ( 'NONE',  ( 16.57605080000000086, 0.000000000000000000, 2.500000000000000000 ) ) ;
#11779=CARTESIAN_POINT ( 'NONE',  ( 16.56872352241294521, -0.009207754980063714498, -0.004907101719994726684 ) ) ;
#11784=VECTOR ( 'NONE', #5214, 999.9999999999998863 ) ;
#11785=CARTESIAN_POINT ( 'NONE',  ( 1.959283090834855745, 0.6676170829052219258, 12.53713130127477982 ) ) ;
#11786=CARTESIAN_POINT ( 'NONE',  ( 3.950837973638675393, 6.888253895133292559, 12.81214529934977797 ) ) ;
#11790=CARTESIAN_POINT ( 'NONE',  ( 1.342453679581834924, -7.902645620902536194, 12.51077660954462978 ) ) ;
#11791=( BOUNDED_SURFACE ( )  B_SPLINE_SURFACE ( 3, 1, ( 
 ( #9173, #4779 ),
 ( #17879, #16451 ),
 ( #16901, #8303 ),
 ( #5056, #3807 ) ),
 .UNSPECIFIED., .F., .F., .T. ) 
 B_SPLINE_SURFACE_WITH_KNOTS ( ( 4, 4 ),
 ( 2, 2 ),
 ( 0.000000000000000000, 1.000000000000000000 ),
 ( 0.000000000000000000, 1.000000000000000000 ),
 .UNSPECIFIED. ) 
 GEOMETRIC_REPRESENTATION_ITEM ( )  RATIONAL_B_SPLINE_SURFACE ( (
 ( 1.000000000000000000, 1.000000000000000000),
 ( 0.7792777138730158093, 0.9689936506012928330),
 ( 0.7792777138730158093, 0.9689936506012928330),
 ( 1.000000000000000000, 1.000000000000000000) ) ) 
 REPRESENTATION_ITEM ( '' )  SURFACE ( )  );
#11801=CARTESIAN_POINT ( 'NONE',  ( 16.57778382496167424, -0.01354073047775762942, -0.006312874906843820091 ) ) ;
#11802=FACE_OUTER_BOUND ( 'NONE', #14506, .T. ) ;
#11804=CARTESIAN_POINT ( 'NONE',  ( 0.4754618798421162973, -7.564402563418551217, 11.68486377711963975 ) ) ;
#11805=CARTESIAN_POINT ( 'NONE',  ( 1.342453679581834924, -9.456403821038877666, 11.38190519890850183 ) ) ;
#11807=CARTESIAN_POINT ( 'NONE',  ( 1.918918678667047129, 4.466049546133911363, 11.69059232068580556 ) ) ;
#11813=LINE ( 'NONE', #10376, #6942 ) ;
#11816=B_SPLINE_CURVE_WITH_KNOTS ( 'NONE', 3,
 ( #13862, #11012, #18353, #780, #17024, #12609 ),
 .UNSPECIFIED., .F., .F.,
 ( 4, 2, 4 ),
 ( 4.240893905418535831E-17, 0.0002014099069817287303, 0.0004028198139634150141 ),
 .UNSPECIFIED. ) ;
#11819=EDGE_LOOP ( 'NONE', ( #12077, #1030, #18782, #12062 ) ) ;
#11832=CARTESIAN_POINT ( 'NONE',  ( 1.847412631396504690, 0.04315047898452520347, -12.44294644888238643 ) ) ;
#11833=CARTESIAN_POINT ( 'NONE',  ( 0.3058872367615230181, -11.46514199369352482, -7.578326039752732335 ) ) ;
#11836=CARTESIAN_POINT ( 'NONE',  ( 0.3150692679895937820, -7.951395415075003470, -11.20465057551034604 ) ) ;
#11840=EDGE_LOOP ( 'NONE', ( #7894, #9274, #7374, #10705 ) ) ;
#11841=ORIENTED_EDGE ( 'NONE', *, *, #5321, .T. ) ;
#11842=CARTESIAN_POINT ( 'NONE',  ( 1.845755665168035575, 9.776700214454821847, 7.694641135843453661 ) ) ;
#11844=CARTESIAN_POINT ( 'NONE',  ( 0.3058872367615226295, -11.46514199369363318, 7.578326039752564469 ) ) ;
#11845=CARTESIAN_POINT ( 'NONE',  ( 0.3170788640506440603, -13.02120094575825249, -4.392045232375947350 ) ) ;
#11847=CARTESIAN_POINT ( 'NONE',  ( 1.846138399168762101, -0.4167076046094680408, -12.43476674860266940 ) ) ;
#11857=ORIENTED_EDGE ( 'NONE', *, *, #8921, .T. ) ;
#11859=CARTESIAN_POINT ( 'NONE',  ( 1.846138399168762101, -10.30487220521574976, 6.971848976710974810 ) ) ;
#11863=CARTESIAN_POINT ( 'NONE',  ( 16.56782317627811096, -0.003357783021327304974, 0.009228812961909584403 ) ) ;
#11869=( BOUNDED_SURFACE ( )  B_SPLINE_SURFACE ( 3, 1, ( 
 ( #16580, #2470 ),
 ( #14238, #14135 ),
 ( #15041, #9408 ),
 ( #2055, #18536 ) ),
 .UNSPECIFIED., .F., .F., .T. ) 
 B_SPLINE_SURFACE_WITH_KNOTS ( ( 4, 4 ),
 ( 2, 2 ),
 ( 0.000000000000000000, 1.000000000000000000 ),
 ( 0.000000000000000000, 1.000000000000000000 ),
 .UNSPECIFIED. ) 
 GEOMETRIC_REPRESENTATION_ITEM ( )  RATIONAL_B_SPLINE_SURFACE ( (
 ( 1.000000000000000000, 1.000000000000000000),
 ( 0.9933953342250438912, 0.8357391271907739227),
 ( 0.9933953342250438912, 0.8357391271907739227),
 ( 1.000000000000000000, 1.000000000000000000) ) ) 
 REPRESENTATION_ITEM ( '' )  SURFACE ( )  );
#11870=VERTEX_POINT ( 'NONE', #1242 ) ;
#11873=CARTESIAN_POINT ( 'NONE',  ( 3.074695600507272086, -2.093687500612061658, 15.41438262616222765 ) ) ;
#11876=EDGE_CURVE ( 'NONE', #17620, #2287, #12900, .T. ) ;
#11883=VERTEX_POINT ( 'NONE', #4502 ) ;
#11884=CARTESIAN_POINT ( 'NONE',  ( 0.3148213771069381384, -4.463459503829087183, 12.99360322443201277 ) ) ;
#11887=ORIENTED_EDGE ( 'NONE', *, *, #15789, .F. ) ;
#11890=CARTESIAN_POINT ( 'NONE',  ( 2.002547531651519996, -3.242439124566736997, 12.17374746633577232 ) ) ;
#11894=ADVANCED_FACE ( 'NONE', ( #15443 ), #9568, .F. ) ;
#11896=FACE_OUTER_BOUND ( 'NONE', #16212, .T. ) ;
#11901=CARTESIAN_POINT ( 'NONE',  ( 0.4862570985993235340, 10.79774104611385965, -8.769551628660616771 ) ) ;
#11903=CARTESIAN_POINT ( 'NONE',  ( 0.3939822652208134768, -3.598529276937167953, -13.34132036472940896 ) ) ;
#11906=CARTESIAN_POINT ( 'NONE',  ( 0.4385251269669945273, -7.540955776459655091, -11.63205320541531052 ) ) ;
#11909=ORIENTED_EDGE ( 'NONE', *, *, #14876, .F. ) ;
#11914=EDGE_CURVE ( 'NONE', #18549, #1302, #1453, .T. ) ;
#11915=CARTESIAN_POINT ( 'NONE',  ( 16.57605080000000086, 0.000000000000000000, 0.000000000000000000 ) ) ;
#11917=CARTESIAN_POINT ( 'NONE',  ( 1.845755665166725290, 0.4784952423730285953, -12.43231320373360660 ) ) ;
#11921=CARTESIAN_POINT ( 'NONE',  ( 16.56872352241294521, -0.004564908236400030961, 0.009382111268607351909 ) ) ;
#11924=CARTESIAN_POINT ( 'NONE',  ( 0.4862570985993252548, -5.003653737315580052, 12.97920246947877665 ) ) ;
#11941=CARTESIAN_POINT ( 'NONE',  ( 1.846138399168762101, 10.30487220521580305, -6.971848976710897539 ) ) ;
#11945=CARTESIAN_POINT ( 'NONE',  ( 2.705023505549867036, 12.88681800078732387, 3.294610156755938934 ) ) ;
#11948=CARTESIAN_POINT ( 'NONE',  ( 1.847380140988738262, -10.00162556679656234, 7.402792205949069171 ) ) ;
#11950=CARTESIAN_POINT ( 'NONE',  ( 3.377929128793398572, 3.070552481925057364, -13.64476897106781017 ) ) ;
#11954=CIRCLE ( 'NONE', #14380, 14.54644660717763927 ) ;
#11959=DIRECTION ( 'NONE',  ( 0.000000000000000000, 0.000000000000000000, 1.000000000000000000 ) ) ;
#11975=B_SPLINE_CURVE_WITH_KNOTS ( 'NONE', 3,
 ( #16948, #3850, #9681, #15506, #11034, #9765 ),
 .UNSPECIFIED., .F., .F.,
 ( 4, 2, 4 ),
 ( 3.527508043940425264E-17, 0.0001825746017570591031, 0.0003651492035140829697 ),
 .UNSPECIFIED. ) ;
#11976=CARTESIAN_POINT ( 'NONE',  ( 16.56782317627811096, -0.005492611183757366636, 0.008141063682853383679 ) ) ;
#11980=CARTESIAN_POINT ( 'NONE',  ( 0.3142011359265320380, -3.879426116491784260, 13.17934269988456819 ) ) ;
#11988=CIRCLE ( 'NONE', #7408, 16.06066017081991149 ) ;
#11994=CARTESIAN_POINT ( 'NONE',  ( 2.002547531651519996, -12.57989064830760206, 0.6781519942171299054 ) ) ;
#11996=CARTESIAN_POINT ( 'NONE',  ( 0.3137051932979792457, -0.4596302728640728752, 13.73004976592201842 ) ) ;
#11997=DIRECTION ( 'NONE',  ( 1.000000000000000000, 0.000000000000000000, 0.000000000000000000 ) ) ;
#11998=ADVANCED_FACE ( 'NONE', ( #6847 ), #16784, .F. ) ;
#12000=FACE_OUTER_BOUND ( 'NONE', #18368, .T. ) ;
#12003=CARTESIAN_POINT ( 'NONE',  ( 0.3145734862173251711, 13.73540602248380971, 0.3064017202075832724 ) ) ;
#12015=CARTESIAN_POINT ( 'NONE',  ( 0.3308579732646998450, 13.74211098745269766, 0.5950689966504839612 ) ) ;
#12021=ADVANCED_FACE ( 'NONE', ( #5312 ), #5763, .F. ) ;
#12023=CARTESIAN_POINT ( 'NONE',  ( 1.846524061778019199, 0.3544704288994222074, -12.43723828841088164 ) ) ;
#12024=CARTESIAN_POINT ( 'NONE',  ( 1.846138399168762101, -9.815003036200353748, -7.646096044340000120 ) ) ;
#12030=ORIENTED_EDGE ( 'NONE', *, *, #17968, .T. ) ;
#12034=CARTESIAN_POINT ( 'NONE',  ( 0.4862570985993235340, -0.7479633556563419772, 13.89016912371017121 ) ) ;
#12035=VECTOR ( 'NONE', #12321, 1000.000000000000000 ) ;
#12040=LINE ( 'NONE', #17778, #11154 ) ;
#12043=CARTESIAN_POINT ( 'NONE',  ( 0.3151926232592501265, 13.09050869763092884, 4.172630140040843649 ) ) ;
#12044=CARTESIAN_POINT ( 'NONE',  ( 16.58200780006414732, 0.009393638146078525306, 0.006043560077721743008 ) ) ;
#12045=CARTESIAN_POINT ( 'NONE',  ( 16.56872352241294521, -0.007240717549633937135, 0.007512283835805527027 ) ) ;
#12046=CARTESIAN_POINT ( 'NONE',  ( 3.950837973638676281, -12.81214529934970336, -6.888253895133431115 ) ) ;
#12047=ADVANCED_FACE ( 'NONE', ( #5578 ), #5165, .F. ) ;
#12048=CARTESIAN_POINT ( 'NONE',  ( 2.636624412714994037, -14.46769361191274328, -6.973567714907344950 ) ) ;
#12052=CARTESIAN_POINT ( 'NONE',  ( 0.3137051932979775248, 0.4596302728639756197, 13.73004976592202198 ) ) ;
#12056=CONICAL_SURFACE ( 'NONE', #3802, 14.54644660717763927, 0.8559913436420816257 ) ;
#12059=ORIENTED_EDGE ( 'NONE', *, *, #16689, .T. ) ;
#12060=CARTESIAN_POINT ( 'NONE',  ( 8.438534575730034959, -4.221456476902624821, -5.415535776177568650 ) ) ;
#12062=ORIENTED_EDGE ( 'NONE', *, *, #1729, .F. ) ;
#12064=DIRECTION ( 'NONE',  ( -0.7635533937278216055, -0.6453904417649388714, 0.02138673900301666167 ) ) ;
#12069=AXIS2_PLACEMENT_3D ( 'NONE', #10408, #18059, #16539 ) ;
#12070=ADVANCED_FACE ( 'NONE', ( #17539 ), #17616, .F. ) ;
#12071=CARTESIAN_POINT ( 'NONE',  ( 1.959283090834840646, -6.829027319138321062, 10.53516775895158020 ) ) ;
#12077=ORIENTED_EDGE ( 'NONE', *, *, #4987, .F. ) ;
#12081=CARTESIAN_POINT ( 'NONE',  ( 0.3151930723728413875, -8.137566970826446422, 11.07033375389128871 ) ) ;
#12082=CARTESIAN_POINT ( 'NONE',  ( 3.950837973638676281, -14.41405733518059229, -1.958075594453940971 ) ) ;
#12088=CARTESIAN_POINT ( 'NONE',  ( 1.918921323896325193, 3.258415356426521026, 12.08297777410666285 ) ) ;
#12091=CARTESIAN_POINT ( 'NONE',  ( 0.4862570985993235340, 13.89016912371017476, -0.7479633556562934604 ) ) ;
#12093=AXIS2_PLACEMENT_3D ( 'NONE', #7120, #12940, #5571 ) ;
#12095=DIRECTION ( 'NONE',  ( 0.000000000000000000, 0.000000000000000000, 1.000000000000000000 ) ) ;
#12097=CARTESIAN_POINT ( 'NONE',  ( 16.56822296793089322, -0.003834730849371946210, -0.009385634690642043892 ) ) ;
#12098=CARTESIAN_POINT ( 'NONE',  ( 0.3137051932979792457, -11.37800749014136592, 7.698472063774431717 ) ) ;
#12099=CARTESIAN_POINT ( 'NONE',  ( 0.3142011359265305392, 8.382042760265909109, 10.88514493056445076 ) ) ;
#12103=CARTESIAN_POINT ( 'NONE',  ( 8.522092701127531811, 6.489356537178224471, -2.505958102592553693 ) ) ;
#12106=VERTEX_POINT ( 'NONE', #6170 ) ;
#12108=AXIS2_PLACEMENT_3D ( 'NONE', #14373, #12843, #11520 ) ;
#12110=B_SPLINE_CURVE_WITH_KNOTS ( 'NONE', 3,
 ( #6668, #564, #6389, #12392, #15263, #12219 ),
 .UNSPECIFIED., .F., .F.,
 ( 4, 2, 4 ),
 ( 1.748223473168675632E-18, 0.0002017457492448079337, 0.0004034914984896141327 ),
 .UNSPECIFIED. ) ;
#12115=CARTESIAN_POINT ( 'NONE',  ( 3.512766787570702043, -7.127386085302744867, -13.25664064834487021 ) ) ;
#12116=ADVANCED_FACE ( 'NONE', ( #14571 ), #10801, .T. ) ;
#12121=FACE_OUTER_BOUND ( 'NONE', #10211, .T. ) ;
#12123=AXIS2_PLACEMENT_3D ( 'NONE', #5433, #12600, #11005 ) ;
#12124=CARTESIAN_POINT ( 'NONE',  ( 1.847372867223026738, 0.1054171785008226614, -12.44269075185938433 ) ) ;
#12125=CARTESIAN_POINT ( 'NONE',  ( 1.977228804421385044, 15.04020501276069588, 3.321884655132254505 ) ) ;
#12126=CARTESIAN_POINT ( 'NONE',  ( 0.3170788640506441158, 0.1533108587036162707, 13.74111462631963576 ) ) ;
#12128=CARTESIAN_POINT ( 'NONE',  ( 2.697797270744668019, 11.26906156738836984, -7.053988368581739721 ) ) ;
#12131=VERTEX_POINT ( 'NONE', #13428 ) ;
#12133=VECTOR ( 'NONE', #3561, 1000.000000000000000 ) ;
#12134=EDGE_LOOP ( 'NONE', ( #17678, #13727, #5184, #15205 ) ) ;
#12137=CONICAL_SURFACE ( 'NONE', #14558, 14.54644660717763927, 0.8559913436420816257 ) ;
#12142=ORIENTED_EDGE ( 'NONE', *, *, #1914, .T. ) ;
#12148=CARTESIAN_POINT ( 'NONE',  ( 0.4754618798421167414, 13.89949764182682657, 0.7484603771384882309 ) ) ;
#12151=CARTESIAN_POINT ( 'NONE',  ( 0.3137051932979792457, 0.4596302728641686874, -13.73004976592201487 ) ) ;
#12152=ORIENTED_EDGE ( 'NONE', *, *, #4338, .F. ) ;
#12153=DIRECTION ( 'NONE',  ( 0.000000000000000000, 0.000000000000000000, 1.000000000000000000 ) ) ;
#12154=CARTESIAN_POINT ( 'NONE',  ( 1.846138399168762101, 11.69739621335927815, -4.238866729160283064 ) ) ;
#12157=CARTESIAN_POINT ( 'NONE',  ( 0.3720661004400037664, 11.58636699658225844, -7.524064345033335321 ) ) ;
#12159=EDGE_LOOP ( 'NONE', ( #18815, #3470, #10660, #15269 ) ) ;
#12163=CARTESIAN_POINT ( 'NONE',  ( 1.342453679581834924, 7.902645620902629453, -12.51077660954457293 ) ) ;
#12165=LINE ( 'NONE', #4899, #3329 ) ;
#12166=CARTESIAN_POINT ( 'NONE',  ( 0.3170788640506441158, 11.20690911610903839, 7.952793437297615675 ) ) ;
#12167=CARTESIAN_POINT ( 'NONE',  ( 2.636624412715137922, -6.973567714907947135, 14.46769361191283920 ) ) ;
#12168=ORIENTED_EDGE ( 'NONE', *, *, #4123, .F. ) ;
#12176=ORIENTED_EDGE ( 'NONE', *, *, #14937, .T. ) ;
#12177=CARTESIAN_POINT ( 'NONE',  ( 3.950837973638677170, 13.10350451991849141, -6.316429227969337923 ) ) ;
#12181=ORIENTED_EDGE ( 'NONE', *, *, #489, .T. ) ;
#12187=EDGE_CURVE ( 'NONE', #14893, #14747, #6495, .T. ) ;
#12192=CARTESIAN_POINT ( 'NONE',  ( 0.8740779401507015045, 14.27348745891557158, -0.8420120399581809689 ) ) ;
#12194=CARTESIAN_POINT ( 'NONE',  ( 0.000000000000000000, 1.805416924949539152E-15, 13.42403576283810906 ) ) ;
#12197=CARTESIAN_POINT ( 'NONE',  ( 2.123976203522053741, -6.261444813538457943, -14.31368049382976260 ) ) ;
#12198=CARTESIAN_POINT ( 'NONE',  ( 0.4385251269669950824, 0.7363879510387324467, -13.84299131624728751 ) ) ;
#12200=CARTESIAN_POINT ( 'NONE',  ( 0.3137051932979757485, 7.698472063774634222, -11.37800749014122736 ) ) ;
#12201=LINE ( 'NONE', #3289, #3877 ) ;
#12202=CARTESIAN_POINT ( 'NONE',  ( 2.747332970342022840, -14.49942876448586482, -7.555624153089806505 ) ) ;
#12203=VECTOR ( 'NONE', #5837, 1000.000000000000114 ) ;
#12207=ORIENTED_EDGE ( 'NONE', *, *, #8715, .T. ) ;
#12209=CARTESIAN_POINT ( 'NONE',  ( 0.3308579732647025651, -13.74211098745268522, -0.5950689966505779971 ) ) ;
#12218=CARTESIAN_POINT ( 'NONE',  ( 8.438534575730034959, 5.688336279099100778, -3.845978796785973763 ) ) ;
#12219=CARTESIAN_POINT ( 'NONE',  ( 0.4862570985993235340, 12.97920246947886191, -5.003653737315353567 ) ) ;
#12222=EDGE_CURVE ( 'NONE', #4080, #11214, #11706, .T. ) ;
#12228=CARTESIAN_POINT ( 'NONE',  ( 0.4862570985993235340, 3.580942890621860109, -13.44146924561377254 ) ) ;
#12229=CARTESIAN_POINT ( 'NONE',  ( 1.846955891736113298, -7.525208385419886348, -9.909315188408124087 ) ) ;
#12236=CARTESIAN_POINT ( 'NONE',  ( 0.3145729642390426295, 13.15786090015083687, 3.952965287571154729 ) ) ;
#12238=ADVANCED_FACE ( 'NONE', ( #12376 ), #1884, .F. ) ;
#12242=CARTESIAN_POINT ( 'NONE',  ( 3.950837973638676281, 14.31366178983253512, 2.591948120961855118 ) ) ;
#12255=CARTESIAN_POINT ( 'NONE',  ( 1.977228804422059394, -15.33060379559095310, 1.488378900182341091 ) ) ;
#12266=CARTESIAN_POINT ( 'NONE',  ( 1.959283090834842200, -11.71721539537258394, 4.509128209890929107 ) ) ;
#12273=CARTESIAN_POINT ( 'NONE',  ( 2.636624412715137922, 2.161493821597615828, 15.91454522070216093 ) ) ;
#12274=FACE_BOUND ( 'NONE', #2676, .T. ) ;
#12279=CARTESIAN_POINT ( 'NONE',  ( 2.123976203522053297, 6.261444813538757259, -14.31368049382962937 ) ) ;
#12282=CARTESIAN_POINT ( 'NONE',  ( 0.3150686449036038117, 8.199336701264542171, 11.02450593298021175 ) ) ;
#12285=EDGE_CURVE ( 'NONE', #17303, #4602, #12616, .T. ) ;
#12286=EDGE_CURVE ( 'NONE', #3873, #14201, #14359, .T. ) ;
#12288=VERTEX_POINT ( 'NONE', #5649 ) ;
#12293=B_SPLINE_CURVE_WITH_KNOTS ( 'NONE', 3,
 ( #10484, #6092, #7727, #13536 ),
 .UNSPECIFIED., .F., .F.,
 ( 4, 4 ),
 ( 1.182319362138779820E-16, 0.002004993803842621859 ),
 .UNSPECIFIED. ) ;
#12295=( BOUNDED_SURFACE ( )  B_SPLINE_SURFACE ( 3, 1, ( 
 ( #18324, #16718 ),
 ( #3617, #9451 ),
 ( #12494, #9720 ),
 ( #5231, #15275 ) ),
 .UNSPECIFIED., .F., .F., .T. ) 
 B_SPLINE_SURFACE_WITH_KNOTS ( ( 4, 4 ),
 ( 2, 2 ),
 ( 0.000000000000000000, 1.000000000000000000 ),
 ( 0.000000000000000000, 1.000000000000000000 ),
 .UNSPECIFIED. ) 
 GEOMETRIC_REPRESENTATION_ITEM ( )  RATIONAL_B_SPLINE_SURFACE ( (
 ( 1.000000000000000000, 1.000000000000000000),
 ( 0.7792777138730160313, 0.9689936506012927220),
 ( 0.7792777138730160313, 0.9689936506012927220),
 ( 1.000000000000000000, 1.000000000000000000) ) ) 
 REPRESENTATION_ITEM ( '' )  SURFACE ( )  );
#12298=CARTESIAN_POINT ( 'NONE',  ( 0.3137051932979792457, 4.679953077377670745, -12.91601973349265720 ) ) ;
#12310=VERTEX_POINT ( 'NONE', #18750 ) ;
#12314=FACE_OUTER_BOUND ( 'NONE', #8365, .T. ) ;
#12315=CARTESIAN_POINT ( 'NONE',  ( 1.847034903785819360, -7.126331315909195219, -10.19974412751572679 ) ) ;
#12318=ORIENTED_EDGE ( 'NONE', *, *, #12615, .F. ) ;
#12321=DIRECTION ( 'NONE',  ( 0.7561779333270775005, 0.6534392409364817578, 0.03481510524965471948 ) ) ;
#12326=CARTESIAN_POINT ( 'NONE',  ( 0.3142014840576502488, 13.17932813834300099, -3.879477880151306568 ) ) ;
#12334=CARTESIAN_POINT ( 'NONE',  ( 0.4754618798421162973, 11.68486377711966817, 7.564402563418513026 ) ) ;
#12336=EDGE_CURVE ( 'NONE', #8092, #1784, #3019, .T. ) ;
#12346=CARTESIAN_POINT ( 'NONE',  ( 16.56872352241294521, 0.01027347319884366721, 0.001821578298043820656 ) ) ;
#12350=B_SPLINE_CURVE_WITH_KNOTS ( 'NONE', 3,
 ( #9154, #16795, #13823, #739, #6669, #18315 ),
 .UNSPECIFIED., .F., .F.,
 ( 4, 2, 4 ),
 ( 2.462833906345087556E-18, 0.0001828790815886951863, 0.0003657581631773856022 ),
 .UNSPECIFIED. ) ;
#12351=VERTEX_POINT ( 'NONE', #9962 ) ;
#12352=CARTESIAN_POINT ( 'NONE',  ( 0.3145734862173208413, -10.93207848441427643, -8.321353293018953323 ) ) ;
#12354=ORIENTED_EDGE ( 'NONE', *, *, #2024, .T. ) ;
#12356=ORIENTED_EDGE ( 'NONE', *, *, #14050, .F. ) ;
#12362=ADVANCED_FACE ( 'NONE', ( #12924 ), #5900, .T. ) ;
#12364=DIRECTION ( 'NONE',  ( -1.000000000000000000, 0.000000000000000000, -0.000000000000000000 ) ) ;
#12368=B_SPLINE_CURVE_WITH_KNOTS ( 'NONE', 3,
 ( #11847, #2936, #1233, #3028, #15757, #7073, #13176 ),
 .UNSPECIFIED., .F., .F.,
 ( 4, 3, 4 ),
 ( 1.951563910473907981E-18, 0.0002299804304191482840, 0.0004168119862248656667 ),
 .UNSPECIFIED. ) ;
#12369=CARTESIAN_POINT ( 'NONE',  ( 16.56822296793089322, 0.008619100080559776930, 0.005339139727952691740 ) ) ;
#12374=CARTESIAN_POINT ( 'NONE',  ( 1.918918678667043576, 3.258447776120001915, -12.08296592096904298 ) ) ;
#12376=FACE_OUTER_BOUND ( 'NONE', #11646, .T. ) ;
#12378=CARTESIAN_POINT ( 'NONE',  ( 2.636624412715137034, -11.60464335004055947, 11.10302021257951743 ) ) ;
#12380=ORIENTED_EDGE ( 'NONE', *, *, #12807, .F. ) ;
#12381=ORIENTED_EDGE ( 'NONE', *, *, #7039, .T. ) ;
#12382=ORIENTED_EDGE ( 'NONE', *, *, #10331, .T. ) ;
#12385=CARTESIAN_POINT ( 'NONE',  ( 1.861706995891668104, -9.751699138048492088, 7.751853334747282886 ) ) ;
#12388=ORIENTED_EDGE ( 'NONE', *, *, #15101, .F. ) ;
#12392=CARTESIAN_POINT ( 'NONE',  ( 0.3939875929385628361, 12.90850834464107244, -4.930599594904421679 ) ) ;
#12399=ORIENTED_EDGE ( 'NONE', *, *, #16832, .T. ) ;
#12412=EDGE_CURVE ( 'NONE', #473, #8092, #13297, .T. ) ;
#12417=CARTESIAN_POINT ( 'NONE',  ( 1.254255976358044311, -7.789651112956927470, -12.44256109021856105 ) ) ;
#12427=ORIENTED_EDGE ( 'NONE', *, *, #13250, .T. ) ;
#12428=CARTESIAN_POINT ( 'NONE',  ( 2.123976203522053297, -14.31368049382965069, -6.261444813538707521 ) ) ;
#12431=ORIENTED_EDGE ( 'NONE', *, *, #513, .T. ) ;
#12432=CARTESIAN_POINT ( 'NONE',  ( 1.861706995891666550, -4.359009869687166194, -11.66987142852988946 ) ) ;
#12435=CARTESIAN_POINT ( 'NONE',  ( 1.847168016377985333, -7.161712042621529939, 10.17509564929255994 ) ) ;
#12436=CARTESIAN_POINT ( 'NONE',  ( 2.636624412716062071, -14.14563173255412742, -7.605649742760987486 ) ) ;
#12440=ADVANCED_FACE ( 'NONE', ( #24 ), #12856, .F. ) ;
#12441=CARTESIAN_POINT ( 'NONE',  ( 16.57210152137263393, 0.008007331252332874558, 0.01214401161737521141 ) ) ;
#12442=CARTESIAN_POINT ( 'NONE',  ( 0.3058872367615230181, 0.6080468242580958638, 13.72992299905060243 ) ) ;
#12448=LINE ( 'NONE', #12532, #12133 ) ;
#12451=ORIENTED_EDGE ( 'NONE', *, *, #10626, .F. ) ;
#12458=ADVANCED_FACE ( 'NONE', ( #8626 ), #4594, .F. ) ;
#12462=EDGE_CURVE ( 'NONE', #6128, #13196, #5531, .T. ) ;
#12463=CARTESIAN_POINT ( 'NONE',  ( 1.846822687350019088, 7.075150813727119292, 10.23524390843941845 ) ) ;
#12466=CARTESIAN_POINT ( 'NONE',  ( 16.56753206892534891, 0.009369540855502130061, 0.001549402974393180796 ) ) ;
#12472=ORIENTED_EDGE ( 'NONE', *, *, #10324, .T. ) ;
#12475=CARTESIAN_POINT ( 'NONE',  ( 1.845756295923361323, -9.776763338604659737, 7.694561132136919390 ) ) ;
#12480=CARTESIAN_POINT ( 'NONE',  ( 0.3132642857406558456, 10.79548167658034608, 8.495623922778108295 ) ) ;
#12494=CARTESIAN_POINT ( 'NONE',  ( 16.57778382496167424, 0.01018821665058833661, 0.01092721432669112661 ) ) ;
#12496=CARTESIAN_POINT ( 'NONE',  ( 1.846138399168762101, -6.971848976710933954, -10.30487220521577818 ) ) ;
#12498=CARTESIAN_POINT ( 'NONE',  ( 16.56753206892534891, 0.001421777558675943985, -0.009389754735542252262 ) ) ;
#12499=EDGE_LOOP ( 'NONE', ( #5477, #13454, #8113, #13709 ) ) ;
#12501=CARTESIAN_POINT ( 'NONE',  ( 1.847380140988742703, -11.86779270755355853, -3.740232970470879881 ) ) ;
#12503=CARTESIAN_POINT ( 'NONE',  ( 3.950837973638675393, 2.591948120961804936, 14.31366178983254578 ) ) ;
#12506=CARTESIAN_POINT ( 'NONE',  ( 3.950837973638676281, 10.05648675950141602, -10.51028938476206953 ) ) ;
#12511=CARTESIAN_POINT ( 'NONE',  ( 0.3095370825347233956, 8.444334731364008917, 10.84046130709061373 ) ) ;
#12516=CARTESIAN_POINT ( 'NONE',  ( 3.377929128793386138, 13.92579934231094718, -1.296196549818984911 ) ) ;
#12521=CARTESIAN_POINT ( 'NONE',  ( 2.002547531651519996, -10.57595306287296921, 6.845637710436153434 ) ) ;
#12523=ADVANCED_FACE ( 'NONE', ( #1945 ), #8959, .F. ) ;
#12526=CARTESIAN_POINT ( 'NONE',  ( 2.320521194583478941, 3.126729093671432480, -15.43440938317170641 ) ) ;
#12529=VERTEX_POINT ( 'NONE', #16655 ) ;
#12532=CARTESIAN_POINT ( 'NONE',  ( 2.636624412714236865, 0.000000000000000000, -16.06066017081991149 ) ) ;
#12533=CARTESIAN_POINT ( 'NONE',  ( 2.636624412714292376, 11.60464335004048309, 11.10302021257707850 ) ) ;
#12535=EDGE_LOOP ( 'NONE', ( #18662, #7627, #13029, #13121 ) ) ;
#12537=DIRECTION ( 'NONE',  ( 0.7561779333270775005, 0.6322161072786955938, -0.1688126975276531827 ) ) ;
#12541=ORIENTED_EDGE ( 'NONE', *, *, #2600, .T. ) ;
#12542=CARTESIAN_POINT ( 'NONE',  ( 1.918918678667071775, -0.6348738215464356793, -12.49849921341423986 ) ) ;
#12543=CARTESIAN_POINT ( 'NONE',  ( 2.002547531651519996, 6.845637710436341727, -10.57595306287284842 ) ) ;
#12544=VECTOR ( 'NONE', #16699, 1000.000000000000114 ) ;
#12549=B_SPLINE_CURVE_WITH_KNOTS ( 'NONE', 3,
 ( #10667, #16498, #5014, #3286, #3485, #14955 ),
 .UNSPECIFIED., .F., .F.,
 ( 4, 2, 4 ),
 ( 0.000000000000000000, 0.001500839035891548753, 0.003001678071783097507 ),
 .UNSPECIFIED. ) ;
#12551=SHAPE_DEFINITION_REPRESENTATION ( #7225, #18049 ) ;
#12553=CARTESIAN_POINT ( 'NONE',  ( 0.3142011359265348691, -12.94258167753015520, 4.608101617236726177 ) ) ;
#12562=EDGE_LOOP ( 'NONE', ( #11144, #8041, #7304, #11289 ) ) ;
#12564=CARTESIAN_POINT ( 'NONE',  ( 1.846138399168762101, -9.815003036200465658, 7.646096044339859787 ) ) ;
#12568=CARTESIAN_POINT ( 'NONE',  ( 1.977228804422057840, -7.806978995470733373, 13.27756617201263545 ) ) ;
#12578=ORIENTED_EDGE ( 'NONE', *, *, #12286, .F. ) ;
#12579=( BOUNDED_SURFACE ( )  B_SPLINE_SURFACE ( 3, 1, ( 
 ( #14719, #10332 ),
 ( #11863, #16161 ),
 ( #1731, #12157 ),
 ( #15110, #10720 ) ),
 .UNSPECIFIED., .F., .F., .T. ) 
 B_SPLINE_SURFACE_WITH_KNOTS ( ( 4, 4 ),
 ( 2, 2 ),
 ( 0.000000000000000000, 1.000000000000000000 ),
 ( 0.000000000000000000, 1.000000000000000000 ),
 .UNSPECIFIED. ) 
 GEOMETRIC_REPRESENTATION_ITEM ( )  RATIONAL_B_SPLINE_SURFACE ( (
 ( 1.000000000000000000, 1.000000000000000000),
 ( 0.9933953342250436691, 0.8357391271907733676),
 ( 0.9933953342250436691, 0.8357391271907733676),
 ( 1.000000000000000000, 1.000000000000000000) ) ) 
 REPRESENTATION_ITEM ( '' )  SURFACE ( )  );
#12580=CARTESIAN_POINT ( 'NONE',  ( 2.747332970342022840, 11.45495994260717865, 11.66639548242811486 ) ) ;
#12585=VERTEX_POINT ( 'NONE', #413 ) ;
#12588=CARTESIAN_POINT ( 'NONE',  ( 0.8740764193766107359, 7.708542792189345683, 12.04241474977975557 ) ) ;
#12593=ADVANCED_FACE ( 'NONE', ( #9199 ), #1249, .F. ) ;
#12599=VERTEX_POINT ( 'NONE', #18449 ) ;
#12600=DIRECTION ( 'NONE',  ( -1.000000000000000000, -0.000000000000000000, -0.000000000000000000 ) ) ;
#12608=CARTESIAN_POINT ( 'NONE',  ( 1.977436885027552549, 15.04044112860454518, -3.321781585407754811 ) ) ;
#12609=CARTESIAN_POINT ( 'NONE',  ( 0.3137051932979809665, -13.20008686438108647, 3.805684345189735307 ) ) ;
#12613=ADVANCED_FACE ( 'NONE', ( #3739 ), #11042, .F. ) ;
#12615=EDGE_CURVE ( 'NONE', #16044, #2096, #18358, .T. ) ;
#12616=CIRCLE ( 'NONE', #14142, 14.54644660717763927 ) ;
#12617=CARTESIAN_POINT ( 'NONE',  ( 16.57210152137263393, -0.0006600038696347039187, 0.01453130299868522074 ) ) ;
#12623=CARTESIAN_POINT ( 'NONE',  ( 0.3148213771069355293, -4.026433757158891957, -13.13560149728604998 ) ) ;
#12625=CARTESIAN_POINT ( 'NONE',  ( 8.438534575730034959, 6.454982381540289360, 2.341351102130301065 ) ) ;
#12627=ORIENTED_EDGE ( 'NONE', *, *, #15837, .F. ) ;
#12639=DIRECTION ( 'NONE',  ( 0.000000000000000000, 0.000000000000000000, 1.000000000000000000 ) ) ;
#12644=CARTESIAN_POINT ( 'NONE',  ( 16.56782317627811096, 0.009439921864426886397, -0.002708056627498675335 ) ) ;
#12646=CARTESIAN_POINT ( 'NONE',  ( 1.847380140988742925, 3.949801494731767892, 11.79969976631073081 ) ) ;
#12652=ORIENTED_EDGE ( 'NONE', *, *, #13309, .F. ) ;
#12656=ORIENTED_EDGE ( 'NONE', *, *, #5609, .F. ) ;
#12657=ORIENTED_EDGE ( 'NONE', *, *, #14548, .T. ) ;
#12662=CARTESIAN_POINT ( 'NONE',  ( 3.074695600507753479, -6.754521329825609932, -14.01296402267891317 ) ) ;
#12667=B_SPLINE_CURVE_WITH_KNOTS ( 'NONE', 3,
 ( #14067, #16660, #10837, #16843, #9489, #10939 ),
 .UNSPECIFIED., .F., .F.,
 ( 4, 2, 4 ),
 ( 8.673617379884035472E-19, 0.0001828790815886931534, 0.0003657581631773854395 ),
 .UNSPECIFIED. ) ;
#12672=ORIENTED_EDGE ( 'NONE', *, *, #6224, .F. ) ;
#12677=DIRECTION ( 'NONE',  ( 0.000000000000000000, 0.000000000000000000, 1.000000000000000000 ) ) ;
#12678=EDGE_CURVE ( 'NONE', #3393, #5038, #6928, .T. ) ;
#12680=FACE_OUTER_BOUND ( 'NONE', #13693, .T. ) ;
#12693=CARTESIAN_POINT ( 'NONE',  ( 8.522092701127531811, -6.946128462138598358, 0.3779863304870977325 ) ) ;
#12701=EDGE_LOOP ( 'NONE', ( #16887, #4249, #11602, #13509 ) ) ;
#12705=FACE_OUTER_BOUND ( 'NONE', #9230, .T. ) ;
#12706=ORIENTED_EDGE ( 'NONE', *, *, #5134, .F. ) ;
#12707=CARTESIAN_POINT ( 'NONE',  ( 1.847247051441596621, -7.448813758297236909, 9.967131402978164800 ) ) ;
#12716=CARTESIAN_POINT ( 'NONE',  ( 16.56872352241294521, 0.009207754980063749192, 0.004907101719994666836 ) ) ;
#12719=DIRECTION ( 'NONE',  ( -0.7561779333270775005, -0.6322161072786931513, -0.1688126975276622865 ) ) ;
#12726=EDGE_CURVE ( 'NONE', #10356, #14041, #6007, .T. ) ;
#12735=CARTESIAN_POINT ( 'NONE',  ( 0.4862570985993235340, -10.79774104611379215, 8.769551628660700260 ) ) ;
#12736=CARTESIAN_POINT ( 'NONE',  ( 8.438534575730034959, -1.899950616255142277, -6.598402093327899287 ) ) ;
#12739=CARTESIAN_POINT ( 'NONE',  ( 0.3939875929385656117, -13.34133634968952720, -3.598491969338368346 ) ) ;
#12740=CARTESIAN_POINT ( 'NONE',  ( 0.3142014840576517476, -13.17932813834297434, 3.879477880151391833 ) ) ;
#12746=CARTESIAN_POINT ( 'NONE',  ( 2.636624412717140764, -2.862162146982851763, -15.80357026013259514 ) ) ;
#12755=CARTESIAN_POINT ( 'NONE',  ( 1.847034903785818694, -9.929438108952092890, -7.498375632854726192 ) ) ;
#12757=CARTESIAN_POINT ( 'NONE',  ( 1.861628059977344263, 6.879051339207292948, 10.38573835516714716 ) ) ;
#12762=B_SPLINE_CURVE_WITH_KNOTS ( 'NONE', 3,
 ( #13348, #1887, #9236, #260, #4655, #17847 ),
 .UNSPECIFIED., .F., .F.,
 ( 4, 2, 4 ),
 ( 8.673617379884035472E-19, 0.001500839035891551572, 0.003001678071783102277 ),
 .UNSPECIFIED. ) ;
#12763=CARTESIAN_POINT ( 'NONE',  ( 16.57210152137263393, -0.009075239946108286035, 0.01136813053532071717 ) ) ;
#12764=CARTESIAN_POINT ( 'NONE',  ( 1.959283090834855745, -12.53713130127478337, 0.6676170829051779609 ) ) ;
#12768=ORIENTED_EDGE ( 'NONE', *, *, #8846, .T. ) ;
#12770=CARTESIAN_POINT ( 'NONE',  ( 16.56822296793089322, -0.009847136207496290372, -0.002414375228568220195 ) ) ;
#12772=DIRECTION ( 'NONE',  ( 0.000000000000000000, 0.000000000000000000, 1.000000000000000000 ) ) ;
#12774=EDGE_CURVE ( 'NONE', #6674, #12889, #11954, .T. ) ;
#12776=CARTESIAN_POINT ( 'NONE',  ( 0.4754618798421162973, 8.775436892861270266, -10.80499583390503382 ) ) ;
#12782=CARTESIAN_POINT ( 'NONE',  ( 1.846138399168762101, -3.446241763652916124, -11.95493567637853971 ) ) ;
#12785=ORIENTED_EDGE ( 'NONE', *, *, #926, .T. ) ;
#12787=ORIENTED_EDGE ( 'NONE', *, *, #13966, .F. ) ;
#12788=CARTESIAN_POINT ( 'NONE',  ( 2.747332970342022840, -14.63517873738941866, -7.289199830147261139 ) ) ;
#12790=EDGE_CURVE ( 'NONE', #18142, #5568, #5096, .T. ) ;
#12792=VERTEX_POINT ( 'NONE', #11859 ) ;
#12797=CARTESIAN_POINT ( 'NONE',  ( 2.747332970342022840, 16.12459247543629814, -2.705255688517677282 ) ) ;
#12798=B_SPLINE_CURVE_WITH_KNOTS ( 'NONE', 3,
 ( #16822, #3914, #3724, #8227 ),
 .UNSPECIFIED., .F., .F.,
 ( 4, 4 ),
 ( 5.210130127421859526E-17, 0.002004993803842660023 ),
 .UNSPECIFIED. ) ;
#12807=EDGE_CURVE ( 'NONE', #1302, #10558, #13763, .T. ) ;
#12808=CARTESIAN_POINT ( 'NONE',  ( 0.4754618798421171855, -12.98792082933648118, 5.007009103465197342 ) ) ;
#12809=CARTESIAN_POINT ( 'NONE',  ( 16.56782317627811096, 0.009814734722106368062, -0.0003415813796015080314 ) ) ;
#12812=CARTESIAN_POINT ( 'NONE',  ( 1.254255976357671720, -9.426444230097072108, 11.25336128106933664 ) ) ;
#12818=ORIENTED_EDGE ( 'NONE', *, *, #1914, .F. ) ;
#12824=EDGE_CURVE ( 'NONE', #9336, #5926, #5324, .T. ) ;
#12828=CARTESIAN_POINT ( 'NONE',  ( 3.074695600507268978, -2.772091048739378394, 15.30693405987788935 ) ) ;
#12830=CARTESIAN_POINT ( 'NONE',  ( 1.847034903785824023, 3.625649561595307269, 11.90269060117935496 ) ) ;
#12833=CARTESIAN_POINT ( 'NONE',  ( 0.3145729642390365788, 10.93201268464384768, -8.321438378985135387 ) ) ;
#12836=ORIENTED_EDGE ( 'NONE', *, *, #4035, .T. ) ;
#12843=DIRECTION ( 'NONE',  ( -1.000000000000000000, -0.000000000000000000, -0.000000000000000000 ) ) ;
#12856=( BOUNDED_SURFACE ( )  B_SPLINE_SURFACE ( 3, 1, ( 
 ( #17617, #1750 ),
 ( #7596, #2779 ),
 ( #11976, #1463 ),
 ( #223, #16178 ) ),
 .UNSPECIFIED., .F., .F., .T. ) 
 B_SPLINE_SURFACE_WITH_KNOTS ( ( 4, 4 ),
 ( 2, 2 ),
 ( 0.000000000000000000, 1.000000000000000000 ),
 ( 0.000000000000000000, 1.000000000000000000 ),
 .UNSPECIFIED. ) 
 GEOMETRIC_REPRESENTATION_ITEM ( )  RATIONAL_B_SPLINE_SURFACE ( (
 ( 1.000000000000000000, 1.000000000000000000),
 ( 0.9933953342250438912, 0.8357391271907739227),
 ( 0.9933953342250438912, 0.8357391271907739227),
 ( 1.000000000000000000, 1.000000000000000000) ) ) 
 REPRESENTATION_ITEM ( '' )  SURFACE ( )  );
#12860=CARTESIAN_POINT ( 'NONE',  ( 1.847380140988742925, 3.740232970470921625, -11.86779270755354432 ) ) ;
#12862=CARTESIAN_POINT ( 'NONE',  ( 0.3720661004400037664, -13.34435358167255181, 3.575426119359132571 ) ) ;
#12864=VERTEX_POINT ( 'NONE', #16357 ) ;
#12870=CARTESIAN_POINT ( 'NONE',  ( 0.4862570985993252548, -12.97920246947875889, -5.003653737315625349 ) ) ;
#12873=EDGE_CURVE ( 'NONE', #5602, #12106, #10099, .T. ) ;
#12874=CARTESIAN_POINT ( 'NONE',  ( 3.950837973638675393, -2.591948120961912849, 14.31366178983252446 ) ) ;
#12875=ORIENTED_EDGE ( 'NONE', *, *, #4504, .T. ) ;
#12876=EDGE_CURVE ( 'NONE', #8134, #6766, #8748, .T. ) ;
#12877=VERTEX_POINT ( 'NONE', #12052 ) ;
#12878=CARTESIAN_POINT ( 'NONE',  ( 0.3170788640506441158, -13.74111462631963576, 0.1533108587035682813 ) ) ;
#12879=FACE_OUTER_BOUND ( 'NONE', #6116, .T. ) ;
#12882=CARTESIAN_POINT ( 'NONE',  ( 1.847034903785822690, -0.2299360331935046409, 12.44051878787773013 ) ) ;
#12889=VERTEX_POINT ( 'NONE', #13158 ) ;
#12890=CARTESIAN_POINT ( 'NONE',  ( 2.353870697619111940, 6.980654702310842730, 10.90705766126222187 ) ) ;
#12895=( BOUNDED_SURFACE ( )  B_SPLINE_SURFACE ( 3, 1, ( 
 ( #7771, #2125 ),
 ( #13687, #9099 ),
 ( #15017, #17898 ),
 ( #6428, #6140 ) ),
 .UNSPECIFIED., .F., .F., .T. ) 
 B_SPLINE_SURFACE_WITH_KNOTS ( ( 4, 4 ),
 ( 2, 2 ),
 ( 0.000000000000000000, 1.000000000000000000 ),
 ( 0.000000000000000000, 1.000000000000000000 ),
 .UNSPECIFIED. ) 
 GEOMETRIC_REPRESENTATION_ITEM ( )  RATIONAL_B_SPLINE_SURFACE ( (
 ( 1.000000000000000000, 1.000000000000000000),
 ( 0.9933953342250438912, 0.8357391271907739227),
 ( 0.9933953342250438912, 0.8357391271907739227),
 ( 1.000000000000000000, 1.000000000000000000) ) ) 
 REPRESENTATION_ITEM ( '' )  SURFACE ( )  );
#12896=CARTESIAN_POINT ( 'NONE',  ( 0.3142014840576535795, -12.94260032291125562, -4.608051180497059640 ) ) ;
#12900=LINE ( 'NONE', #1533, #8058 ) ;
#12902=B_SPLINE_CURVE_WITH_KNOTS ( 'NONE', 3,
 ( #11744, #5704, #14795, #7452 ),
 .UNSPECIFIED., .F., .F.,
 ( 4, 4 ),
 ( 2.851299179213411365E-16, 0.002004993803842618823 ),
 .UNSPECIFIED. ) ;
#12905=LINE ( 'NONE', #1154, #4804 ) ;
#12910=CARTESIAN_POINT ( 'NONE',  ( 0.3137051932979775248, 3.805684345189972895, -13.20008686438101719 ) ) ;
#12917=CARTESIAN_POINT ( 'NONE',  ( 0.3058872367615226295, -13.72992299905059355, -0.6080468242582393046 ) ) ;
#12924=FACE_OUTER_BOUND ( 'NONE', #5800, .T. ) ;
#12925=CARTESIAN_POINT ( 'NONE',  ( 16.56753206892534891, -0.009389754735541561842, 0.001421777558676752366 ) ) ;
#12928=CARTESIAN_POINT ( 'NONE',  ( 3.950837973638668288, 0.000000000000000000, 0.000000000000000000 ) ) ;
#12940=DIRECTION ( 'NONE',  ( -1.000000000000000000, 0.000000000000000000, 0.000000000000000000 ) ) ;
#12945=CARTESIAN_POINT ( 'NONE',  ( 8.438534575730034959, 5.415535776177522465, 4.221456476902686106 ) ) ;
#12946=CARTESIAN_POINT ( 'NONE',  ( 2.747332970342022840, 2.409922051470906990, -16.17136872824896443 ) ) ;
#12949=ORIENTED_EDGE ( 'NONE', *, *, #9989, .T. ) ;
#12950=ORIENTED_EDGE ( 'NONE', *, *, #4931, .T. ) ;
#12954=EDGE_CURVE ( 'NONE', #17449, #6674, #5751, .T. ) ;
#12957=CARTESIAN_POINT ( 'NONE',  ( 16.56753206892534891, -0.009389754735542259201, -0.001421777558675912110 ) ) ;
#12961=CARTESIAN_POINT ( 'NONE',  ( 8.438534575730034959, -6.598402093327893958, 1.899950616255162483 ) ) ;
#12963=CARTESIAN_POINT ( 'NONE',  ( 0.4862570985993235340, -0.7479633556561480212, -13.89016912371018186 ) ) ;
#12971=VECTOR ( 'NONE', #6781, 1000.000000000000000 ) ;
#12972=ORIENTED_EDGE ( 'NONE', *, *, #7643, .T. ) ;
#12974=ORIENTED_EDGE ( 'NONE', *, *, #10784, .T. ) ;
#12976=B_SPLINE_CURVE_WITH_KNOTS ( 'NONE', 3,
 ( #4063, #12662, #5305, #9787 ),
 .UNSPECIFIED., .F., .F.,
 ( 4, 4 ),
 ( 2.298835888684693015E-16, 0.002004993803842571552 ),
 .UNSPECIFIED. ) ;
#12978=ORIENTED_EDGE ( 'NONE', *, *, #18076, .F. ) ;
#12981=CARTESIAN_POINT ( 'NONE',  ( 1.847168016377983335, 11.89018175117595177, 3.666915430942639720 ) ) ;
#12985=CARTESIAN_POINT ( 'NONE',  ( 1.846138399168762101, -10.30487220521565028, -6.971848976711123136 ) ) ;
#12988=CARTESIAN_POINT ( 'NONE',  ( 0.3151930723728408879, -13.04315954105012310, -4.318364831037728280 ) ) ;
#12998=CARTESIAN_POINT ( 'NONE',  ( 0.3145729642390366343, 7.825496023201474749, -11.29233589755984113 ) ) ;
#13002=VERTEX_POINT ( 'NONE', #7346 ) ;
#13004=CARTESIAN_POINT ( 'NONE',  ( 0.4754618798421171855, 13.89949764182682657, -0.7484603771384882309 ) ) ;
#13006=CARTESIAN_POINT ( 'NONE',  ( 1.846138399168762101, -6.971848976711082280, 10.30487220521567693 ) ) ;
#13007=CARTESIAN_POINT ( 'NONE',  ( 1.977228804422057840, -3.321884655132009811, 15.04020501276143662 ) ) ;
#13008=ADVANCED_FACE ( 'NONE', ( #69 ), #16162, .F. ) ;
#13010=CARTESIAN_POINT ( 'NONE',  ( 0.3151926232592480726, -0.07678256780548071980, -13.73922722301401578 ) ) ;
#13011=CARTESIAN_POINT ( 'NONE',  ( 0.3720661004400037664, -13.79610186261029270, -0.7231997263366251039 ) ) ;
#13013=CONICAL_SURFACE ( 'NONE', #4790, 14.54644660717763927, 0.8559913436420816257 ) ;
#13015=B_SPLINE_CURVE_WITH_KNOTS ( 'NONE', 3,
 ( #13960, #9285, #961, #3643, #3551, #7968 ),
 .UNSPECIFIED., .F., .F.,
 ( 4, 2, 4 ),
 ( 3.897476843869763523E-18, 0.0002017457492448077711, 0.0004034914984896116391 ),
 .UNSPECIFIED. ) ;
#13020=CARTESIAN_POINT ( 'NONE',  ( 16.56782317627811096, 0.006045301465876630996, 0.007739510688078455984 ) ) ;
#13022=CARTESIAN_POINT ( 'NONE',  ( 0.3132642857406501835, 7.641821025099867271, 11.41580579227779779 ) ) ;
#13029=ORIENTED_EDGE ( 'NONE', *, *, #5310, .T. ) ;
#13031=VERTEX_POINT ( 'NONE', #14497 ) ;
#13033=EDGE_CURVE ( 'NONE', #6505, #10137, #9661, .T. ) ;
#13034=ORIENTED_EDGE ( 'NONE', *, *, #13873, .F. ) ;
#13040=CARTESIAN_POINT ( 'NONE',  ( 0.8740764193771586310, 12.04241474978035420, -7.708542792189425619 ) ) ;
#13042=CARTESIAN_POINT ( 'NONE',  ( 1.847426409206450959, 1.966388007708274189E-11, -12.44303504652081038 ) ) ;
#13044=CARTESIAN_POINT ( 'NONE',  ( 16.56753206892534891, 0.009389754735541551434, -0.001421777558676823056 ) ) ;
#13045=CARTESIAN_POINT ( 'NONE',  ( 2.636624412715137922, -7.605649742761668719, 14.14563173255331741 ) ) ;
#13046=EDGE_CURVE ( 'NONE', #18257, #10202, #8512, .T. ) ;
#13047=ORIENTED_EDGE ( 'NONE', *, *, #3811, .F. ) ;
#13051=VERTEX_POINT ( 'NONE', #14684 ) ;
#13055=CARTESIAN_POINT ( 'NONE',  ( 2.636624412714763555, 6.973567714907159321, 14.46769361191226722 ) ) ;
#13062=CARTESIAN_POINT ( 'NONE',  ( 1.254009781011994340, -1.011465182608154434, -14.64464726212624690 ) ) ;
#13065=CARTESIAN_POINT ( 'NONE',  ( 8.438534575730034959, 6.862570336891075762, -0.2320579683290367456 ) ) ;
#13067=ADVANCED_FACE ( 'NONE', ( #13251 ), #11642, .F. ) ;
#13069=B_SPLINE_CURVE_WITH_KNOTS ( 'NONE', 3,
 ( #1776, #8751, #14866, #1491 ),
 .UNSPECIFIED., .F., .F.,
 ( 4, 4 ),
 ( 0.000000000000000000, 0.002004993803842287058 ),
 .UNSPECIFIED. ) ;
#13074=CARTESIAN_POINT ( 'NONE',  ( 2.002547531651519996, 12.57989064830759496, 0.6781519942172178350 ) ) ;
#13077=B_SPLINE_CURVE_WITH_KNOTS ( 'NONE', 3,
 ( #1740, #13486, #6232, #10636 ),
 .UNSPECIFIED., .F., .F.,
 ( 4, 4 ),
 ( 1.330347433792404293E-17, 0.003005512676784847462 ),
 .UNSPECIFIED. ) ;
#13081=CONICAL_SURFACE ( 'NONE', #3313, 14.54644660717763927, 0.8559913436420816257 ) ;
#13085=CARTESIAN_POINT ( 'NONE',  ( 0.3151926232592509591, -13.73922722301401400, 0.07678256780552859817 ) ) ;
#13086=CARTESIAN_POINT ( 'NONE',  ( 0.3137051932979792457, -12.91601973349266963, -4.679953077377624560 ) ) ;
#13089=CARTESIAN_POINT ( 'NONE',  ( 2.636624412715137922, -14.46769361191291559, 6.973567714907789927 ) ) ;
#13096=ORIENTED_EDGE ( 'NONE', *, *, #6275, .F. ) ;
#13102=CARTESIAN_POINT ( 'NONE',  ( 0.3720661004400040439, 3.575426119359372823, -13.34435358167249142 ) ) ;
#13107=EDGE_CURVE ( 'NONE', #6766, #666, #6187, .T. ) ;
#13108=VERTEX_POINT ( 'NONE', #6387 ) ;
#13110=CARTESIAN_POINT ( 'NONE',  ( 2.320521194582657376, -3.126729093671833937, 15.43440938317077915 ) ) ;
#13111=CARTESIAN_POINT ( 'NONE',  ( 0.4385251269669978580, 3.577373010348713134, 13.39302348765809825 ) ) ;
#13112=CARTESIAN_POINT ( 'NONE',  ( 0.3137051932979792457, -13.73004976592202375, 0.4596302728639276580 ) ) ;
#13118=CARTESIAN_POINT ( 'NONE',  ( 0.3132635586635995617, 11.41586812343490109, 7.641727604903931770 ) ) ;
#13119=CARTESIAN_POINT ( 'NONE',  ( 1.861628059977341154, -12.44564375541077084, -0.5393144007391572625 ) ) ;
#13121=ORIENTED_EDGE ( 'NONE', *, *, #18614, .T. ) ;
#13127=CARTESIAN_POINT ( 'NONE',  ( 2.747332970342022840, -16.17136872824897154, -2.409922051470850146 ) ) ;
#13128=ORIENTED_EDGE ( 'NONE', *, *, #9873, .T. ) ;
#13133=CARTESIAN_POINT ( 'NONE',  ( 0.4754618798421167414, -3.583352865732579051, -13.45049478164063217 ) ) ;
#13139=CARTESIAN_POINT ( 'NONE',  ( 2.002547531651519996, -3.242439124566736997, 12.17374746633577232 ) ) ;
#13149=CARTESIAN_POINT ( 'NONE',  ( 1.861628059977342931, -12.00316790821103652, 3.332996951203584413 ) ) ;
#13152=ORIENTED_EDGE ( 'NONE', *, *, #16854, .F. ) ;
#13155=CARTESIAN_POINT ( 'NONE',  ( 3.074695600507182824, 6.754521329825023734, -14.01296402267889007 ) ) ;
#13158=CARTESIAN_POINT ( 'NONE',  ( 3.950837973638675393, 14.31366178983257242, -2.591948120961654833 ) ) ;
#13160=CARTESIAN_POINT ( 'NONE',  ( 1.847247051441594401, 0.1676840720647037319, -12.44188156437793680 ) ) ;
#13169=CARTESIAN_POINT ( 'NONE',  ( 16.56753206892534891, 0.006760771273035115839, -0.006669401563385219701 ) ) ;
#13170=EDGE_CURVE ( 'NONE', #4291, #12792, #16426, .T. ) ;
#13176=CARTESIAN_POINT ( 'NONE',  ( 1.847426409206450959, 1.966388007708274189E-11, -12.44303504652081038 ) ) ;
#13189=CARTESIAN_POINT ( 'NONE',  ( 0.3142014840576500267, 8.382000553815611710, -10.88517824918533883 ) ) ;
#13195=( BOUNDED_SURFACE ( )  B_SPLINE_SURFACE ( 3, 1, ( 
 ( #4707, #6234 ),
 ( #17900, #118 ),
 ( #16273, #17806 ),
 ( #11779, #10537 ) ),
 .UNSPECIFIED., .F., .F., .T. ) 
 B_SPLINE_SURFACE_WITH_KNOTS ( ( 4, 4 ),
 ( 2, 2 ),
 ( 0.000000000000000000, 1.000000000000000000 ),
 ( 0.000000000000000000, 1.000000000000000000 ),
 .UNSPECIFIED. ) 
 GEOMETRIC_REPRESENTATION_ITEM ( )  RATIONAL_B_SPLINE_SURFACE ( (
 ( 1.000000000000000000, 1.000000000000000000),
 ( 0.7792777138730158093, 0.9689936506012928330),
 ( 0.7792777138730158093, 0.9689936506012928330),
 ( 1.000000000000000000, 1.000000000000000000) ) ) 
 REPRESENTATION_ITEM ( '' )  SURFACE ( )  );
#13196=VERTEX_POINT ( 'NONE', #4855 ) ;
#13198=ADVANCED_FACE ( 'NONE', ( #12121 ), #4003, .T. ) ;
#13199=EDGE_CURVE ( 'NONE', #16036, #12529, #18759, .T. ) ;
#13201=B_SPLINE_CURVE_WITH_KNOTS ( 'NONE', 3,
 ( #9833, #11380, #5447, #15664 ),
 .UNSPECIFIED., .F., .F.,
 ( 4, 4 ),
 ( 3.750785467376078809E-16, 0.002004993803842428438 ),
 .UNSPECIFIED. ) ;
#13202=DIRECTION ( 'NONE',  ( -1.000000000000000000, -0.000000000000000000, -0.000000000000000000 ) ) ;
#13208=CARTESIAN_POINT ( 'NONE',  ( 0.4862570985993235340, 11.67702470553376060, -7.559321496869298329 ) ) ;
#13211=CARTESIAN_POINT ( 'NONE',  ( 0.3151926232592475174, -8.013596737356467159, 11.16039997398650918 ) ) ;
#13213=VERTEX_POINT ( 'NONE', #3810 ) ;
#13215=CARTESIAN_POINT ( 'NONE',  ( 16.56679352167444819, 0.006618561353599204840, -0.006526964904752983153 ) ) ;
#13218=ORIENTED_EDGE ( 'NONE', *, *, #7703, .F. ) ;
#13219=EDGE_CURVE ( 'NONE', #13213, #16036, #17430, .T. ) ;
#13223=CARTESIAN_POINT ( 'NONE',  ( 0.3132635586635977298, -0.5277914263192144961, -13.72732610560089128 ) ) ;
#13224=B_SPLINE_CURVE_WITH_KNOTS ( 'NONE', 3,
 ( #14734, #17322, #16278, #14452 ),
 .UNSPECIFIED., .F., .F.,
 ( 4, 4 ),
 ( 0.000000000000000000, 0.002004993803842618390 ),
 .UNSPECIFIED. ) ;
#13227=CARTESIAN_POINT ( 'NONE',  ( 2.636624412716902288, 7.605649742760546950, -14.14563173255513995 ) ) ;
#13230=CARTESIAN_POINT ( 'NONE',  ( 3.950837973638676281, -14.41405733518059229, -1.958075594453940971 ) ) ;
#13232=CARTESIAN_POINT ( 'NONE',  ( 0.3939822652208120890, -10.75310269629515325, -8.678192463540291612 ) ) ;
#13235=VECTOR ( 'NONE', #1236, 1000.000000000000000 ) ;
#13248=CARTESIAN_POINT ( 'NONE',  ( 1.846138399168762101, -12.43476674860266229, -0.4167076046096845898 ) ) ;
#13250=EDGE_CURVE ( 'NONE', #10871, #18854, #3257, .T. ) ;
#13251=FACE_OUTER_BOUND ( 'NONE', #7720, .T. ) ;
#13256=CARTESIAN_POINT ( 'NONE',  ( 0.3142014840576502488, -7.762239086932773091, -11.33546131209471142 ) ) ;
#13261=EDGE_CURVE ( 'NONE', #1036, #13957, #10093, .T. ) ;
#13262=VERTEX_POINT ( 'NONE', #12506 ) ;
#13263=CARTESIAN_POINT ( 'NONE',  ( 0.3058872367615230181, -3.664492643742856881, 13.24582953854924128 ) ) ;
#13264=ORIENTED_EDGE ( 'NONE', *, *, #17693, .T. ) ;
#13266=CARTESIAN_POINT ( 'NONE',  ( 0.3095370825347224519, -13.20347358821911854, -3.806662003783552350 ) ) ;
#13270=DIRECTION ( 'NONE',  ( 0.7635533937278216055, -0.02138673900302784023, 0.6453904417649385383 ) ) ;
#13281=CARTESIAN_POINT ( 'NONE',  ( 0.3095370825347224519, 4.681152801286340370, -12.91933430393602933 ) ) ;
#13283=CARTESIAN_POINT ( 'NONE',  ( 1.254255976357644409, -12.44256109021810097, 7.789651112956895496 ) ) ;
#13288=CARTESIAN_POINT ( 'NONE',  ( 16.56679352167444819, -0.006618561353599251677, 0.006526964904752932846 ) ) ;
#13289=EDGE_LOOP ( 'NONE', ( #15915, #10938, #2828, #15250 ) ) ;
#13291=CARTESIAN_POINT ( 'NONE',  ( 2.636624412714237309, 14.14563173255211126, 7.605649742762011556 ) ) ;
#13294=CONICAL_SURFACE ( 'NONE', #2302, 12.15840553252917289, 0.7853981625000049371 ) ;
#13297=B_SPLINE_CURVE_WITH_KNOTS ( 'NONE', 3,
 ( #10061, #11785, #6148, #7396, #4618, #4329 ),
 .UNSPECIFIED., .F., .F.,
 ( 4, 2, 4 ),
 ( 5.421010862427522170E-19, 0.0001825746017570577750, 0.0003651492035141150078 ),
 .UNSPECIFIED. ) ;
#13309=EDGE_CURVE ( 'NONE', #16119, #17964, #11216, .T. ) ;
#13311=CARTESIAN_POINT ( 'NONE',  ( 16.57210152137263393, 0.01361613799508855013, 0.005118120558001428358 ) ) ;
#13313=VERTEX_POINT ( 'NONE', #2018 ) ;
#13314=ORIENTED_EDGE ( 'NONE', *, *, #10100, .T. ) ;
#13319=CARTESIAN_POINT ( 'NONE',  ( 0.3720661004400037664, 13.79610186261029625, 0.7231997263365286255 ) ) ;
#13320=CARTESIAN_POINT ( 'NONE',  ( 3.950837973638668288, 0.000000000000000000, 0.000000000000000000 ) ) ;
#13321=B_SPLINE_CURVE_WITH_KNOTS ( 'NONE', 3,
 ( #888, #17123, #12542, #9679, #2406, #8258 ),
 .UNSPECIFIED., .F., .F.,
 ( 4, 2, 4 ),
 ( 5.421010862427522170E-19, 0.0001825746017570583442, 0.0003651492035141161462 ),
 .UNSPECIFIED. ) ;
#13322=CARTESIAN_POINT ( 'NONE',  ( 0.3137051932979757485, 13.73004976592202020, -0.4596302728640235258 ) ) ;
#13333=CARTESIAN_POINT ( 'NONE',  ( 0.3148213771069373057, 13.73693585713733967, 0.2297580318215192152 ) ) ;
#13337=EDGE_CURVE ( 'NONE', #13901, #3568, #3667, .T. ) ;
#13338=CARTESIAN_POINT ( 'NONE',  ( 1.846822687350018866, -11.92063725419901843, 3.566003975885642774 ) ) ;
#13339=CARTESIAN_POINT ( 'NONE',  ( 16.56679352167444819, 0.009170718284672540327, 0.001518074900130682347 ) ) ;
#13343=VERTEX_POINT ( 'NONE', #18798 ) ;
#13348=CARTESIAN_POINT ( 'NONE',  ( 2.002547531651519996, -11.75462648437098601, -4.532360870844453160 ) ) ;
#13363=EDGE_LOOP ( 'NONE', ( #17569, #7872, #3559, #18577 ) ) ;
#13368=CARTESIAN_POINT ( 'NONE',  ( 0.4384471787762819206, -11.63197976518323173, -7.540925784514680430 ) ) ;
#13372=ORIENTED_EDGE ( 'NONE', *, *, #14597, .F. ) ;
#13376=CARTESIAN_POINT ( 'NONE',  ( 1.959212340397946450, 11.71715421693498449, 4.509090217468559203 ) ) ;
#13378=CARTESIAN_POINT ( 'NONE',  ( 2.123976203522053297, 15.54801196254786966, 1.531817366691807125 ) ) ;
#13383=CARTESIAN_POINT ( 'NONE',  ( 1.254009781011619307, -11.25324419414205224, 9.426200207651413976 ) ) ;
#13389=DIRECTION ( 'NONE',  ( -1.000000000000000000, -0.000000000000000000, -0.000000000000000000 ) ) ;
#13392=ORIENTED_EDGE ( 'NONE', *, *, #15042, .F. ) ;
#13395=CARTESIAN_POINT ( 'NONE',  ( 0.4862570985993235340, -10.79774104611379215, 8.769551628660700260 ) ) ;
#13407=CARTESIAN_POINT ( 'NONE',  ( 0.3151928476913592458, -4.245457024760312947, 13.06684726503524807 ) ) ;
#13408=CARTESIAN_POINT ( 'NONE',  ( 16.56679352167444819, -0.001390132774595520624, -0.009190982326619362083 ) ) ;
#13419=CARTESIAN_POINT ( 'NONE',  ( 2.636624412714237309, 15.91454522070173638, -2.161493821596664144 ) ) ;
#13421=EDGE_CURVE ( 'NONE', #8935, #10941, #8669, .T. ) ;
#13426=CARTESIAN_POINT ( 'NONE',  ( 2.002547531651519996, 3.242439124566649511, 12.17374746633579541 ) ) ;
#13428=CARTESIAN_POINT ( 'NONE',  ( 1.846138399168762101, 6.971848976711011225, 10.30487220521572667 ) ) ;
#13431=DIRECTION ( 'NONE',  ( 0.000000000000000000, 0.000000000000000000, 1.000000000000000000 ) ) ;
#13432=ORIENTED_EDGE ( 'NONE', *, *, #13965, .T. ) ;
#13434=VERTEX_POINT ( 'NONE', #14501 ) ;
#13438=CARTESIAN_POINT ( 'NONE',  ( 2.002547531651519996, 0.6781519942173496185, -12.57989064830758785 ) ) ;
#13439=CARTESIAN_POINT ( 'NONE',  ( 0.3137051932979792457, 13.73004976592202198, 0.4596302728640249136 ) ) ;
#13443=CARTESIAN_POINT ( 'NONE',  ( 3.950837973638668288, 0.000000000000000000, 0.000000000000000000 ) ) ;
#13445=B_SPLINE_CURVE_WITH_KNOTS ( 'NONE', 3,
 ( #12091, #12192, #7509, #16298, #18018, #13419 ),
 .UNSPECIFIED., .F., .F.,
 ( 4, 2, 4 ),
 ( 0.000000000000000000, 0.001657017934709842290, 0.003314035869419685448 ),
 .UNSPECIFIED. ) ;
#13446=CARTESIAN_POINT ( 'NONE',  ( 16.56822296793089322, 0.006547366384936635295, 0.007741272030791194678 ) ) ;
#13447=CARTESIAN_POINT ( 'NONE',  ( 3.512766787570761107, 14.91422000116819468, -2.025881399556438200 ) ) ;
#13450=CARTESIAN_POINT ( 'NONE',  ( 3.950837973638675393, 14.31366178983257242, -2.591948120961654833 ) ) ;
#13453=ORIENTED_EDGE ( 'NONE', *, *, #2994, .F. ) ;
#13454=ORIENTED_EDGE ( 'NONE', *, *, #10894, .F. ) ;
#13456=ORIENTED_EDGE ( 'NONE', *, *, #10294, .F. ) ;
#13458=CARTESIAN_POINT ( 'NONE',  ( 3.950837973638675393, -10.51028938476210328, -10.05648675950137871 ) ) ;
#13459=AXIS2_PLACEMENT_3D ( 'NONE', #7730, #16522, #9244 ) ;
#13476=CARTESIAN_POINT ( 'NONE',  ( 1.562796894703937678, 0.000000000000000000, 0.000000000000000000 ) ) ;
#13477=CARTESIAN_POINT ( 'NONE',  ( 2.320521194582183977, 6.542541239684722676, 14.32454473829914399 ) ) ;
#13478=VERTEX_POINT ( 'NONE', #5892 ) ;
#13482=DIRECTION ( 'NONE',  ( -0.7635533937278214944, -0.3966532189476559833, -0.5095610256143900951 ) ) ;
#13486=CARTESIAN_POINT ( 'NONE',  ( 3.377929128793393687, 1.296196549818942501, 13.92579934231096317 ) ) ;
#13499=CARTESIAN_POINT ( 'NONE',  ( 2.705023505549862151, 8.489131503859777439, 10.24007717649583782 ) ) ;
#13500=EDGE_LOOP ( 'NONE', ( #13034, #236, #18763, #470, #8112, #10791, #3072, #12399, #7256, #8248, #13744, #16827, #16290, #15253, #8914, #5952, #2210, #3793, #18637, #2626, #12768, #638, #17481, #8987, #14947, #13547, #11165, #15111, #8184, #17681, #16362, #1188, #12176, #10912, #8698, #5739, #18213, #4945, #12427, #13707, #2140, #16479, #16185, #10183, #11343, #5410, #13314, #14537, #11259, #10872, #14873, #8652, #10327, #9323, #10549, #5274, #3943, #12354, #1104, #7628, #10423, #3024, #8202, #13096 ) ) ;
#13501=DIRECTION ( 'NONE',  ( -0.7635533937278214944, -0.6071939193889592801, 0.2197766120036439286 ) ) ;
#13503=ORIENTED_EDGE ( 'NONE', *, *, #7158, .F. ) ;
#13507=ORIENTED_EDGE ( 'NONE', *, *, #1534, .T. ) ;
#13509=ORIENTED_EDGE ( 'NONE', *, *, #7813, .T. ) ;
#13511=CARTESIAN_POINT ( 'NONE',  ( 0.3058872367615230181, -13.72992299905060598, 0.6080468242580479021 ) ) ;
#13514=CARTESIAN_POINT ( 'NONE',  ( 1.845756295923373758, 7.694561132136944259, 9.776763338604617104 ) ) ;
#13516=CARTESIAN_POINT ( 'NONE',  ( 16.56753206892534891, 0.006760771273036174887, 0.006669401563384942146 ) ) ;
#13518=CARTESIAN_POINT ( 'NONE',  ( 16.56782317627811096, -0.002708056627498708728, -0.009439921864426879458 ) ) ;
#13519=CARTESIAN_POINT ( 'NONE',  ( 0.8740764193769091639, -3.609949042658162188, -13.83508774436024957 ) ) ;
#13529=ORIENTED_EDGE ( 'NONE', *, *, #17018, .F. ) ;
#13533=CARTESIAN_POINT ( 'NONE',  ( 0.4385251269669950269, -13.84299131624728929, -0.7363879510386833749 ) ) ;
#13536=CARTESIAN_POINT ( 'NONE',  ( 3.950837973638677170, 10.51028938476232355, -10.05648675950114956 ) ) ;
#13543=CARTESIAN_POINT ( 'NONE',  ( 3.353306896162453477, -12.02594772223101494, 7.069984850384768649 ) ) ;
#13547=ORIENTED_EDGE ( 'NONE', *, *, #18076, .T. ) ;
#13557=CARTESIAN_POINT ( 'NONE',  ( 1.342453679581834924, 13.74702459364884533, 5.476372339890065000 ) ) ;
#13566=SURFACE_STYLE_FILL_AREA ( #7663 ) ;
#13569=VECTOR ( 'NONE', #8522, 1000.000000000000000 ) ;
#13570=CARTESIAN_POINT ( 'NONE',  ( 1.846613052777651420, 11.72395935470504291, -4.166957398589727468 ) ) ;
#13572=CARTESIAN_POINT ( 'NONE',  ( 2.002547531651519996, -12.57989064830760206, 0.6781519942171299054 ) ) ;
#13575=EDGE_CURVE ( 'NONE', #10202, #11719, #6575, .T. ) ;
#13578=CARTESIAN_POINT ( 'NONE',  ( 2.636624412714236865, 15.91454522070173638, 2.161493821596668585 ) ) ;
#13586=CARTESIAN_POINT ( 'NONE',  ( 0.3095370825347224519, 11.38092634279628790, 7.700448427571914500 ) ) ;
#13590=B_SPLINE_CURVE_WITH_KNOTS ( 'NONE', 3,
 ( #8704, #11304, #5456, #11486, #4122, #5539 ),
 .UNSPECIFIED., .F., .F.,
 ( 4, 2, 4 ),
 ( 4.206917491929696500E-17, 0.0002014099069817275648, 0.0004028198139634130625 ),
 .UNSPECIFIED. ) ;
#13591=ORIENTED_EDGE ( 'NONE', *, *, #408, .F. ) ;
#13595=CARTESIAN_POINT ( 'NONE',  ( 1.959212340397942675, 10.53510106265292023, -6.829000156128068433 ) ) ;
#13596=EDGE_LOOP ( 'NONE', ( #7325, #3660, #13874, #8364 ) ) ;
#13597=CARTESIAN_POINT ( 'NONE',  ( 2.747332970342022840, -11.66639548242798696, -11.45495994260730654 ) ) ;
#13601=CARTESIAN_POINT ( 'NONE',  ( 2.002547531651519996, 11.75462648437101976, 4.532360870844369671 ) ) ;
#13602=CARTESIAN_POINT ( 'NONE',  ( 3.353306896162453921, -13.88482890973695660, -1.348936822032970495 ) ) ;
#13607=EDGE_CURVE ( 'NONE', #13957, #16055, #715, .T. ) ;
#13613=DIRECTION ( 'NONE',  ( -1.000000000000000000, -0.000000000000000000, -0.000000000000000000 ) ) ;
#13621=CARTESIAN_POINT ( 'NONE',  ( 1.845756295923353996, 3.386818134580228179, -11.97166802574122890 ) ) ;
#13627=CARTESIAN_POINT ( 'NONE',  ( 2.123976203522053741, -13.47898556379307244, -7.899625852120357727 ) ) ;
#13630=VERTEX_POINT ( 'NONE', #18135 ) ;
#13639=CARTESIAN_POINT ( 'NONE',  ( 1.847034903785823579, -12.44051878787772836, -0.2299360331935480506 ) ) ;
#13646=AXIS2_PLACEMENT_3D ( 'NONE', #18496, #15914, #14102 ) ;
#13653=CARTESIAN_POINT ( 'NONE',  ( 16.58200780006414732, -0.008650561019685852962, -0.007066318000005976374 ) ) ;
#13663=CARTESIAN_POINT ( 'NONE',  ( 2.123976203522053741, 13.47898556379313284, 7.899625852120258251 ) ) ;
#13664=CARTESIAN_POINT ( 'NONE',  ( 1.846613052777651198, -7.585914669018095857, -9.862487290071081603 ) ) ;
#13668=CARTESIAN_POINT ( 'NONE',  ( 0.3132635586635982294, 3.740017578711948953, -13.21855946425832684 ) ) ;
#13671=CARTESIAN_POINT ( 'NONE',  ( 1.847372867223027848, -10.12831093686727080, 7.228345833872717563 ) ) ;
#13673=EDGE_CURVE ( 'NONE', #6835, #12288, #12350, .T. ) ;
#13675=CARTESIAN_POINT ( 'NONE',  ( 0.3142014840576518031, 0.3830336514510798707, -13.73311050063163563 ) ) ;
#13676=EDGE_LOOP ( 'NONE', ( #59, #16575, #7498, #10067 ) ) ;
#13683=DIRECTION ( 'NONE',  ( 0.000000000000000000, 0.000000000000000000, 1.000000000000000000 ) ) ;
#13686=CARTESIAN_POINT ( 'NONE',  ( 16.57210152137263393, -0.01361613799508851197, -0.005118120558001528972 ) ) ;
#13687=CARTESIAN_POINT ( 'NONE',  ( 16.56822296793089322, -0.007741272030791128758, -0.006547366384935482571 ) ) ;
#13688=CARTESIAN_POINT ( 'NONE',  ( 2.636624412715137922, -15.91454522070252153, 2.161493821597598508 ) ) ;
#13690=ADVANCED_FACE ( 'NONE', ( #11063 ), #6554, .F. ) ;
#13692=EDGE_CURVE ( 'NONE', #13860, #1293, #1769, .T. ) ;
#13693=EDGE_LOOP ( 'NONE', ( #7086, #14917, #9123, #2825 ) ) ;
#13694=( LENGTH_UNIT ( ) NAMED_UNIT ( * ) SI_UNIT ( .MILLI., .METRE. ) );
#13695=FACE_OUTER_BOUND ( 'NONE', #309, .T. ) ;
#13700=ORIENTED_EDGE ( 'NONE', *, *, #14047, .F. ) ;
#13704=VERTEX_POINT ( 'NONE', #15442 ) ;
#13707=ORIENTED_EDGE ( 'NONE', *, *, #10780, .T. ) ;
#13709=ORIENTED_EDGE ( 'NONE', *, *, #1998, .F. ) ;
#13713=CARTESIAN_POINT ( 'NONE',  ( 2.636624412716902288, 7.605649742760546950, -14.14563173255513995 ) ) ;
#13715=( BOUNDED_SURFACE ( )  B_SPLINE_SURFACE ( 3, 1, ( 
 ( #436, #9129 ),
 ( #6265, #12197 ),
 ( #2237, #18022 ),
 ( #8080, #16497 ) ),
 .UNSPECIFIED., .F., .F., .T. ) 
 B_SPLINE_SURFACE_WITH_KNOTS ( ( 4, 4 ),
 ( 2, 2 ),
 ( 0.000000000000000000, 1.000000000000000000 ),
 ( 0.000000000000000000, 1.000000000000000000 ),
 .UNSPECIFIED. ) 
 GEOMETRIC_REPRESENTATION_ITEM ( )  RATIONAL_B_SPLINE_SURFACE ( (
 ( 1.000000000000000000, 1.000000000000000000),
 ( 0.7792777138730158093, 0.9689936506012928330),
 ( 0.7792777138730158093, 0.9689936506012928330),
 ( 1.000000000000000000, 1.000000000000000000) ) ) 
 REPRESENTATION_ITEM ( '' )  SURFACE ( )  );
#13716=CARTESIAN_POINT ( 'NONE',  ( 16.56872352241294521, -0.004907101719995745834, -0.009207754980064182873 ) ) ;
#13727=ORIENTED_EDGE ( 'NONE', *, *, #664, .F. ) ;
#13732=CARTESIAN_POINT ( 'NONE',  ( 0.3142014840576536905, 10.88517824918543297, 8.382000553815492694 ) ) ;
#13734=CARTESIAN_POINT ( 'NONE',  ( 1.861706995891669880, 9.751699138048550708, -7.751853334747211832 ) ) ;
#13741=ORIENTED_EDGE ( 'NONE', *, *, #12412, .F. ) ;
#13742=EDGE_CURVE ( 'NONE', #8095, #8500, #5308, .T. ) ;
#13744=ORIENTED_EDGE ( 'NONE', *, *, #5472, .T. ) ;
#13745=( BOUNDED_SURFACE ( )  B_SPLINE_SURFACE ( 3, 1, ( 
 ( #1344, #1446 ),
 ( #7283, #13102 ),
 ( #17493, #4400 ),
 ( #10234, #16060 ) ),
 .UNSPECIFIED., .F., .F., .T. ) 
 B_SPLINE_SURFACE_WITH_KNOTS ( ( 4, 4 ),
 ( 2, 2 ),
 ( 0.000000000000000000, 1.000000000000000000 ),
 ( 0.000000000000000000, 1.000000000000000000 ),
 .UNSPECIFIED. ) 
 GEOMETRIC_REPRESENTATION_ITEM ( )  RATIONAL_B_SPLINE_SURFACE ( (
 ( 1.000000000000000000, 1.000000000000000000),
 ( 0.9933953342250438912, 0.8357391271907739227),
 ( 0.9933953342250438912, 0.8357391271907739227),
 ( 1.000000000000000000, 1.000000000000000000) ) ) 
 REPRESENTATION_ITEM ( '' )  SURFACE ( )  );
#13749=CARTESIAN_POINT ( 'NONE',  ( 3.950837973638676281, -1.958075594453890789, 14.41405733518059940 ) ) ;
#13750=CARTESIAN_POINT ( 'NONE',  ( 1.847372867223024961, -7.228345833872678483, -10.12831093686730100 ) ) ;
#13760=B_SPLINE_CURVE_WITH_KNOTS ( 'NONE', 3,
 ( #7557, #1425, #184, #12981, #11559, #6013, #284, #6113, #1610, #16041, #17775, #7266, #4678 ),
 .UNSPECIFIED., .F., .F.,
 ( 4, 3, 3, 3, 4 ),
 ( 2.168404344971008868E-18, 0.0002299804304191468746, 0.0004599608082120234371, 0.0006467586077648000654, 0.0008336169836825981817 ),
 .UNSPECIFIED. ) ;
#13761=B_SPLINE_CURVE_WITH_KNOTS ( 'NONE', 3,
 ( #18170, #2121, #18434, #12432, #15480, #9742 ),
 .UNSPECIFIED., .F., .F.,
 ( 4, 2, 4 ),
 ( 3.361796080452501619E-17, 0.0001825746017570592115, 0.0003651492035140848128 ),
 .UNSPECIFIED. ) ;
#13763=B_SPLINE_CURVE_WITH_KNOTS ( 'NONE', 3,
 ( #7470, #7859, #7576, #1927, #6416, #3341 ),
 .UNSPECIFIED., .F., .F.,
 ( 4, 2, 4 ),
 ( 0.000000000000000000, 0.001656992708822557434, 0.003313985417645114867 ),
 .UNSPECIFIED. ) ;
#13764=CARTESIAN_POINT ( 'NONE',  ( 0.4754618798421171855, -10.80499583390519192, 8.775436892861074867 ) ) ;
#13765=ORIENTED_EDGE ( 'NONE', *, *, #14050, .T. ) ;
#13766=CARTESIAN_POINT ( 'NONE',  ( 0.4862570985993235340, -12.97920246947883172, 5.003653737315437944 ) ) ;
#13770=ORIENTED_EDGE ( 'NONE', *, *, #2678, .T. ) ;
#13777=CARTESIAN_POINT ( 'NONE',  ( 1.861628059977341154, -11.66985327793196170, -4.358833901513171405 ) ) ;
#13780=CARTESIAN_POINT ( 'NONE',  ( 16.57778382496167424, -0.006312874906843772387, 0.01354073047775764503 ) ) ;
#13788=VERTEX_POINT ( 'NONE', #9615 ) ;
#13790=ORIENTED_EDGE ( 'NONE', *, *, #14203, .T. ) ;
#13791=LINE ( 'NONE', #11220, #3548 ) ;
#13792=DIRECTION ( 'NONE',  ( 0.000000000000000000, 0.000000000000000000, 1.000000000000000000 ) ) ;
#13802=CARTESIAN_POINT ( 'NONE',  ( 3.950837973638677170, 12.81214529934985080, -6.888253895133152227 ) ) ;
#13803=CARTESIAN_POINT ( 'NONE',  ( 1.847247051441592181, 7.448813758297314180, -9.967131402978116839 ) ) ;
#13806=CONICAL_SURFACE ( 'NONE', #16258, 14.54644660717763927, 0.8559913436420816257 ) ;
#13807=CARTESIAN_POINT ( 'NONE',  ( 16.57778382496167424, -0.01018821665058785610, 0.01092721432668990016 ) ) ;
#13816=( BOUNDED_SURFACE ( )  B_SPLINE_SURFACE ( 3, 1, ( 
 ( #6757, #14009 ),
 ( #9705, #8281 ),
 ( #14294, #14096 ),
 ( #15439, #1094 ) ),
 .UNSPECIFIED., .F., .F., .T. ) 
 B_SPLINE_SURFACE_WITH_KNOTS ( ( 4, 4 ),
 ( 2, 2 ),
 ( 0.000000000000000000, 1.000000000000000000 ),
 ( 0.000000000000000000, 1.000000000000000000 ),
 .UNSPECIFIED. ) 
 GEOMETRIC_REPRESENTATION_ITEM ( )  RATIONAL_B_SPLINE_SURFACE ( (
 ( 1.000000000000000000, 1.000000000000000000),
 ( 0.7792777138730160313, 0.9689936506012927220),
 ( 0.7792777138730160313, 0.9689936506012927220),
 ( 1.000000000000000000, 1.000000000000000000) ) ) 
 REPRESENTATION_ITEM ( '' )  SURFACE ( )  );
#13821=CARTESIAN_POINT ( 'NONE',  ( 0.3939822652208145870, 10.75310269629521365, 8.678192463540208124 ) ) ;
#13822=LINE ( 'NONE', #7927, #1295 ) ;
#13823=CARTESIAN_POINT ( 'NONE',  ( 1.861628059977343819, -7.751680370225458638, 9.751736252960339968 ) ) ;
#13825=CARTESIAN_POINT ( 'NONE',  ( 16.56872352241294521, 0.004564908236399969378, -0.009382111268607383134 ) ) ;
#13828=ORIENTED_EDGE ( 'NONE', *, *, #1779, .F. ) ;
#13829=ORIENTED_EDGE ( 'NONE', *, *, #14023, .T. ) ;
#13831=DIRECTION ( 'NONE',  ( -1.000000000000000000, -0.000000000000000000, -0.000000000000000000 ) ) ;
#13833=CARTESIAN_POINT ( 'NONE',  ( 2.747332970342022840, 14.49942876448592521, 7.555624153089699924 ) ) ;
#13834=EDGE_CURVE ( 'NONE', #11551, #9965, #943, .T. ) ;
#13846=DIRECTION ( 'NONE',  ( 0.000000000000000000, 0.000000000000000000, 1.000000000000000000 ) ) ;
#13851=ORIENTED_EDGE ( 'NONE', *, *, #7813, .F. ) ;
#13852=CARTESIAN_POINT ( 'NONE',  ( 0.4754618798421167414, -12.98792082933641012, -5.007009103465385635 ) ) ;
#13860=VERTEX_POINT ( 'NONE', #4641 ) ;
#13861=CARTESIAN_POINT ( 'NONE',  ( 2.697797270744666243, 8.537712152181008207, -10.19107313879048249 ) ) ;
#13862=CARTESIAN_POINT ( 'NONE',  ( 0.4862570985993235340, -13.44146924561383827, 3.580942890621619412 ) ) ;
#13863=CARTESIAN_POINT ( 'NONE',  ( 1.254009781011620417, -14.64464726212587919, 1.011465182608038305 ) ) ;
#13866=EDGE_CURVE ( 'NONE', #4817, #14724, #7803, .T. ) ;
#13871=ORIENTED_EDGE ( 'NONE', *, *, #7117, .F. ) ;
#13872=CARTESIAN_POINT ( 'NONE',  ( 2.636624412716061627, -7.605649742761058540, -14.14563173255469408 ) ) ;
#13873=EDGE_CURVE ( 'NONE', #18002, #7476, #10937, .T. ) ;
#13874=ORIENTED_EDGE ( 'NONE', *, *, #16986, .T. ) ;
#13887=CARTESIAN_POINT ( 'NONE',  ( 2.320520222536938348, -1.795797593768547085, 15.64520721754664123 ) ) ;
#13898=CARTESIAN_POINT ( 'NONE',  ( 0.8740764193767950330, -14.27348595579787371, -0.8420116711623154560 ) ) ;
#13901=VERTEX_POINT ( 'NONE', #16202 ) ;
#13904=ORIENTED_EDGE ( 'NONE', *, *, #16501, .T. ) ;
#13906=AXIS2_PLACEMENT_3D ( 'NONE', #6454, #18109, #12095 ) ;
#13908=CARTESIAN_POINT ( 'NONE',  ( 0.3137051932979792457, 11.37800749014131263, 7.698472063774513430 ) ) ;
#13910=DIRECTION ( 'NONE',  ( -0.7561779333270775005, -0.2350349629540143537, -0.6106991889125079620 ) ) ;
#13914=EDGE_CURVE ( 'NONE', #14481, #14993, #8457, .T. ) ;
#13924=VERTEX_POINT ( 'NONE', #13426 ) ;
#13926=CARTESIAN_POINT ( 'NONE',  ( 1.846138399168762101, -7.646096044339819819, -9.815003036200495856 ) ) ;
#13932=EDGE_LOOP ( 'NONE', ( #14942, #2358, #925, #1261 ) ) ;
#13935=CARTESIAN_POINT ( 'NONE',  ( 1.254255976357310010, 7.789651112956863521, 12.44256109021772438 ) ) ;
#13941=CARTESIAN_POINT ( 'NONE',  ( 3.512766787570714477, -14.81029789862161117, -2.682019731918549255 ) ) ;
#13943=ORIENTED_EDGE ( 'NONE', *, *, #16449, .T. ) ;
#13947=CARTESIAN_POINT ( 'NONE',  ( 2.747332970342022840, -11.66639548242815572, 11.45495994260713957 ) ) ;
#13954=CARTESIAN_POINT ( 'NONE',  ( 2.002547531651519996, 11.75462648437101976, 4.532360870844369671 ) ) ;
#13957=VERTEX_POINT ( 'NONE', #341 ) ;
#13958=CARTESIAN_POINT ( 'NONE',  ( 1.846955891736119293, -7.098901504650428684, 10.21904526726843798 ) ) ;
#13960=CARTESIAN_POINT ( 'NONE',  ( 0.3137051932979757485, -8.442169467526770887, -10.83767969834812561 ) ) ;
#13964=CARTESIAN_POINT ( 'NONE',  ( 2.636624412714237309, 15.80357026013209953, 2.862162146984226663 ) ) ;
#13965=EDGE_CURVE ( 'NONE', #16993, #17332, #17602, .T. ) ;
#13966=EDGE_CURVE ( 'NONE', #12106, #5602, #17635, .T. ) ;
#13973=CARTESIAN_POINT ( 'NONE',  ( 16.57210152137263393, -0.01402404281922924566, 0.003862718596009228310 ) ) ;
#13974=CARTESIAN_POINT ( 'NONE',  ( 0.3148208552358936485, -4.463611911212133521, -12.99355031785210102 ) ) ;
#13976=ORIENTED_EDGE ( 'NONE', *, *, #7260, .F. ) ;
#13982=EDGE_CURVE ( 'NONE', #14041, #4291, #15060, .T. ) ;
#13983=CARTESIAN_POINT ( 'NONE',  ( 1.861706995891668104, 6.878962591851903063, -10.38589138506418408 ) ) ;
#13985=LINE ( 'NONE', #712, #9324 ) ;
#13991=CARTESIAN_POINT ( 'NONE',  ( 0.3150692679895942816, -13.11337225490255776, 4.099798979280796729 ) ) ;
#13992=B_SPLINE_CURVE_WITH_KNOTS ( 'NONE', 3,
 ( #249, #18874, #12003, #13333, #8845, #10572, #14572, #5972, #17448, #5869, #17541, #14667, #4354 ),
 .UNSPECIFIED., .F., .F.,
 ( 4, 3, 3, 3, 4 ),
 ( 3.198396408832238080E-18, 0.0002299780670421061189, 0.0004599561239687905540, 0.0006896788984287883888, 0.0009194956271626399547 ),
 .UNSPECIFIED. ) ;
#13993=DIRECTION ( 'NONE',  ( -1.000000000000000000, -0.000000000000000000, -0.000000000000000000 ) ) ;
#13995=CARTESIAN_POINT ( 'NONE',  ( 1.959283090834856189, 12.53713130127477804, -0.6676170829052656686 ) ) ;
#13997=VERTEX_POINT ( 'NONE', #8081 ) ;
#14004=VERTEX_POINT ( 'NONE', #17933 ) ;
#14008=CARTESIAN_POINT ( 'NONE',  ( 8.438534575730034959, -6.862570336891073985, -0.2320579683290849293 ) ) ;
#14009=CARTESIAN_POINT ( 'NONE',  ( 0.4754618798421167414, 7.564402563418470393, 11.68486377711969126 ) ) ;
#14016=ORIENTED_EDGE ( 'NONE', *, *, #16986, .F. ) ;
#14019=VERTEX_POINT ( 'NONE', #16591 ) ;
#14023=EDGE_CURVE ( 'NONE', #3394, #11870, #8232, .T. ) ;
#14030=CARTESIAN_POINT ( 'NONE',  ( 2.747332970342022840, -2.705255688517733681, -16.12459247543629104 ) ) ;
#14032=CARTESIAN_POINT ( 'NONE',  ( 16.56753206892534891, 0.001421777558676785977, 0.009389754735541558373 ) ) ;
#14033=LINE ( 'NONE', #937, #12035 ) ;
#14035=CARTESIAN_POINT ( 'NONE',  ( 2.636624412714134280, 2.862162146984768896, 15.80357026013147426 ) ) ;
#14038=B_SPLINE_CURVE_WITH_KNOTS ( 'NONE', 3,
 ( #5862, #2986, #3079, #14753, #1664, #4923 ),
 .UNSPECIFIED., .F., .F.,
 ( 4, 2, 4 ),
 ( 8.673617379884034509E-19, 0.0001828790815886950508, 0.0003657581631773892342 ),
 .UNSPECIFIED. ) ;
#14041=VERTEX_POINT ( 'NONE', #16406 ) ;
#14047=EDGE_CURVE ( 'NONE', #14167, #18612, #12549, .T. ) ;
#14050=EDGE_CURVE ( 'NONE', #16214, #15892, #10979, .T. ) ;
#14051=CARTESIAN_POINT ( 'NONE',  ( 16.56822296793089322, -0.002414375228568911048, -0.009847136207495301580 ) ) ;
#14053=EDGE_CURVE ( 'NONE', #12529, #16119, #1833, .T. ) ;
#14054=ORIENTED_EDGE ( 'NONE', *, *, #12187, .F. ) ;
#14056=CARTESIAN_POINT ( 'NONE',  ( 8.522092701127531811, -1.786985377232080285, 6.722964936702092054 ) ) ;
#14061=CARTESIAN_POINT ( 'NONE',  ( 3.512766787570759774, -13.55823433651952925, 6.535475144496928124 ) ) ;
#14062=CARTESIAN_POINT ( 'NONE',  ( 16.57778382496167424, -0.01354073047775889056, 0.006312874906844006574 ) ) ;
#14063=LINE ( 'NONE', #11299, #2629 ) ;
#14065=CARTESIAN_POINT ( 'NONE',  ( 16.56753206892534891, 0.004253784598196760393, 0.008490833999798020129 ) ) ;
#14067=CARTESIAN_POINT ( 'NONE',  ( 1.846138399168762101, 11.95493567637855392, -3.446241763652874379 ) ) ;
#14068=CARTESIAN_POINT ( 'NONE',  ( 2.002547531651519996, 4.532360870844494016, -11.75462648437097180 ) ) ;
#14071=CARTESIAN_POINT ( 'NONE',  ( 8.522092701127531811, -6.722964936702111594, 1.786985377232005900 ) ) ;
#14080=CARTESIAN_POINT ( 'NONE',  ( 1.918918678667045574, 12.08296592096908384, 3.258447776119875350 ) ) ;
#14086=EDGE_CURVE ( 'NONE', #7817, #14561, #7565, .T. ) ;
#14089=ORIENTED_EDGE ( 'NONE', *, *, #12222, .F. ) ;
#14094=CARTESIAN_POINT ( 'NONE',  ( 1.846138399168762101, -9.815003036200353748, -7.646096044340000120 ) ) ;
#14095=CARTESIAN_POINT ( 'NONE',  ( 0.3095370825347234511, -0.4597470195091165057, 13.73357284481724605 ) ) ;
#14096=CARTESIAN_POINT ( 'NONE',  ( 2.123976203522053297, 7.899625852120206737, 13.47898556379315771 ) ) ;
#14101=CARTESIAN_POINT ( 'NONE',  ( 16.56872352241294521, 0.007512283835805451566, 0.007240717549634016065 ) ) ;
#14102=DIRECTION ( 'NONE',  ( 0.000000000000000000, 0.000000000000000000, 1.000000000000000000 ) ) ;
#14110=CARTESIAN_POINT ( 'NONE',  ( 0.4754618798421162973, 7.564402563418467729, 11.68486377711969304 ) ) ;
#14113=ORIENTED_EDGE ( 'NONE', *, *, #18693, .T. ) ;
#14115=CARTESIAN_POINT ( 'NONE',  ( 1.847372867223022963, -11.80112642014552371, -3.945260592619169948 ) ) ;
#14120=CARTESIAN_POINT ( 'NONE',  ( 1.846138399168762101, -10.30487220521565028, -6.971848976711123136 ) ) ;
#14128=FACE_OUTER_BOUND ( 'NONE', #15904, .T. ) ;
#14132=CARTESIAN_POINT ( 'NONE',  ( 1.846524061778019199, -3.506196582971023545, -11.93805390544204670 ) ) ;
#14133=B_SPLINE_CURVE_WITH_KNOTS ( 'NONE', 3,
 ( #1176, #813, #2687, #15515 ),
 .UNSPECIFIED., .F., .F.,
 ( 4, 4 ),
 ( 0.000000000000000000, 0.002004993803842355579 ),
 .UNSPECIFIED. ) ;
#14135=CARTESIAN_POINT ( 'NONE',  ( 0.3720661004400040439, 13.34435358167253227, 3.575426119359231603 ) ) ;
#14136=ORIENTED_EDGE ( 'NONE', *, *, #4018, .F. ) ;
#14140=CARTESIAN_POINT ( 'NONE',  ( 0.3137051932979792457, -12.91601973349266963, -4.679953077377624560 ) ) ;
#14141=CARTESIAN_POINT ( 'NONE',  ( 1.846138399168762101, 7.646096044339892650, 9.815003036200437236 ) ) ;
#14142=AXIS2_PLACEMENT_3D ( 'NONE', #5474, #13993, #14277 ) ;
#14143=ADVANCED_FACE ( 'NONE', ( #11231 ), #10415, .F. ) ;
#14146=EDGE_CURVE ( 'NONE', #11242, #16036, #14133, .T. ) ;
#14153=CARTESIAN_POINT ( 'NONE',  ( 16.56679352167444819, 0.008252760440870188924, -0.004277682826583317083 ) ) ;
#14154=CARTESIAN_POINT ( 'NONE',  ( 1.254255976357087521, 11.25336128106905420, 9.426444230096484134 ) ) ;
#14155=B_SPLINE_CURVE_WITH_KNOTS ( 'NONE', 3,
 ( #5221, #18314, #11062, #16878 ),
 .UNSPECIFIED., .F., .F.,
 ( 4, 4 ),
 ( 4.873469348537302793E-16, 0.002004993803842133101 ),
 .UNSPECIFIED. ) ;
#14159=ORIENTED_EDGE ( 'NONE', *, *, #4214, .F. ) ;
#14163=CARTESIAN_POINT ( 'NONE',  ( 2.697797270744666687, -8.537712152180933600, 10.19107313879054466 ) ) ;
#14167=VERTEX_POINT ( 'NONE', #1076 ) ;
#14169=B_SPLINE_CURVE_WITH_KNOTS ( 'NONE', 3,
 ( #12533, #3938, #9757, #14154, #5368, #11218 ),
 .UNSPECIFIED., .F., .F.,
 ( 4, 2, 4 ),
 ( 0.000000000000000000, 0.001656992708821599649, 0.003313985417643199299 ),
 .UNSPECIFIED. ) ;
#14173=CARTESIAN_POINT ( 'NONE',  ( 16.56679352167444819, -0.006526964904752395082, 0.006618561353600064395 ) ) ;
#14178=CARTESIAN_POINT ( 'NONE',  ( 0.3150692679895978343, 11.20465057551037091, -7.951395415074959061 ) ) ;
#14186=EDGE_CURVE ( 'NONE', #13031, #14481, #6646, .T. ) ;
#14187=B_SPLINE_CURVE_WITH_KNOTS ( 'NONE', 3,
 ( #11890, #8733, #1762, #1473, #14562, #1656 ),
 .UNSPECIFIED., .F., .F.,
 ( 4, 2, 4 ),
 ( 3.337089043155729788E-17, 0.0001825746017570573684, 0.0003651492035140813976 ),
 .UNSPECIFIED. ) ;
#14189=CARTESIAN_POINT ( 'NONE',  ( 1.977436885026784941, 6.153171729169462090, -14.12046670317587704 ) ) ;
#14198=B_SPLINE_CURVE_WITH_KNOTS ( 'NONE', 3,
 ( #16541, #13668, #10615, #580, #3128, #9261 ),
 .UNSPECIFIED., .F., .F.,
 ( 4, 2, 4 ),
 ( 2.790109556687801444E-18, 0.0002017457492448089095, 0.0004034914984896150001 ),
 .UNSPECIFIED. ) ;
#14201=VERTEX_POINT ( 'NONE', #4524 ) ;
#14202=EDGE_CURVE ( 'NONE', #5120, #12310, #13224, .T. ) ;
#14203=EDGE_CURVE ( 'NONE', #17476, #6505, #14903, .T. ) ;
#14204=( BOUNDED_SURFACE ( )  B_SPLINE_SURFACE ( 3, 1, ( 
 ( #8001, #12202 ),
 ( #13807, #13627 ),
 ( #10767, #15335 ),
 ( #18027, #6655 ) ),
 .UNSPECIFIED., .F., .F., .T. ) 
 B_SPLINE_SURFACE_WITH_KNOTS ( ( 4, 4 ),
 ( 2, 2 ),
 ( 0.000000000000000000, 1.000000000000000000 ),
 ( 0.000000000000000000, 1.000000000000000000 ),
 .UNSPECIFIED. ) 
 GEOMETRIC_REPRESENTATION_ITEM ( )  RATIONAL_B_SPLINE_SURFACE ( (
 ( 1.000000000000000000, 1.000000000000000000),
 ( 0.7792777138730158093, 0.9689936506012928330),
 ( 0.7792777138730158093, 0.9689936506012928330),
 ( 1.000000000000000000, 1.000000000000000000) ) ) 
 REPRESENTATION_ITEM ( '' )  SURFACE ( )  );
#14212=CARTESIAN_POINT ( 'NONE',  ( 3.353306896162455697, -13.62210141459498125, 3.007732942432364442 ) ) ;
#14213=CARTESIAN_POINT ( 'NONE',  ( 16.56753206892534891, -0.008432171035096417550, 0.004368917149005425125 ) ) ;
#14214=CARTESIAN_POINT ( 'NONE',  ( 0.3137051932979792457, 13.20008686438105983, 3.805684345189833451 ) ) ;
#14217=CARTESIAN_POINT ( 'NONE',  ( 16.56822296793089322, 0.0007467251401297140970, 0.01011126603341077831 ) ) ;
#14223=CARTESIAN_POINT ( 'NONE',  ( 8.522092701127531811, -5.841710761610102942, -3.777034505568587885 ) ) ;
#14226=DIRECTION ( 'NONE',  ( -1.000000000000000000, -0.000000000000000000, -0.000000000000000000 ) ) ;
#14229=EDGE_LOOP ( 'NONE', ( #17916, #18615, #7691, #15254 ) ) ;
#14234=CARTESIAN_POINT ( 'NONE',  ( 16.57605080000000086, 3.061616997868383141E-16, -2.500000000000000000 ) ) ;
#14238=CARTESIAN_POINT ( 'NONE',  ( 16.56822296793089322, -0.005339139727952984908, -0.008619100080558656299 ) ) ;
#14239=ORIENTED_EDGE ( 'NONE', *, *, #6393, .F. ) ;
#14242=DIRECTION ( 'NONE',  ( -0.7561779333270775005, -0.1688126975276600938, 0.6322161072786937064 ) ) ;
#14243=CARTESIAN_POINT ( 'NONE',  ( 0.3148208552358917056, -13.73693263646118901, 0.2299193288886990094 ) ) ;
#14250=AXIS2_PLACEMENT_3D ( 'NONE', #6079, #14765, #13431 ) ;
#14253=CARTESIAN_POINT ( 'NONE',  ( 1.562796894703937678, 0.000000000000000000, 0.000000000000000000 ) ) ;
#14259=ORIENTED_EDGE ( 'NONE', *, *, #18693, .F. ) ;
#14277=DIRECTION ( 'NONE',  ( 0.000000000000000000, 0.000000000000000000, 1.000000000000000000 ) ) ;
#14281=CARTESIAN_POINT ( 'NONE',  ( 2.636624412715435462, -15.80357026013316712, -2.862162146983298516 ) ) ;
#14285=ORIENTED_EDGE ( 'NONE', *, *, #7158, .T. ) ;
#14291=CARTESIAN_POINT ( 'NONE',  ( 0.3137051932979757485, -4.679953077377398074, -12.91601973349275134 ) ) ;
#14293=CARTESIAN_POINT ( 'NONE',  ( 8.522092701127531811, 6.722964936702098271, 1.786985377232055860 ) ) ;
#14294=CARTESIAN_POINT ( 'NONE',  ( 16.57778382496167424, -0.01092721432669101385, 0.01018821665058845458 ) ) ;
#14299=CARTESIAN_POINT ( 'NONE',  ( 16.56872352241294521, -0.001821578298043862289, 0.01027347319884366027 ) ) ;
#14300=DIRECTION ( 'NONE',  ( -1.000000000000000000, -0.000000000000000000, -0.000000000000000000 ) ) ;
#14302=EDGE_LOOP ( 'NONE', ( #17728, #1996, #13770, #8562 ) ) ;
#14307=CARTESIAN_POINT ( 'NONE',  ( 2.697797270744668019, -12.89731672021093090, 3.226410068829379973 ) ) ;
#14309=EDGE_LOOP ( 'NONE', ( #7494, #13372, #9531, #8160 ) ) ;
#14314=CARTESIAN_POINT ( 'NONE',  ( 16.56822296793089322, -0.008619100080559813359, -0.005339139727952636229 ) ) ;
#14319=( BOUNDED_SURFACE ( )  B_SPLINE_SURFACE ( 3, 1, ( 
 ( #13825, #8198 ),
 ( #15076, #923 ),
 ( #1995, #7833 ),
 ( #13653, #6391 ) ),
 .UNSPECIFIED., .F., .F., .T. ) 
 B_SPLINE_SURFACE_WITH_KNOTS ( ( 4, 4 ),
 ( 2, 2 ),
 ( 0.000000000000000000, 1.000000000000000000 ),
 ( 0.000000000000000000, 1.000000000000000000 ),
 .UNSPECIFIED. ) 
 GEOMETRIC_REPRESENTATION_ITEM ( )  RATIONAL_B_SPLINE_SURFACE ( (
 ( 1.000000000000000000, 1.000000000000000000),
 ( 0.7792777138730160313, 0.9689936506012927220),
 ( 0.7792777138730160313, 0.9689936506012927220),
 ( 1.000000000000000000, 1.000000000000000000) ) ) 
 REPRESENTATION_ITEM ( '' )  SURFACE ( )  );
#14323=ORIENTED_EDGE ( 'NONE', *, *, #15042, .T. ) ;
#14332=ORIENTED_EDGE ( 'NONE', *, *, #747, .T. ) ;
#14333=CARTESIAN_POINT ( 'NONE',  ( 16.56753206892534891, -0.006669401563385243120, -0.006760771273035091553 ) ) ;
#14336=CARTESIAN_POINT ( 'NONE',  ( 0.3151926232592464627, -13.09050869763090219, -4.172630140040936908 ) ) ;
#14340=CARTESIAN_POINT ( 'NONE',  ( 0.4754618798421167414, 3.583352865732670534, 13.45049478164061263 ) ) ;
#14343=CARTESIAN_POINT ( 'NONE',  ( 0.4862570985993235340, -8.769551628660812170, 10.79774104611370333 ) ) ;
#14347=CARTESIAN_POINT ( 'NONE',  ( 1.847412631396505356, 10.04119192206686328, 7.348689888531877656 ) ) ;
#14349=( BOUNDED_SURFACE ( )  B_SPLINE_SURFACE ( 3, 1, ( 
 ( #2631, #16101 ),
 ( #2983, #11264 ),
 ( #3075, #5501 ),
 ( #9800, #14564 ) ),
 .UNSPECIFIED., .F., .F., .T. ) 
 B_SPLINE_SURFACE_WITH_KNOTS ( ( 4, 4 ),
 ( 2, 2 ),
 ( 0.000000000000000000, 1.000000000000000000 ),
 ( 0.000000000000000000, 1.000000000000000000 ),
 .UNSPECIFIED. ) 
 GEOMETRIC_REPRESENTATION_ITEM ( )  RATIONAL_B_SPLINE_SURFACE ( (
 ( 1.000000000000000000, 1.000000000000000000),
 ( 0.9933953342250438912, 0.8357391271907739227),
 ( 0.9933953342250438912, 0.8357391271907739227),
 ( 1.000000000000000000, 1.000000000000000000) ) ) 
 REPRESENTATION_ITEM ( '' )  SURFACE ( )  );
#14350=ORIENTED_EDGE ( 'NONE', *, *, #9332, .T. ) ;
#14359=LINE ( 'NONE', #11321, #11712 ) ;
#14360=CARTESIAN_POINT ( 'NONE',  ( 2.002547531651519996, 9.778737580845815458, -7.942910686618064986 ) ) ;
#14363=ORIENTED_EDGE ( 'NONE', *, *, #8264, .F. ) ;
#14368=VECTOR ( 'NONE', #7445, 1000.000000000000114 ) ;
#14373=CARTESIAN_POINT ( 'NONE',  ( 3.950837973638668288, 0.000000000000000000, 0.000000000000000000 ) ) ;
#14374=CARTESIAN_POINT ( 'NONE',  ( 1.846524061778019199, -9.853584647934329865, -7.597197846158187495 ) ) ;
#14376=CARTESIAN_POINT ( 'NONE',  ( 16.56822296793089322, 0.003834730849371879857, 0.009385634690642069913 ) ) ;
#14380=AXIS2_PLACEMENT_3D ( 'NONE', #6, #17490, #1341 ) ;
#14382=CARTESIAN_POINT ( 'NONE',  ( 1.342453679581834924, 9.456403821038962931, -11.38190519890843255 ) ) ;
#14388=ORIENTED_EDGE ( 'NONE', *, *, #16460, .F. ) ;
#14390=VERTEX_POINT ( 'NONE', #17905 ) ;
#14391=B_SPLINE_CURVE_WITH_KNOTS ( 'NONE', 3,
 ( #7418, #4261, #11903, #11614, #16109, #1386 ),
 .UNSPECIFIED., .F., .F.,
 ( 4, 2, 4 ),
 ( 4.003426615173598157E-17, 0.0002014099069817276190, 0.0004028198139634152309 ),
 .UNSPECIFIED. ) ;
#14393=CARTESIAN_POINT ( 'NONE',  ( 0.3095370825347224519, 13.73357284481724783, -0.4597470195090672673 ) ) ;
#14396=CARTESIAN_POINT ( 'NONE',  ( 16.58200780006414732, -0.009393638146079803797, 0.006043560077721671885 ) ) ;
#14402=B_SPLINE_CURVE_WITH_KNOTS ( 'NONE', 3,
 ( #3451, #8238, #10927, #18085, #2126, #4985 ),
 .UNSPECIFIED., .F., .F.,
 ( 4, 2, 4 ),
 ( 3.522439207679730663E-17, 0.0001825746017570575039, 0.0003651492035140797713 ),
 .UNSPECIFIED. ) ;
#14410=CARTESIAN_POINT ( 'NONE',  ( 1.959212340397916030, 9.750290364083625150, 7.909199412631181758 ) ) ;
#14421=CARTESIAN_POINT ( 'NONE',  ( 0.3148213771069381384, -13.73693585713733611, -0.2297580318216151940 ) ) ;
#14425=CARTESIAN_POINT ( 'NONE',  ( 0.4862570985993252548, -3.580942890621766406, 13.44146924561379741 ) ) ;
#14434=ORIENTED_EDGE ( 'NONE', *, *, #17191, .T. ) ;
#14438=CARTESIAN_POINT ( 'NONE',  ( 0.3095370825347224519, -13.20347358821917183, 3.806662003783363613 ) ) ;
#14439=EDGE_LOOP ( 'NONE', ( #5777, #7487, #3022, #16415 ) ) ;
#14440=CARTESIAN_POINT ( 'NONE',  ( 1.846822687350021974, 9.891732594446578375, 7.547953575784160485 ) ) ;
#14445=CARTESIAN_POINT ( 'NONE',  ( 0.3137051932979809665, 3.805684345189785933, 13.20008686438107581 ) ) ;
#14447=FACE_OUTER_BOUND ( 'NONE', #7677, .T. ) ;
#14452=CARTESIAN_POINT ( 'NONE',  ( 2.636624412714237309, 7.605649742761960042, 14.14563173255213613 ) ) ;
#14453=CARTESIAN_POINT ( 'NONE',  ( 0.3095370825347233956, -13.20347358821911854, -3.806662003783550574 ) ) ;
#14458=CARTESIAN_POINT ( 'NONE',  ( 16.56753206892534891, 0.001549402974393146101, -0.009369540855502138735 ) ) ;
#14461=CARTESIAN_POINT ( 'NONE',  ( 2.320520222537543198, -15.43440824796705613, 3.126729907239071959 ) ) ;
#14462=STYLED_ITEM ( 'NONE', ( #387 ), #10437 ) ;
#14470=CARTESIAN_POINT ( 'NONE',  ( 16.56753206892534891, -0.004368917149004301892, 0.008432171035096367243 ) ) ;
#14473=DIRECTION ( 'NONE',  ( 0.000000000000000000, 0.000000000000000000, 1.000000000000000000 ) ) ;
#14477=CARTESIAN_POINT ( 'NONE',  ( 3.950837973638668288, 0.000000000000000000, 0.000000000000000000 ) ) ;
#14478=EDGE_LOOP ( 'NONE', ( #9448, #7648, #12059, #6485 ) ) ;
#14481=VERTEX_POINT ( 'NONE', #12874 ) ;
#14492=ADVANCED_FACE ( 'NONE', ( #5512 ), #10004, .T. ) ;
#14497=CARTESIAN_POINT ( 'NONE',  ( 2.636624412715137478, -2.862162146983530775, 15.80357026013314048 ) ) ;
#14498=CARTESIAN_POINT ( 'NONE',  ( 16.56753206892534891, -0.006760771273036220858, -0.006669401563384898778 ) ) ;
#14499=CARTESIAN_POINT ( 'NONE',  ( 2.636624412715093513, -14.14563173255330142, 7.605649742761597665 ) ) ;
#14501=CARTESIAN_POINT ( 'NONE',  ( 0.3137051932979757485, -7.698472063774552510, 11.37800749014128421 ) ) ;
#14506=EDGE_LOOP ( 'NONE', ( #1294, #9956, #1679, #9090 ) ) ;
#14516=CARTESIAN_POINT ( 'NONE',  ( 16.56753206892534891, -0.009369540855502522109, 0.001549402974394259360 ) ) ;
#14521=CARTESIAN_POINT ( 'NONE',  ( 16.56679352167444819, -0.006618561353600137254, -0.006526964904752322223 ) ) ;
#14523=EDGE_CURVE ( 'NONE', #11535, #9475, #17162, .T. ) ;
#14525=ORIENTED_EDGE ( 'NONE', *, *, #10930, .F. ) ;
#14532=CARTESIAN_POINT ( 'NONE',  ( 0.000000000000000000, 0.000000000000000000, 0.000000000000000000 ) ) ;
#14533=EDGE_LOOP ( 'NONE', ( #10497, #3277, #5591, #9968 ) ) ;
#14534=CARTESIAN_POINT ( 'NONE',  ( 2.636624412715384391, -11.60464335004044223, -11.10302021258006278 ) ) ;
#14537=ORIENTED_EDGE ( 'NONE', *, *, #14818, .T. ) ;
#14539=CARTESIAN_POINT ( 'NONE',  ( 2.636624412715137478, -2.862162146983530775, 15.80357026013314048 ) ) ;
#14542=CARTESIAN_POINT ( 'NONE',  ( 2.636624412714134280, 2.862162146984768896, 15.80357026013147426 ) ) ;
#14548=EDGE_CURVE ( 'NONE', #9110, #3117, #6870, .T. ) ;
#14550=CARTESIAN_POINT ( 'NONE',  ( 1.846524061778020531, 3.506196582971103926, 11.93805390544202361 ) ) ;
#14554=FACE_OUTER_BOUND ( 'NONE', #9456, .T. ) ;
#14558=AXIS2_PLACEMENT_3D ( 'NONE', #6362, #4541, #14852 ) ;
#14561=VERTEX_POINT ( 'NONE', #2645 ) ;
#14562=CARTESIAN_POINT ( 'NONE',  ( 1.845756295923355328, -3.386818134580144690, 11.97166802574125022 ) ) ;
#14564=CARTESIAN_POINT ( 'NONE',  ( 0.3095370825347233956, 4.681152801286161846, 12.91933430393609683 ) ) ;
#14566=CARTESIAN_POINT ( 'NONE',  ( 2.123976203522053297, -7.899625852120107261, -13.47898556379321633 ) ) ;
#14568=CARTESIAN_POINT ( 'NONE',  ( 2.636624412717099908, 11.60464335004051861, -11.10302021258208249 ) ) ;
#14569=FACE_OUTER_BOUND ( 'NONE', #6929, .T. ) ;
#14571=FACE_OUTER_BOUND ( 'NONE', #13500, .T. ) ;
#14572=CARTESIAN_POINT ( 'NONE',  ( 0.3151928476913591903, 13.73922860838471749, -0.0002082997484259338093 ) ) ;
#14574=ORIENTED_EDGE ( 'NONE', *, *, #1380, .F. ) ;
#14582=CARTESIAN_POINT ( 'NONE',  ( 0.3170788640506441158, 13.74111462631963576, -0.1533108587036642600 ) ) ;
#14583=DIRECTION ( 'NONE',  ( 0.7561779333270775005, -0.03481510524965699543, 0.6534392409364816467 ) ) ;
#14584=VERTEX_POINT ( 'NONE', #18895 ) ;
#14586=CARTESIAN_POINT ( 'NONE',  ( 16.57210152137263393, -0.01402404281923042353, -0.003862718596009419997 ) ) ;
#14587=B_SPLINE_CURVE_WITH_KNOTS ( 'NONE', 3,
 ( #6087, #11917, #3399, #4941, #10481, #13438 ),
 .UNSPECIFIED., .F., .F.,
 ( 4, 2, 4 ),
 ( 0.000000000000000000, 0.0001828790815886946713, 0.0003657581631773893427 ),
 .UNSPECIFIED. ) ;
#14588=LINE ( 'NONE', #10486, #15849 ) ;
#14597=EDGE_CURVE ( 'NONE', #11580, #6611, #79, .T. ) ;
#14601=VERTEX_POINT ( 'NONE', #3015 ) ;
#14606=CARTESIAN_POINT ( 'NONE',  ( 1.342453679581834924, 14.34050741580211508, -3.649820028552582585 ) ) ;
#14621=CARTESIAN_POINT ( 'NONE',  ( 0.4862570985993252548, 5.003653737315486794, 12.97920246947881395 ) ) ;
#14635=B_SPLINE_CURVE_WITH_KNOTS ( 'NONE', 3,
 ( #12024, #6190, #4571, #17468, #10394, #1409 ),
 .UNSPECIFIED., .F., .F.,
 ( 4, 2, 4 ),
 ( 8.940560153363745023E-19, 0.0001828790815886946442, 0.0003657581631773883669 ),
 .UNSPECIFIED. ) ;
#14637=CARTESIAN_POINT ( 'NONE',  ( 0.8740779401508875779, -3.609949156401464965, 13.83508928787437142 ) ) ;
#14645=DIRECTION ( 'NONE',  ( -1.000000000000000000, -0.000000000000000000, -0.000000000000000000 ) ) ;
#14654=CARTESIAN_POINT ( 'NONE',  ( 16.57778382496167424, -0.007244066302947598825, 0.01306626476309386518 ) ) ;
#14659=CARTESIAN_POINT ( 'NONE',  ( 0.3142011359265368120, 4.608101617236774139, 12.94258167753013922 ) ) ;
#14662=CARTESIAN_POINT ( 'NONE',  ( 0.4862570985993235340, 11.67702470553376060, -7.559321496869298329 ) ) ;
#14667=CARTESIAN_POINT ( 'NONE',  ( 0.3142011359265305392, 13.73310835363014348, -0.3830873813806805472 ) ) ;
#14671=ORIENTED_EDGE ( 'NONE', *, *, #6837, .F. ) ;
#14672=EDGE_CURVE ( 'NONE', #4027, #3394, #7402, .T. ) ;
#14674=EDGE_LOOP ( 'NONE', ( #30, #5479, #5023, #9514 ) ) ;
#14684=CARTESIAN_POINT ( 'NONE',  ( 0.4862570985993252548, -3.580942890621766406, 13.44146924561379741 ) ) ;
#14687=DIRECTION ( 'NONE',  ( 1.000000000000000000, 0.000000000000000000, 0.000000000000000000 ) ) ;
#14690=CARTESIAN_POINT ( 'NONE',  ( 0.3145734862173198421, -7.825584895511444650, -11.29227530924455003 ) ) ;
#14707=B_SPLINE_CURVE_WITH_KNOTS ( 'NONE', 3,
 ( #1707, #10610, #3025, #7555, #13368, #283 ),
 .UNSPECIFIED., .F., .F.,
 ( 4, 2, 4 ),
 ( 2.468197616305571356E-18, 0.0002017457492448094245, 0.0004034914984896164096 ),
 .UNSPECIFIED. ) ;
#14711=CARTESIAN_POINT ( 'NONE',  ( 0.3170788640506440603, 4.392045232375992647, -13.02120094575823472 ) ) ;
#14712=ORIENTED_EDGE ( 'NONE', *, *, #6680, .T. ) ;
#14715=CARTESIAN_POINT ( 'NONE',  ( 2.705023505549862595, -10.24007717649586624, 8.489131503859741912 ) ) ;
#14716=CARTESIAN_POINT ( 'NONE',  ( 1.977228804421669262, 6.152949558600965041, 14.12033626431027322 ) ) ;
#14719=CARTESIAN_POINT ( 'NONE',  ( 16.56753206892534891, -0.004253784598196239108, 0.008490833999798910042 ) ) ;
#14724=VERTEX_POINT ( 'NONE', #3511 ) ;
#14726=LINE ( 'NONE', #11778, #1508 ) ;
#14728=EDGE_CURVE ( 'NONE', #13924, #14584, #17656, .T. ) ;
#14730=ADVANCED_FACE ( 'NONE', ( #9248 ), #14319, .F. ) ;
#14734=CARTESIAN_POINT ( 'NONE',  ( 3.950837973638675393, 6.888253895133292559, 12.81214529934977797 ) ) ;
#14735=CARTESIAN_POINT ( 'NONE',  ( 0.3720661004400040439, -13.34435358167250207, -3.575426119359325750 ) ) ;
#14736=CARTESIAN_POINT ( 'NONE',  ( 3.950837973638668288, 14.41405733518061716, 1.958075594453843493 ) ) ;
#14739=CARTESIAN_POINT ( 'NONE',  ( 0.3142011359265323156, -7.762194356530850214, 11.33549115679420538 ) ) ;
#14741=ORIENTED_EDGE ( 'NONE', *, *, #9263, .T. ) ;
#14747=VERTEX_POINT ( 'NONE', #10786 ) ;
#14752=CARTESIAN_POINT ( 'NONE',  ( 2.747332970342022840, 2.705255688518072965, -16.12459247543623064 ) ) ;
#14753=CARTESIAN_POINT ( 'NONE',  ( 1.918921323896325193, -4.466082741316288462, 11.69058285425789201 ) ) ;
#14755=CARTESIAN_POINT ( 'NONE',  ( 8.438534575730034959, 4.221456476902743837, -5.415535776177475391 ) ) ;
#14760=CARTESIAN_POINT ( 'NONE',  ( 16.56753206892534891, 0.004253784598196178393, -0.008490833999798937798 ) ) ;
#14762=AXIS2_PLACEMENT_3D ( 'NONE', #13443, #6384, #17850 ) ;
#14764=CARTESIAN_POINT ( 'NONE',  ( 1.846613052777650976, -11.72395935470501627, 4.166957398589803852 ) ) ;
#14765=DIRECTION ( 'NONE',  ( -1.000000000000000000, -0.000000000000000000, -0.000000000000000000 ) ) ;
#14766=EDGE_LOOP ( 'NONE', ( #8445, #1275, #2786, #9157 ) ) ;
#14773=CARTESIAN_POINT ( 'NONE',  ( 1.846138399168762101, -7.646096044339819819, -9.815003036200495856 ) ) ;
#14779=CARTESIAN_POINT ( 'NONE',  ( 0.3058872367615230181, -4.821066432589238282, -12.87003593440633331 ) ) ;
#14781=ADVANCED_FACE ( 'NONE', ( #9713 ), #16280, .F. ) ;
#14795=CARTESIAN_POINT ( 'NONE',  ( 3.512766787570769100, 13.55823433651956833, -6.535475144496838418 ) ) ;
#14798=ORIENTED_EDGE ( 'NONE', *, *, #3580, .F. ) ;
#14799=CARTESIAN_POINT ( 'NONE',  ( 1.861628059977344263, -6.879051339207215676, -10.38573835516720401 ) ) ;
#14814=CARTESIAN_POINT ( 'NONE',  ( 3.377929128793393687, 12.02809354424100619, 7.136734442940879219 ) ) ;
#14815=VERTEX_POINT ( 'NONE', #9986 ) ;
#14818=EDGE_CURVE ( 'NONE', #13997, #8831, #15172, .T. ) ;
#14827=CARTESIAN_POINT ( 'NONE',  ( 16.56753206892534891, -0.009369540855502119653, -0.001549402974393242162 ) ) ;
#14830=CARTESIAN_POINT ( 'NONE',  ( 0.4384471787762824757, -13.84291427302852107, 0.7363690479465839767 ) ) ;
#14831=ORIENTED_EDGE ( 'NONE', *, *, #3955, .T. ) ;
#14844=ADVANCED_FACE ( 'NONE', ( #2716 ), #6930, .T. ) ;
#14852=DIRECTION ( 'NONE',  ( 0.000000000000000000, 0.000000000000000000, 1.000000000000000000 ) ) ;
#14855=AXIS2_PLACEMENT_3D ( 'NONE', #535, #895, #10754 ) ;
#14857=CARTESIAN_POINT ( 'NONE',  ( 16.56782317627811096, -0.009439921864426449247, -0.002708056627497712563 ) ) ;
#14860=CARTESIAN_POINT ( 'NONE',  ( 0.000000000000000000, 0.000000000000000000, 0.000000000000000000 ) ) ;
#14862=APPLICATION_CONTEXT ( 'automotive_design' ) ;
#14864=CARTESIAN_POINT ( 'NONE',  ( 2.636624412714236865, 0.000000000000000000, 0.000000000000000000 ) ) ;
#14866=CARTESIAN_POINT ( 'NONE',  ( 3.074695600507349358, 10.75417554975707368, -11.23985886659415279 ) ) ;
#14870=EDGE_LOOP ( 'NONE', ( #4746, #16707, #17724, #4719 ) ) ;
#14871=ORIENTED_EDGE ( 'NONE', *, *, #7923, .T. ) ;
#14873=ORIENTED_EDGE ( 'NONE', *, *, #15665, .T. ) ;
#14875=CARTESIAN_POINT ( 'NONE',  ( 0.3145729642390401870, 0.3065092323351212289, 13.73540280162740501 ) ) ;
#14876=EDGE_CURVE ( 'NONE', #9110, #16337, #5544, .T. ) ;
#14879=CARTESIAN_POINT ( 'NONE',  ( 2.002547531651519996, -7.942910686618100513, -9.778737580845787036 ) ) ;
#14882=CARTESIAN_POINT ( 'NONE',  ( 0.4754618798421162973, 13.45049478164064638, -3.583352865732528425 ) ) ;
#14883=CARTESIAN_POINT ( 'NONE',  ( 1.847380140988738262, 12.44273713935591097, -0.1101766933249076624 ) ) ;
#14884=CARTESIAN_POINT ( 'NONE',  ( 1.562796894703937678, 0.000000000000000000, 0.000000000000000000 ) ) ;
#14885=CARTESIAN_POINT ( 'NONE',  ( 1.254255976357671942, -5.487601330835209623, 13.61551404021223455 ) ) ;
#14888=CARTESIAN_POINT ( 'NONE',  ( 0.3151930723728413319, -8.013866567350813597, -11.16020735774775829 ) ) ;
#14893=VERTEX_POINT ( 'NONE', #9888 ) ;
#14894=ORIENTED_EDGE ( 'NONE', *, *, #5927, .T. ) ;
#14899=CARTESIAN_POINT ( 'NONE',  ( 3.353306896162456585, 10.44017738170056298, 9.252610477110303933 ) ) ;
#14903=CIRCLE ( 'NONE', #16737, 14.54644660717763927 ) ;
#14907=FILL_AREA_STYLE_COLOUR ( '', #7102 ) ;
#14909=ORIENTED_EDGE ( 'NONE', *, *, #3930, .F. ) ;
#14917=ORIENTED_EDGE ( 'NONE', *, *, #13337, .F. ) ;
#14920=ORIENTED_EDGE ( 'NONE', *, *, #6998, .F. ) ;
#14923=CARTESIAN_POINT ( 'NONE',  ( 16.56679352167444819, -0.008311568981098013675, -0.004162264567718770153 ) ) ;
#14925=EDGE_CURVE ( 'NONE', #6426, #15645, #3035, .T. ) ;
#14927=AXIS2_PLACEMENT_3D ( 'NONE', #6522, #18268, #5169 ) ;
#14935=CARTESIAN_POINT ( 'NONE',  ( 0.4754618798421167414, -10.80499583390506402, -8.775436892861231186 ) ) ;
#14937=EDGE_CURVE ( 'NONE', #4406, #10941, #13992, .T. ) ;
#14939=CARTESIAN_POINT ( 'NONE',  ( 8.438534575730034959, -6.454982381540305347, 2.341351102130253103 ) ) ;
#14940=CARTESIAN_POINT ( 'NONE',  ( 0.3170788640506441158, 4.392045232375811459, 13.02120094575829867 ) ) ;
#14942=ORIENTED_EDGE ( 'NONE', *, *, #13742, .F. ) ;
#14947=ORIENTED_EDGE ( 'NONE', *, *, #12876, .T. ) ;
#14950=CARTESIAN_POINT ( 'NONE',  ( 16.56872352241294521, 0.01033355228142499721, 0.001442253899401261912 ) ) ;
#14952=CARTESIAN_POINT ( 'NONE',  ( 16.57778382496167424, 0.01466529584256784369, 0.002851818597094051173 ) ) ;
#14953=CARTESIAN_POINT ( 'NONE',  ( 3.950837973638676281, 1.958075594453990487, -14.41405733518058341 ) ) ;
#14955=CARTESIAN_POINT ( 'NONE',  ( 3.950837973638675393, -2.591948120961706792, -14.31366178983255466 ) ) ;
#14964=ORIENTED_EDGE ( 'NONE', *, *, #462, .T. ) ;
#14976=CARTESIAN_POINT ( 'NONE',  ( 1.847426409206449405, 0.01438352405959898543, -12.44303504652077841 ) ) ;
#14977=EDGE_CURVE ( 'NONE', #5119, #18618, #10823, .T. ) ;
#14978=CARTESIAN_POINT ( 'NONE',  ( 0.8740779401507027258, 13.83508928787419912, 3.609949156401401904 ) ) ;
#14979=EDGE_CURVE ( 'NONE', #13788, #11580, #17404, .T. ) ;
#14991=CARTESIAN_POINT ( 'NONE',  ( 3.664313757352972711, 10.50730552161232545, 9.645155442698788661 ) ) ;
#14993=VERTEX_POINT ( 'NONE', #3288 ) ;
#15000=CARTESIAN_POINT ( 'NONE',  ( 3.950837973638676281, 2.591948120962007884, -14.31366178983250670 ) ) ;
#15006=CARTESIAN_POINT ( 'NONE',  ( 2.320521194583479829, -10.64885423995220393, -11.60169518685964363 ) ) ;
#15009=CARTESIAN_POINT ( 'NONE',  ( 0.3308579732647030647, -4.812490080619291177, 12.88563776947744088 ) ) ;
#15010=EDGE_CURVE ( 'NONE', #13262, #8831, #13069, .T. ) ;
#15011=ORIENTED_EDGE ( 'NONE', *, *, #5833, .T. ) ;
#15017=CARTESIAN_POINT ( 'NONE',  ( 16.56782317627811096, -0.008141063682853442660, -0.005492611183757281634 ) ) ;
#15024=CARTESIAN_POINT ( 'NONE',  ( 1.846138399168762101, -6.971848976711082280, 10.30487220521567693 ) ) ;
#15034=CARTESIAN_POINT ( 'NONE',  ( 2.353870697619111496, -12.92712089195302561, -0.7635393531607687079 ) ) ;
#15041=CARTESIAN_POINT ( 'NONE',  ( 16.56782317627811096, -0.006045301465876687375, -0.007739510688078416953 ) ) ;
#15042=EDGE_CURVE ( 'NONE', #4171, #15500, #16513, .T. ) ;
#15048=CARTESIAN_POINT ( 'NONE',  ( 0.4754618798421162973, -3.583352865732575943, -13.45049478164063395 ) ) ;
#15051=CARTESIAN_POINT ( 'NONE',  ( 0.3939822652208131992, -11.57634296752772229, 7.545099438011985349 ) ) ;
#15058=EDGE_LOOP ( 'NONE', ( #10330, #9349, #6359, #5725 ) ) ;
#15060=B_SPLINE_CURVE_WITH_KNOTS ( 'NONE', 3,
 ( #15243, #2068, #15051, #9321, #10954, #12098 ),
 .UNSPECIFIED., .F., .F.,
 ( 4, 2, 4 ),
 ( 4.253224384355279651E-17, 0.0002014099069817287574, 0.0004028198139634150141 ),
 .UNSPECIFIED. ) ;
#15065=CARTESIAN_POINT ( 'NONE',  ( 0.3137051932979809665, -4.679953077377580151, 12.91601973349268917 ) ) ;
#15067=CARTESIAN_POINT ( 'NONE',  ( 3.074695600507134419, -7.366518011945905720, -13.70113613813221676 ) ) ;
#15073=CARTESIAN_POINT ( 'NONE',  ( 2.002547531651519996, -10.57595306287296921, 6.845637710436153434 ) ) ;
#15076=CARTESIAN_POINT ( 'NONE',  ( 16.57210152137263393, -0.0006600038696348781500, -0.01453130299868639688 ) ) ;
#15078=B_SPLINE_CURVE_WITH_KNOTS ( 'NONE', 3,
 ( #15073, #2175, #16609, #13543, #9523, #18132 ),
 .UNSPECIFIED., .F., .F.,
 ( 4, 2, 4 ),
 ( 0.000000000000000000, 0.001500839035891550271, 0.003001678071783100542 ),
 .UNSPECIFIED. ) ;
#15082=( BOUNDED_SURFACE ( )  B_SPLINE_SURFACE ( 3, 1, ( 
 ( #8825, #7405 ),
 ( #13215, #5657 ),
 ( #8546, #133 ),
 ( #4152, #9972 ) ),
 .UNSPECIFIED., .F., .F., .T. ) 
 B_SPLINE_SURFACE_WITH_KNOTS ( ( 4, 4 ),
 ( 2, 2 ),
 ( 0.000000000000000000, 1.000000000000000000 ),
 ( 0.000000000000000000, 1.000000000000000000 ),
 .UNSPECIFIED. ) 
 GEOMETRIC_REPRESENTATION_ITEM ( )  RATIONAL_B_SPLINE_SURFACE ( (
 ( 1.000000000000000000, 1.000000000000000000),
 ( 0.9593108457356467333, 0.9995965569486454649),
 ( 0.9593108457356467333, 0.9995965569486454649),
 ( 1.000000000000000000, 1.000000000000000000) ) ) 
 REPRESENTATION_ITEM ( '' )  SURFACE ( )  );
#15090=CARTESIAN_POINT ( 'NONE',  ( 3.950837973638675393, 10.51028938476217967, 10.05648675950130233 ) ) ;
#15091=PRODUCT_DEFINITION_FORMATION_WITH_SPECIFIED_SOURCE ( 'ANY', '', #537, .NOT_KNOWN. ) ;
#15093=VERTEX_POINT ( 'NONE', #10956 ) ;
#15095=CARTESIAN_POINT ( 'NONE',  ( 1.846138399168762989, 11.69739621335922308, 4.238866729160444713 ) ) ;
#15097=CARTESIAN_POINT ( 'NONE',  ( 16.56872352241294521, -0.009207754980064163791, 0.004907101719995779661 ) ) ;
#15101=EDGE_CURVE ( 'NONE', #3664, #15826, #7812, .T. ) ;
#15105=CARTESIAN_POINT ( 'NONE',  ( 1.847372867223030068, 11.86627781945713167, -3.744745203533853317 ) ) ;
#15110=CARTESIAN_POINT ( 'NONE',  ( 16.56872352241294521, -0.001442253899401298341, 0.01033355228142499027 ) ) ;
#15111=ORIENTED_EDGE ( 'NONE', *, *, #8543, .T. ) ;
#15112=LINE ( 'NONE', #12060, #10256 ) ;
#15114=ORIENTED_EDGE ( 'NONE', *, *, #2429, .F. ) ;
#15115=FACE_OUTER_BOUND ( 'NONE', #18807, .T. ) ;
#15119=CARTESIAN_POINT ( 'NONE',  ( 0.4384471787762852513, 7.540925784514715957, -11.63197976518319798 ) ) ;
#15122=B_SPLINE_CURVE_WITH_KNOTS ( 'NONE', 3,
 ( #18380, #1437, #11130, #16856, #18904, #3763, #16769, #3670, #15510, #8693, #12463, #16951, #18721 ),
 .UNSPECIFIED., .F., .F.,
 ( 4, 3, 3, 3, 4 ),
 ( 0.000000000000000000, 0.0002299804304191501543, 0.0004599608082120262018, 0.0006467586077648019086, 0.0008336169836825998080 ),
 .UNSPECIFIED. ) ;
#15133=FACE_OUTER_BOUND ( 'NONE', #18483, .T. ) ;
#15143=CARTESIAN_POINT ( 'NONE',  ( 8.438534575730034959, 6.598402093327905504, -1.899950616255119407 ) ) ;
#15144=CARTESIAN_POINT ( 'NONE',  ( 16.56782317627811096, 0.008141063682853404496, 0.005492611183757338013 ) ) ;
#15145=CARTESIAN_POINT ( 'NONE',  ( 1.254255976357524505, -1.011593778944422262, 14.64488542023450535 ) ) ;
#15147=CARTESIAN_POINT ( 'NONE',  ( 0.4385251269669978025, 12.93791070501034390, 4.978066129061732070 ) ) ;
#15148=FACE_OUTER_BOUND ( 'NONE', #4287, .T. ) ;
#15150=EDGE_CURVE ( 'NONE', #11214, #12864, #7615, .T. ) ;
#15152=CARTESIAN_POINT ( 'NONE',  ( 0.3132642857406495174, 0.5276792104584192566, -13.72733058964894681 ) ) ;
#15154=CARTESIAN_POINT ( 'NONE',  ( 1.847034903785823357, 7.498375632854758166, -9.929438108952064468 ) ) ;
#15158=CARTESIAN_POINT ( 'NONE',  ( 0.3095370825347224519, -3.806662003783507497, 13.20347358821913275 ) ) ;
#15160=ORIENTED_EDGE ( 'NONE', *, *, #15381, .T. ) ;
#15162=VERTEX_POINT ( 'NONE', #16864 ) ;
#15164=VERTEX_POINT ( 'NONE', #12200 ) ;
#15165=CARTESIAN_POINT ( 'NONE',  ( 1.846524061778018311, -12.43723828841088341, -0.3544704288993787422 ) ) ;
#15166=( BOUNDED_SURFACE ( )  B_SPLINE_SURFACE ( 3, 1, ( 
 ( #3787, #7274 ),
 ( #15952, #5814 ),
 ( #14521, #2840 ),
 ( #17104, #18015 ) ),
 .UNSPECIFIED., .F., .F., .T. ) 
 B_SPLINE_SURFACE_WITH_KNOTS ( ( 4, 4 ),
 ( 2, 2 ),
 ( 0.000000000000000000, 1.000000000000000000 ),
 ( 0.000000000000000000, 1.000000000000000000 ),
 .UNSPECIFIED. ) 
 GEOMETRIC_REPRESENTATION_ITEM ( )  RATIONAL_B_SPLINE_SURFACE ( (
 ( 1.000000000000000000, 1.000000000000000000),
 ( 0.9593108457356467333, 0.9995965569486454649),
 ( 0.9593108457356467333, 0.9995965569486454649),
 ( 1.000000000000000000, 1.000000000000000000) ) ) 
 REPRESENTATION_ITEM ( '' )  SURFACE ( )  );
#15168=CARTESIAN_POINT ( 'NONE',  ( 1.846138399168762101, 9.815003036200520725, -7.646096044339786069 ) ) ;
#15172=CIRCLE ( 'NONE', #13646, 16.06066017081991149 ) ;
#15177=DIRECTION ( 'NONE',  ( -1.000000000000000000, -0.000000000000000000, -0.000000000000000000 ) ) ;
#15178=( GEOMETRIC_REPRESENTATION_CONTEXT ( 3 ) GLOBAL_UNCERTAINTY_ASSIGNED_CONTEXT ( ( #8838 ) ) GLOBAL_UNIT_ASSIGNED_CONTEXT ( ( #13694, #410, #18544 ) ) REPRESENTATION_CONTEXT ( 'NONE', 'WORKASPACE' ) );
#15185=ORIENTED_EDGE ( 'NONE', *, *, #7188, .F. ) ;
#15188=DIRECTION ( 'NONE',  ( -1.000000000000000000, -0.000000000000000000, -0.000000000000000000 ) ) ;
#15190=CARTESIAN_POINT ( 'NONE',  ( 16.58200780006414732, 0.01041078477703982763, -0.004047297414157931088 ) ) ;
#15191=CARTESIAN_POINT ( 'NONE',  ( 1.847380140988736708, -7.402792205949027426, -10.00162556679659076 ) ) ;
#15194=ORIENTED_EDGE ( 'NONE', *, *, #14876, .T. ) ;
#15196=CARTESIAN_POINT ( 'NONE',  ( 2.636624412714237309, 7.605649742761960042, 14.14563173255213613 ) ) ;
#15198=CARTESIAN_POINT ( 'NONE',  ( 1.847461586945732703, -10.04711372545050097, 7.341074796295904648 ) ) ;
#15201=CARTESIAN_POINT ( 'NONE',  ( 3.950837973638676281, -6.888253895133199300, -12.81214529934982949 ) ) ;
#15203=DIRECTION ( 'NONE',  ( -1.000000000000000000, -0.000000000000000000, -0.000000000000000000 ) ) ;
#15205=ORIENTED_EDGE ( 'NONE', *, *, #17148, .F. ) ;
#15206=CARTESIAN_POINT ( 'NONE',  ( 16.58200780006414732, 0.0006320991582340733123, 0.01115192838421469670 ) ) ;
#15211=CARTESIAN_POINT ( 'NONE',  ( 3.950837973638668288, 14.41405733518061538, -1.958075594453841273 ) ) ;
#15214=CARTESIAN_POINT ( 'NONE',  ( 0.3170788640506441158, 13.02120094575834131, -4.392045232375677344 ) ) ;
#15216=CARTESIAN_POINT ( 'NONE',  ( 1.918921323896321862, -11.69058285425787247, -4.466082741316331983 ) ) ;
#15221=CARTESIAN_POINT ( 'NONE',  ( 16.58200780006414732, -0.008650561019685578876, 0.007066318000004673597 ) ) ;
#15228=CARTESIAN_POINT ( 'NONE',  ( 0.3142011359265350912, -11.33549115679417696, -7.762194356530893735 ) ) ;
#15233=CARTESIAN_POINT ( 'NONE',  ( 3.950837973638668288, 0.000000000000000000, 0.000000000000000000 ) ) ;
#15234=ORIENTED_EDGE ( 'NONE', *, *, #721, .F. ) ;
#15237=LINE ( 'NONE', #16674, #4422 ) ;
#15239=CARTESIAN_POINT ( 'NONE',  ( 16.56872352241294521, 0.004907101719995680782, 0.009207754980064214098 ) ) ;
#15242=CARTESIAN_POINT ( 'NONE',  ( 16.56822296793089322, -0.009847136207495329335, 0.002414375228568802195 ) ) ;
#15243=CARTESIAN_POINT ( 'NONE',  ( 0.4862570985993235340, -11.67702470553370553, 7.559321496869385371 ) ) ;
#15245=CARTESIAN_POINT ( 'NONE',  ( 0.4862570985993235340, 8.769551628660735787, 10.79774104611376373 ) ) ;
#15249=CIRCLE ( 'NONE', #16155, 14.54644660717763927 ) ;
#15250=ORIENTED_EDGE ( 'NONE', *, *, #1001, .F. ) ;
#15253=ORIENTED_EDGE ( 'NONE', *, *, #15375, .T. ) ;
#15254=ORIENTED_EDGE ( 'NONE', *, *, #12954, .T. ) ;
#15263=CARTESIAN_POINT ( 'NONE',  ( 0.4384471787762840855, 12.93784327393180433, -4.978024343488911541 ) ) ;
#15264=CARTESIAN_POINT ( 'NONE',  ( 0.3170788640506440603, -0.1533108587037102788, 13.74111462631963576 ) ) ;
#15269=ORIENTED_EDGE ( 'NONE', *, *, #5210, .F. ) ;
#15274=LINE ( 'NONE', #7938, #3091 ) ;
#15275=CARTESIAN_POINT ( 'NONE',  ( 2.747332970342022840, 14.49942876448603180, -7.555624153089486761 ) ) ;
#15278=CARTESIAN_POINT ( 'NONE',  ( 0.3939875929385642239, 13.34133634968955917, 3.598491969338272867 ) ) ;
#15285=B_SPLINE_CURVE_WITH_KNOTS ( 'NONE', 3,
 ( #3650, #12071, #9197, #10829, #2037, #15024 ),
 .UNSPECIFIED., .F., .F.,
 ( 4, 2, 4 ),
 ( 3.303099811781675862E-17, 0.0001825746017570575581, 0.0003651492035140820481 ),
 .UNSPECIFIED. ) ;
#15288=CARTESIAN_POINT ( 'NONE',  ( 0.3137051932979757485, 12.91601973349276733, -4.679953077377353665 ) ) ;
#15294=ORIENTED_EDGE ( 'NONE', *, *, #3630, .F. ) ;
#15295=CARTESIAN_POINT ( 'NONE',  ( 16.56782317627811096, -0.003357783021327886107, -0.009228812961908644183 ) ) ;
#15301=CARTESIAN_POINT ( 'NONE',  ( 2.320521194582656932, -15.64520804578280888, 1.795798718313643683 ) ) ;
#15304=CARTESIAN_POINT ( 'NONE',  ( 0.4754618798421171855, -13.45049478164057000, -3.583352865732813530 ) ) ;
#15308=ORIENTED_EDGE ( 'NONE', *, *, #18238, .T. ) ;
#15311=FACE_OUTER_BOUND ( 'NONE', #3685, .T. ) ;
#15313=ORIENTED_EDGE ( 'NONE', *, *, #14086, .F. ) ;
#15314=ORIENTED_EDGE ( 'NONE', *, *, #7372, .T. ) ;
#15315=CARTESIAN_POINT ( 'NONE',  ( 2.002547531651519996, 4.532360870844494016, -11.75462648437097180 ) ) ;
#15320=EDGE_CURVE ( 'NONE', #5117, #1184, #16011, .T. ) ;
#15326=CARTESIAN_POINT ( 'NONE',  ( 1.254009781011619751, -13.61532727684435251, 5.487405433548490308 ) ) ;
#15331=CARTESIAN_POINT ( 'NONE',  ( 0.3148208552358926493, 8.260375059853341639, 10.97826876274314856 ) ) ;
#15333=CARTESIAN_POINT ( 'NONE',  ( 1.845756295923357326, 12.43231724724606835, -0.4783934145702458673 ) ) ;
#15335=CARTESIAN_POINT ( 'NONE',  ( 1.342453679581834924, -12.51077660954460136, -7.902645620902585932 ) ) ;
#15337=ORIENTED_EDGE ( 'NONE', *, *, #2024, .F. ) ;
#15339=ORIENTED_EDGE ( 'NONE', *, *, #1380, .T. ) ;
#15344=ADVANCED_FACE ( 'NONE', ( #7211 ), #2071, .T. ) ;
#15359=CARTESIAN_POINT ( 'NONE',  ( 16.57778382496167424, 0.01018821665058777630, -0.01092721432668997822 ) ) ;
#15360=CARTESIAN_POINT ( 'NONE',  ( 3.664313757352979373, 13.97913389346637736, -2.831308606787096949 ) ) ;
#15363=CARTESIAN_POINT ( 'NONE',  ( 1.846138399168762989, 3.446241763652997836, 11.95493567637851839 ) ) ;
#15364=ORIENTED_EDGE ( 'NONE', *, *, #14146, .F. ) ;
#15366=CIRCLE ( 'NONE', #4071, 14.54644660717763927 ) ;
#15367=FACE_OUTER_BOUND ( 'NONE', #1451, .T. ) ;
#15373=CARTESIAN_POINT ( 'NONE',  ( 2.705023505549862595, -7.115606223895247773, 11.23800170568054568 ) ) ;
#15374=CARTESIAN_POINT ( 'NONE',  ( 0.3148213771069364175, 0.2297580318216631001, -13.73693585713733967 ) ) ;
#15375=EDGE_CURVE ( 'NONE', #7136, #4080, #15777, .T. ) ;
#15381=EDGE_CURVE ( 'NONE', #4624, #4964, #17615, .T. ) ;
#15383=VECTOR ( 'NONE', #1599, 1000.000000000000000 ) ;
#15387=CARTESIAN_POINT ( 'NONE',  ( 2.353870697619111052, 4.720869121224300358, -12.05847592522638934 ) ) ;
#15388=B_SPLINE_CURVE_WITH_KNOTS ( 'NONE', 3,
 ( #1694, #6097, #17760, #16326, #14883, #3205, #9054, #1796, #7638, #17853, #2189, #15546, #8121 ),
 .UNSPECIFIED., .F., .F.,
 ( 4, 3, 3, 3, 4 ),
 ( 1.897353801849632760E-18, 0.0002299804304191482569, 0.0004599608082120252260, 0.0006467586077648016917, 0.0008336169836825988323 ),
 .UNSPECIFIED. ) ;
#15391=CARTESIAN_POINT ( 'NONE',  ( 1.846138399168762101, -7.646096044339961040, 9.815003036200383946 ) ) ;
#15393=CARTESIAN_POINT ( 'NONE',  ( 0.4862570985993235340, 7.559321496869593204, -11.67702470553357053 ) ) ;
#15394=CARTESIAN_POINT ( 'NONE',  ( 1.847034903785821136, 10.19974412751574810, -7.126331315909155251 ) ) ;
#15401=ORIENTED_EDGE ( 'NONE', *, *, #5210, .T. ) ;
#15402=CARTESIAN_POINT ( 'NONE',  ( 0.8740764193767940338, -9.070946295054064024, 11.05257066464529281 ) ) ;
#15404=DIRECTION ( 'NONE',  ( 0.000000000000000000, 0.000000000000000000, 1.000000000000000000 ) ) ;
#15410=CARTESIAN_POINT ( 'NONE',  ( 2.747332970342022840, 16.17136872824898575, -2.409922051470736459 ) ) ;
#15414=CONICAL_SURFACE ( 'NONE', #2864, 14.54644660717763927, 0.8559913436420816257 ) ;
#15420=CARTESIAN_POINT ( 'NONE',  ( 0.3132635586635980074, -13.21855946425834283, -3.740017578711901436 ) ) ;
#15431=DIRECTION ( 'NONE',  ( 0.7561779333270775005, -0.6322161072786965930, 0.1688126975276491026 ) ) ;
#15438=CARTESIAN_POINT ( 'NONE',  ( 16.56872352241294521, 0.004907101719995680782, 0.009207754980064214098 ) ) ;
#15439=CARTESIAN_POINT ( 'NONE',  ( 16.58200780006414732, -0.004047297414158971054, 0.01041078477704053193 ) ) ;
#15441=CARTESIAN_POINT ( 'NONE',  ( 0.3720661004400037664, -10.73619472937695640, -8.694226082900707198 ) ) ;
#15442=CARTESIAN_POINT ( 'NONE',  ( 2.636624412714134280, 2.862162146984768896, 15.80357026013147426 ) ) ;
#15443=FACE_OUTER_BOUND ( 'NONE', #14309, .T. ) ;
#15444=EDGE_CURVE ( 'NONE', #17476, #9556, #11027, .T. ) ;
#15457=ORIENTED_EDGE ( 'NONE', *, *, #10677, .T. ) ;
#15458=CARTESIAN_POINT ( 'NONE',  ( 0.3058872367615230181, -8.562166468153638021, -10.75034008168925226 ) ) ;
#15460=CARTESIAN_POINT ( 'NONE',  ( 0.3132642857406501280, 11.41580579227788128, -7.641821025099742926 ) ) ;
#15462=CARTESIAN_POINT ( 'NONE',  ( 0.4862570985993235340, -7.559321496869339185, -11.67702470553373750 ) ) ;
#15466=DIRECTION ( 'NONE',  ( -1.000000000000000000, -0.000000000000000000, -0.000000000000000000 ) ) ;
#15469=VERTEX_POINT ( 'NONE', #13872 ) ;
#15473=CARTESIAN_POINT ( 'NONE',  ( 0.4754618798421162973, 8.775436892861113947, 10.80499583390515994 ) ) ;
#15475=CIRCLE ( 'NONE', #1857, 14.54644660717763927 ) ;
#15476=ADVANCED_FACE ( 'NONE', ( #7784 ), #18713, .F. ) ;
#15480=CARTESIAN_POINT ( 'NONE',  ( 1.845756295923360435, -4.296776483139397307, -11.67600463554277468 ) ) ;
#15486=CARTESIAN_POINT ( 'NONE',  ( 1.847461586945727152, 10.04711372545055781, -7.341074796295831817 ) ) ;
#15489=B_SPLINE_CURVE_WITH_KNOTS ( 'NONE', 3,
 ( #12273, #18104, #5003, #16670 ),
 .UNSPECIFIED., .F., .F.,
 ( 4, 4 ),
 ( 1.117853977359352840E-16, 0.002004993803842554205 ),
 .UNSPECIFIED. ) ;
#15490=( NAMED_UNIT ( * ) SI_UNIT ( $, .STERADIAN. ) SOLID_ANGLE_UNIT ( ) );
#15491=CARTESIAN_POINT ( 'NONE',  ( 3.950837973638675393, -13.10350451991845055, 6.316429227969417859 ) ) ;
#15495=CARTESIAN_POINT ( 'NONE',  ( 0.3095370825347224519, -10.84046130709052491, -8.444334731364122604 ) ) ;
#15498=CARTESIAN_POINT ( 'NONE',  ( 1.342453679581834924, -0.9602753779829698022, -14.76648944001040498 ) ) ;
#15499=CARTESIAN_POINT ( 'NONE',  ( 1.861628059977342486, 4.358833901513207820, -11.66985327793194216 ) ) ;
#15500=VERTEX_POINT ( 'NONE', #7692 ) ;
#15506=CARTESIAN_POINT ( 'NONE',  ( 1.861706995891664773, 10.38589138506426934, 6.878962591851789377 ) ) ;
#15510=CARTESIAN_POINT ( 'NONE',  ( 1.847247051441591292, 7.177495230324704600, 10.16425585218603267 ) ) ;
#15515=CARTESIAN_POINT ( 'NONE',  ( 2.636624412715999011, 2.161493821598055920, -15.91454522070273647 ) ) ;
#15518=CARTESIAN_POINT ( 'NONE',  ( 2.002547531651519996, 12.57989064830759496, -0.6781519942172177240 ) ) ;
#15519=CARTESIAN_POINT ( 'NONE',  ( 2.002547531651519996, 7.942910686618313676, -9.778737580845612953 ) ) ;
#15521=EDGE_LOOP ( 'NONE', ( #17730, #2574, #12030, #14054 ) ) ;
#15523=ORIENTED_EDGE ( 'NONE', *, *, #15897, .T. ) ;
#15525=CARTESIAN_POINT ( 'NONE',  ( 0.3307726912345187453, 0.5948952607472642873, 13.74203354050372461 ) ) ;
#15526=CARTESIAN_POINT ( 'NONE',  ( 0.3939822652208163078, 4.930560016699244485, -12.90851734139301499 ) ) ;
#15528=CARTESIAN_POINT ( 'NONE',  ( 16.56753206892534891, -0.004368917149005395635, -0.008432171035096433162 ) ) ;
#15531=CARTESIAN_POINT ( 'NONE',  ( 2.002547531651519996, -4.532360870844247991, -11.75462648437106417 ) ) ;
#15541=ORIENTED_EDGE ( 'NONE', *, *, #8735, .T. ) ;
#15544=CARTESIAN_POINT ( 'NONE',  ( 1.846613052777651198, 3.520031056876471887, -11.93415846513958023 ) ) ;
#15545=CARTESIAN_POINT ( 'NONE',  ( 1.846524061778019421, -7.023652644192194927, -10.27028962889604813 ) ) ;
#15546=CARTESIAN_POINT ( 'NONE',  ( 1.846524061778019199, 12.43723828841088341, 0.3544704288992919228 ) ) ;
#15547=CARTESIAN_POINT ( 'NONE',  ( 0.3720661004400037664, -8.694226082900666341, 10.73619472937699015 ) ) ;
#15548=CARTESIAN_POINT ( 'NONE',  ( 1.977228804421389485, 13.27756617201186096, 7.806978995470745808 ) ) ;
#15553=CARTESIAN_POINT ( 'NONE',  ( 1.846613052777650310, -11.93415846513959444, -3.520031056876430142 ) ) ;
#15557=CARTESIAN_POINT ( 'NONE',  ( 0.3132642857406530146, 13.21852905223344088, -3.740125687984594993 ) ) ;
#15562=ORIENTED_EDGE ( 'NONE', *, *, #8671, .T. ) ;
#15563=CARTESIAN_POINT ( 'NONE',  ( 2.002547531651521773, 9.778737580845699995, 7.942910686618207983 ) ) ;
#15570=CARTESIAN_POINT ( 'NONE',  ( 1.847412631396503357, -7.348689888531914072, 10.04119192206683664 ) ) ;
#15572=CARTESIAN_POINT ( 'NONE',  ( 2.636624412715138366, -11.10302021257964888, 11.60464335004044223 ) ) ;
#15575=CARTESIAN_POINT ( 'NONE',  ( 2.002547531651519996, 7.942910686618173344, 9.778737580845726640 ) ) ;
#15576=EDGE_CURVE ( 'NONE', #4785, #381, #8705, .T. ) ;
#15591=CARTESIAN_POINT ( 'NONE',  ( 3.950837973638668288, 0.000000000000000000, 0.000000000000000000 ) ) ;
#15598=DIRECTION ( 'NONE',  ( 0.000000000000000000, 0.000000000000000000, 1.000000000000000000 ) ) ;
#15599=ADVANCED_FACE ( 'NONE', ( #9944 ), #11530, .F. ) ;
#15617=LINE ( 'NONE', #7032, #18474 ) ;
#15625=EDGE_CURVE ( 'NONE', #4817, #3568, #6721, .T. ) ;
#15627=ORIENTED_EDGE ( 'NONE', *, *, #7311, .T. ) ;
#15630=CARTESIAN_POINT ( 'NONE',  ( 3.950837973638677170, -14.31366178983255466, 2.591948120961746760 ) ) ;
#15633=ORIENTED_EDGE ( 'NONE', *, *, #2848, .T. ) ;
#15634=CARTESIAN_POINT ( 'NONE',  ( 16.56782317627811096, -0.0003415813796006971566, 0.009814734722107082768 ) ) ;
#15636=B_SPLINE_CURVE_WITH_KNOTS ( 'NONE', 3,
 ( #5825, #4699, #305, #15009, #3242, #6133 ),
 .UNSPECIFIED., .F., .F.,
 ( 4, 2, 4 ),
 ( 4.083989690778167730E-17, 0.0002014099069817300042, 0.0004028198139634191341 ),
 .UNSPECIFIED. ) ;
#15640=CARTESIAN_POINT ( 'NONE',  ( 16.56872352241294521, 0.007240717549633888563, 0.007512283835804339609 ) ) ;
#15645=VERTEX_POINT ( 'NONE', #11114 ) ;
#15648=FACE_OUTER_BOUND ( 'NONE', #7684, .T. ) ;
#15652=CARTESIAN_POINT ( 'NONE',  ( 1.847247051441591514, -0.1676840720646167182, 12.44188156437794213 ) ) ;
#15653=B_SPLINE_CURVE_WITH_KNOTS ( 'NONE', 3,
 ( #7247, #2815, #13155, #10098 ),
 .UNSPECIFIED., .F., .F.,
 ( 4, 4 ),
 ( 0.000000000000000000, 0.002004993803842804005 ),
 .UNSPECIFIED. ) ;
#15659=DIRECTION ( 'NONE',  ( 0.7561779333270775005, 0.4122479608995740508, -0.5081796452863232005 ) ) ;
#15661=CARTESIAN_POINT ( 'NONE',  ( 3.950837973638676281, -14.41405733518061716, 1.958075594453740687 ) ) ;
#15663=DIRECTION ( 'NONE',  ( 0.000000000000000000, 0.000000000000000000, 1.000000000000000000 ) ) ;
#15664=CARTESIAN_POINT ( 'NONE',  ( 3.950837973638677170, -1.958075594453692503, -14.41405733518062959 ) ) ;
#15665=EDGE_CURVE ( 'NONE', #17143, #15164, #8941, .T. ) ;
#15667=CARTESIAN_POINT ( 'NONE',  ( 16.56872352241294521, 0.004564908236400220913, 0.009382111268606271176 ) ) ;
#15668=VECTOR ( 'NONE', #17171, 1000.000000000000000 ) ;
#15677=CARTESIAN_POINT ( 'NONE',  ( 3.377929128793395908, -12.84367544717939680, 5.536064832134110603 ) ) ;
#15679=CARTESIAN_POINT ( 'NONE',  ( 16.56872352241294521, -0.007240717549633941472, -0.007512283835804289302 ) ) ;
#15682=ORIENTED_EDGE ( 'NONE', *, *, #15320, .T. ) ;
#15688=CARTESIAN_POINT ( 'NONE',  ( 2.002547531651519996, 12.17374746633578475, 3.242439124566693476 ) ) ;
#15689=UNCERTAINTY_MEASURE_WITH_UNIT (LENGTH_MEASURE( 1.000000000000000082E-05 ), #6212, 'distance_accuracy_value', 'NONE');
#15690=EDGE_CURVE ( 'NONE', #17676, #2099, #18731, .T. ) ;
#15694=CARTESIAN_POINT ( 'NONE',  ( 16.56872352241294521, 0.009207754980064196751, -0.004907101719995712874 ) ) ;
#15695=CARTESIAN_POINT ( 'NONE',  ( 1.846955891736119737, 0.2634721419535199782, 12.44001089941741256 ) ) ;
#15696=CARTESIAN_POINT ( 'NONE',  ( 1.847372867223028070, 3.744745203533978106, 11.86627781945709792 ) ) ;
#15698=B_SPLINE_CURVE_WITH_KNOTS ( 'NONE', 3,
 ( #1068, #18561, #2683, #11312, #17128, #9851 ),
 .UNSPECIFIED., .F., .F.,
 ( 4, 2, 4 ),
 ( 0.000000000000000000, 0.0001828790815886955387, 0.0003657581631773888006 ),
 .UNSPECIFIED. ) ;
#15700=CARTESIAN_POINT ( 'NONE',  ( 0.3148208552358927048, 10.97826876274324270, -8.260375059853219071 ) ) ;
#15701=CARTESIAN_POINT ( 'NONE',  ( 16.58200780006414732, -0.01080144354108990290, 0.002844973367390998473 ) ) ;
#15707=ORIENTED_EDGE ( 'NONE', *, *, #2442, .F. ) ;
#15714=VECTOR ( 'NONE', #5666, 1000.000000000000114 ) ;
#15716=CARTESIAN_POINT ( 'NONE',  ( 0.000000000000000000, 0.000000000000000000, 0.000000000000000000 ) ) ;
#15719=CARTESIAN_POINT ( 'NONE',  ( 2.747332970342022840, 11.45495994260734918, -11.66639548242795144 ) ) ;
#15721=ORIENTED_EDGE ( 'NONE', *, *, #14728, .T. ) ;
#15725=CONICAL_SURFACE ( 'NONE', #2311, 14.54644660717763927, 0.8559913436420816257 ) ;
#15729=CARTESIAN_POINT ( 'NONE',  ( 0.3095370825347234511, -13.20347358821917183, 3.806662003783360504 ) ) ;
#15730=CARTESIAN_POINT ( 'NONE',  ( 0.3137051932979775248, -0.4596302728638797519, -13.73004976592202553 ) ) ;
#15732=CARTESIAN_POINT ( 'NONE',  ( 16.56872352241294521, 0.009382111268607367521, 0.004564908236399998868 ) ) ;
#15738=CARTESIAN_POINT ( 'NONE',  ( 1.959212340397943786, -10.53510106265286517, 6.829000156128149257 ) ) ;
#15740=DIRECTION ( 'NONE',  ( 0.000000000000000000, 0.000000000000000000, 1.000000000000000000 ) ) ;
#15742=CARTESIAN_POINT ( 'NONE',  ( 0.4862570985993235340, 13.44146924561385958, -3.580942890621532371 ) ) ;
#15749=CARTESIAN_POINT ( 'NONE',  ( 16.57210152137263393, -0.01136813053532068768, -0.009075239946108325934 ) ) ;
#15751=CARTESIAN_POINT ( 'NONE',  ( 1.847426409206446518, -0.01438352405999345808, 12.44303504652078018 ) ) ;
#15752=ORIENTED_EDGE ( 'NONE', *, *, #6251, .F. ) ;
#15757=CARTESIAN_POINT ( 'NONE',  ( 1.847340342630335641, -0.1245571717074845930, -12.44248139376885831 ) ) ;
#15762=CARTESIAN_POINT ( 'NONE',  ( 16.57778382496167424, 0.006312874906843677844, -0.01354073047775769707 ) ) ;
#15763=( BOUNDED_SURFACE ( )  B_SPLINE_SURFACE ( 3, 1, ( 
 ( #12498, #933 ),
 ( #9538, #6774 ),
 ( #18508, #15547 ),
 ( #8122, #5417 ) ),
 .UNSPECIFIED., .F., .F., .T. ) 
 B_SPLINE_SURFACE_WITH_KNOTS ( ( 4, 4 ),
 ( 2, 2 ),
 ( 0.000000000000000000, 1.000000000000000000 ),
 ( 0.000000000000000000, 1.000000000000000000 ),
 .UNSPECIFIED. ) 
 GEOMETRIC_REPRESENTATION_ITEM ( )  RATIONAL_B_SPLINE_SURFACE ( (
 ( 1.000000000000000000, 1.000000000000000000),
 ( 0.9933953342250436691, 0.8357391271907733676),
 ( 0.9933953342250436691, 0.8357391271907733676),
 ( 1.000000000000000000, 1.000000000000000000) ) ) 
 REPRESENTATION_ITEM ( '' )  SURFACE ( )  );
#15770=CARTESIAN_POINT ( 'NONE',  ( 1.342453679581834924, 3.649820028552730022, 14.34050741580208133 ) ) ;
#15777=B_SPLINE_CURVE_WITH_KNOTS ( 'NONE', 3,
 ( #10255, #8628, #6054, #16180, #13022, #1647 ),
 .UNSPECIFIED., .F., .F.,
 ( 4, 2, 4 ),
 ( 4.014301552767626103E-17, 0.0002014099069817288116, 0.0004028198139634175078 ),
 .UNSPECIFIED. ) ;
#15779=CARTESIAN_POINT ( 'NONE',  ( 0.3145734862173253377, 4.535879238195112073, -12.96846406299301258 ) ) ;
#15787=CARTESIAN_POINT ( 'NONE',  ( 0.3142011359265295956, -0.3830873813805367734, -13.73310835363015059 ) ) ;
#15788=CARTESIAN_POINT ( 'NONE',  ( 1.959283090834842644, 12.12982544407805108, 3.239245055717007826 ) ) ;
#15789=EDGE_CURVE ( 'NONE', #14893, #15164, #15962, .T. ) ;
#15790=ADVANCED_FACE ( 'NONE', ( #1540 ), #13745, .F. ) ;
#15791=ORIENTED_EDGE ( 'NONE', *, *, #17255, .T. ) ;
#15795=CARTESIAN_POINT ( 'NONE',  ( 0.4754618798421162973, -12.98792082933640835, -5.007009103465388300 ) ) ;
#15802=ORIENTED_EDGE ( 'NONE', *, *, #6620, .F. ) ;
#15804=CARTESIAN_POINT ( 'NONE',  ( 8.522092701127531811, -0.3779863304871711183, 6.946128462138593918 ) ) ;
#15807=FACE_OUTER_BOUND ( 'NONE', #5796, .T. ) ;
#15811=CARTESIAN_POINT ( 'NONE',  ( 3.950837973638676281, 14.31366178983253512, 2.591948120961855118 ) ) ;
#15813=EDGE_CURVE ( 'NONE', #12599, #18854, #9181, .T. ) ;
#15815=CARTESIAN_POINT ( 'NONE',  ( 2.705023505549862151, -4.909285963183986468, -12.36217802824811152 ) ) ;
#15822=B_SPLINE_CURVE_WITH_KNOTS ( 'NONE', 3,
 ( #15730, #13223, #11698, #4078, #4540, #138 ),
 .UNSPECIFIED., .F., .F.,
 ( 4, 2, 4 ),
 ( 2.185279341460844539E-18, 0.0002017457492448067953, 0.0004034914984896113680 ),
 .UNSPECIFIED. ) ;
#15823=B_SPLINE_CURVE_WITH_KNOTS ( 'NONE', 3,
 ( #6427, #6334, #1739, #16644 ),
 .UNSPECIFIED., .F., .F.,
 ( 4, 4 ),
 ( 1.582786644015060892E-17, 0.003005512676784847896 ),
 .UNSPECIFIED. ) ;
#15825=ORIENTED_EDGE ( 'NONE', *, *, #9482, .T. ) ;
#15826=VERTEX_POINT ( 'NONE', #13766 ) ;
#15833=CARTESIAN_POINT ( 'NONE',  ( 16.57778382496167424, -0.01482878558584693925, 0.001819584982831843212 ) ) ;
#15835=CARTESIAN_POINT ( 'NONE',  ( 16.56872352241294521, -0.009382111268607402216, -0.004564908236399935551 ) ) ;
#15837=EDGE_CURVE ( 'NONE', #13196, #12599, #7333, .T. ) ;
#15843=EDGE_LOOP ( 'NONE', ( #2792, #17556, #4728, #17843 ) ) ;
#15845=CARTESIAN_POINT ( 'NONE',  ( 16.56679352167444819, 0.009170718284672562878, -0.001518074900131760043 ) ) ;
#15849=VECTOR ( 'NONE', #10389, 1000.000000000000000 ) ;
#15851=VECTOR ( 'NONE', #10219, 1000.000000000000000 ) ;
#15853=ORIENTED_EDGE ( 'NONE', *, *, #7391, .F. ) ;
#15856=CARTESIAN_POINT ( 'NONE',  ( 16.57778382496167424, 0.006312874906843865194, 0.01354073047775895648 ) ) ;
#15860=CARTESIAN_POINT ( 'NONE',  ( 2.002547531651519996, -10.57595306287287329, -6.845637710436306200 ) ) ;
#15863=CARTESIAN_POINT ( 'NONE',  ( 16.56872352241294521, -0.004564908236400289435, -0.009382111268606239951 ) ) ;
#15864=CARTESIAN_POINT ( 'NONE',  ( 0.3307726912345235748, -3.680742887039399669, 13.25328329128664606 ) ) ;
#15875=CARTESIAN_POINT ( 'NONE',  ( 1.977228804422746400, -6.152949558601968683, -14.12033626431101041 ) ) ;
#15876=( BOUNDED_SURFACE ( )  B_SPLINE_SURFACE ( 3, 1, ( 
 ( #4206, #7169 ),
 ( #18814, #10317 ),
 ( #11655, #5710 ),
 ( #5808, #11561 ) ),
 .UNSPECIFIED., .F., .F., .T. ) 
 B_SPLINE_SURFACE_WITH_KNOTS ( ( 4, 4 ),
 ( 2, 2 ),
 ( 0.000000000000000000, 1.000000000000000000 ),
 ( 0.000000000000000000, 1.000000000000000000 ),
 .UNSPECIFIED. ) 
 GEOMETRIC_REPRESENTATION_ITEM ( )  RATIONAL_B_SPLINE_SURFACE ( (
 ( 1.000000000000000000, 1.000000000000000000),
 ( 0.9593108457356467333, 0.9995965569486454649),
 ( 0.9593108457356467333, 0.9995965569486454649),
 ( 1.000000000000000000, 1.000000000000000000) ) ) 
 REPRESENTATION_ITEM ( '' )  SURFACE ( )  );
#15877=ORIENTED_EDGE ( 'NONE', *, *, #1998, .T. ) ;
#15881=CARTESIAN_POINT ( 'NONE',  ( 0.3151928476913565258, -0.0002082997482820912163, -13.73922860838471927 ) ) ;
#15892=VERTEX_POINT ( 'NONE', #16552 ) ;
#15897=EDGE_CURVE ( 'NONE', #17303, #9110, #6660, .T. ) ;
#15899=ORIENTED_EDGE ( 'NONE', *, *, #3443, .F. ) ;
#15904=EDGE_LOOP ( 'NONE', ( #9331, #12380, #4229, #16416 ) ) ;
#15906=CARTESIAN_POINT ( 'NONE',  ( 0.4862570985993235340, 5.003653737315670647, -12.97920246947874112 ) ) ;
#15913=CARTESIAN_POINT ( 'NONE',  ( 2.123976203522053741, -10.37815841598482969, -11.67822624909937090 ) ) ;
#15914=DIRECTION ( 'NONE',  ( -1.000000000000000000, -0.000000000000000000, -0.000000000000000000 ) ) ;
#15915=ORIENTED_EDGE ( 'NONE', *, *, #2524, .F. ) ;
#15917=VERTEX_POINT ( 'NONE', #10913 ) ;
#15920=CARTESIAN_POINT ( 'NONE',  ( 1.847247051441591070, 4.004229874809190903, -11.78111530882019053 ) ) ;
#15924=ORIENTED_EDGE ( 'NONE', *, *, #17742, .T. ) ;
#15928=CARTESIAN_POINT ( 'NONE',  ( 16.56782317627811096, -0.006045301465876417625, 0.007739510688079494216 ) ) ;
#15929=CARTESIAN_POINT ( 'NONE',  ( 16.56782317627811096, -0.007739510688079557534, -0.006045301465876337828 ) ) ;
#15942=CARTESIAN_POINT ( 'NONE',  ( 0.4862570985993235340, -13.44146924561378498, -3.580942890621813923 ) ) ;
#15945=CARTESIAN_POINT ( 'NONE',  ( 2.636624412715138366, -11.10302021257964888, 11.60464335004044223 ) ) ;
#15946=CARTESIAN_POINT ( 'NONE',  ( 8.438534575730034959, -2.341351102130323714, 6.454982381540280478 ) ) ;
#15951=CARTESIAN_POINT ( 'NONE',  ( 0.3151928476913592458, -13.73922860838471749, 0.0002082997483299325046 ) ) ;
#15952=CARTESIAN_POINT ( 'NONE',  ( 16.56679352167444819, -0.004162264567719712108, -0.008311568981097318051 ) ) ;
#15955=CARTESIAN_POINT ( 'NONE',  ( 3.664313757352976264, 1.627055439596472475, -14.16986885736090329 ) ) ;
#15957=CARTESIAN_POINT ( 'NONE',  ( 16.56753206892534891, 0.001549402974394159613, 0.009369540855502535986 ) ) ;
#15962=LINE ( 'NONE', #9, #17923 ) ;
#15965=ORIENTED_EDGE ( 'NONE', *, *, #10810, .F. ) ;
#15966=CARTESIAN_POINT ( 'NONE',  ( 0.3151926232592475174, 4.172630140040981317, -13.09050869763088443 ) ) ;
#15975=ADVANCED_FACE ( 'NONE', ( #15648 ), #4437, .F. ) ;
#15978=ADVANCED_FACE ( 'NONE', ( #18529 ), #3571, .T. ) ;
#15988=VECTOR ( 'NONE', #6118, 1000.000000000000114 ) ;
#15993=DIRECTION ( 'NONE',  ( -1.000000000000000000, -0.000000000000000000, -0.000000000000000000 ) ) ;
#15994=CARTESIAN_POINT ( 'NONE',  ( 1.847412631396500249, -10.04119192206681177, -7.348689888531952263 ) ) ;
#15998=EDGE_CURVE ( 'NONE', #5926, #18142, #12798, .T. ) ;
#16001=CARTESIAN_POINT ( 'NONE',  ( 0.4862570985993235340, -10.79774104611366781, -8.769551628660854803 ) ) ;
#16005=EDGE_LOOP ( 'NONE', ( #325, #16520, #7604, #11162 ) ) ;
#16007=ORIENTED_EDGE ( 'NONE', *, *, #7216, .T. ) ;
#16009=VERTEX_POINT ( 'NONE', #15563 ) ;
#16010=ORIENTED_EDGE ( 'NONE', *, *, #404, .F. ) ;
#16011=B_SPLINE_CURVE_WITH_KNOTS ( 'NONE', 3,
 ( #124, #6150, #3063, #17422 ),
 .UNSPECIFIED., .F., .F.,
 ( 4, 4 ),
 ( 0.000000000000000000, 0.002004993803842607548 ),
 .UNSPECIFIED. ) ;
#16020=CARTESIAN_POINT ( 'NONE',  ( 0.4754618798421167414, -0.7484603771385368587, 13.89949764182682301 ) ) ;
#16021=LINE ( 'NONE', #4565, #1197 ) ;
#16027=CARTESIAN_POINT ( 'NONE',  ( 1.977436885026095270, -6.153171729168663617, 14.12046670317548980 ) ) ;
#16028=ADVANCED_FACE ( 'NONE', ( #14128 ), #6410, .F. ) ;
#16030=ADVANCED_FACE ( 'NONE', ( #18613 ), #8352, .F. ) ;
#16032=ORIENTED_EDGE ( 'NONE', *, *, #5861, .F. ) ;
#16036=VERTEX_POINT ( 'NONE', #9919 ) ;
#16041=CARTESIAN_POINT ( 'NONE',  ( 1.847034903785822246, 11.76058231742745797, 4.063013886994747637 ) ) ;
#16042=CARTESIAN_POINT ( 'NONE',  ( 2.123976203522053297, 15.26039569100264082, -3.347755036805743600 ) ) ;
#16044=VERTEX_POINT ( 'NONE', #9040 ) ;
#16048=CARTESIAN_POINT ( 'NONE',  ( 16.56872352241294521, 0.007512283835804314455, -0.007240717549633915451 ) ) ;
#16050=CIRCLE ( 'NONE', #2863, 14.54644660717763927 ) ;
#16055=VERTEX_POINT ( 'NONE', #1781 ) ;
#16057=CARTESIAN_POINT ( 'NONE',  ( 2.002547531651519996, -9.778737580845755062, 7.942910686618138705 ) ) ;
#16060=CARTESIAN_POINT ( 'NONE',  ( 0.3095370825347233956, 3.806662003783596759, -13.20347358821910433 ) ) ;
#16061=AXIS2_PLACEMENT_3D ( 'NONE', #17528, #4436, #4060 ) ;
#16062=CARTESIAN_POINT ( 'NONE',  ( 2.636624412714236865, 0.000000000000000000, 0.000000000000000000 ) ) ;
#16064=CARTESIAN_POINT ( 'NONE',  ( 3.950837973638676281, -12.81214529934979929, 6.888253895133251703 ) ) ;
#16067=EDGE_LOOP ( 'NONE', ( #16010, #15802, #2741, #2775 ) ) ;
#16072=DIRECTION ( 'NONE',  ( 0.7561779333270775005, -0.1688126975276555974, -0.6322161072786950387 ) ) ;
#16073=FACE_OUTER_BOUND ( 'NONE', #7262, .T. ) ;
#16078=ADVANCED_FACE ( 'NONE', ( #10377 ), #817, .T. ) ;
#16085=DIRECTION ( 'NONE',  ( 1.000000000000000000, 0.000000000000000000, 0.000000000000000000 ) ) ;
#16087=CARTESIAN_POINT ( 'NONE',  ( 1.845755665166723736, -12.43231320373360482, -0.4784952423729852966 ) ) ;
#16100=ADVANCED_FACE ( 'NONE', ( #444 ), #10304, .F. ) ;
#16101=CARTESIAN_POINT ( 'NONE',  ( 0.4754618798421162973, 5.007009103465249744, 12.98792082933646341 ) ) ;
#16102=CARTESIAN_POINT ( 'NONE',  ( 16.57778382496167424, 0.01354073047775893567, -0.006312874906843913766 ) ) ;
#16107=CARTESIAN_POINT ( 'NONE',  ( 16.56872352241294521, -0.009207754980063714498, -0.004907101719994726684 ) ) ;
#16108=FACE_OUTER_BOUND ( 'NONE', #3448, .T. ) ;
#16109=CARTESIAN_POINT ( 'NONE',  ( 0.3132642857406499615, -3.740125687984641178, -13.21852905223342667 ) ) ;
#16110=CARTESIAN_POINT ( 'NONE',  ( 3.377929128793395908, -3.070552481924963217, 13.64476897106782971 ) ) ;
#16119=VERTEX_POINT ( 'NONE', #7717 ) ;
#16128=CARTESIAN_POINT ( 'NONE',  ( 3.512766787570899663, 10.87507422923878586, 10.40533104696127076 ) ) ;
#16137=ORIENTED_EDGE ( 'NONE', *, *, #8189, .T. ) ;
#16139=EDGE_CURVE ( 'NONE', #5819, #12351, #16311, .T. ) ;
#16141=EDGE_CURVE ( 'NONE', #5568, #9336, #7815, .T. ) ;
#16148=CARTESIAN_POINT ( 'NONE',  ( 3.353306896162455697, 7.069984850384810393, 12.02594772223098651 ) ) ;
#16151=CARTESIAN_POINT ( 'NONE',  ( 0.8740779401512879243, 13.31469722824398794, -5.211551231203936929 ) ) ;
#16155=AXIS2_PLACEMENT_3D ( 'NONE', #3203, #3307, #9052 ) ;
#16161=CARTESIAN_POINT ( 'NONE',  ( 0.3058872367615226295, 11.46514199369368825, -7.578326039752480092 ) ) ;
#16162=( BOUNDED_SURFACE ( )  B_SPLINE_SURFACE ( 3, 1, ( 
 ( #11544, #9053 ),
 ( #15928, #17363 ),
 ( #2817, #1595 ),
 ( #11921, #14882 ) ),
 .UNSPECIFIED., .F., .F., .T. ) 
 B_SPLINE_SURFACE_WITH_KNOTS ( ( 4, 4 ),
 ( 2, 2 ),
 ( 0.000000000000000000, 1.000000000000000000 ),
 ( 0.000000000000000000, 1.000000000000000000 ),
 .UNSPECIFIED. ) 
 GEOMETRIC_REPRESENTATION_ITEM ( )  RATIONAL_B_SPLINE_SURFACE ( (
 ( 1.000000000000000000, 1.000000000000000000),
 ( 0.9933953342250436691, 0.8357391271907733676),
 ( 0.9933953342250436691, 0.8357391271907733676),
 ( 1.000000000000000000, 1.000000000000000000) ) ) 
 REPRESENTATION_ITEM ( '' )  SURFACE ( )  );
#16170=EDGE_CURVE ( 'NONE', #9139, #8437, #9330, .T. ) ;
#16171=DIRECTION ( 'NONE',  ( 0.000000000000000000, 0.000000000000000000, 1.000000000000000000 ) ) ;
#16173=ADVANCED_FACE ( 'NONE', ( #9510 ), #14204, .F. ) ;
#16175=ADVANCED_FACE ( 'NONE', ( #3591 ), #1141, .F. ) ;
#16178=CARTESIAN_POINT ( 'NONE',  ( 0.3095370825347233956, -0.4597470195089253808, -13.73357284481725316 ) ) ;
#16180=CARTESIAN_POINT ( 'NONE',  ( 0.3308579732647042304, 7.595989242675130093, 11.46737410776356469 ) ) ;
#16183=DIRECTION ( 'NONE',  ( -1.000000000000000000, -0.000000000000000000, -0.000000000000000000 ) ) ;
#16185=ORIENTED_EDGE ( 'NONE', *, *, #10097, .T. ) ;
#16186=CARTESIAN_POINT ( 'NONE',  ( 0.4862570985993235340, -5.003653737315397976, -12.97920246947884770 ) ) ;
#16188=ORIENTED_EDGE ( 'NONE', *, *, #17188, .F. ) ;
#16195=CARTESIAN_POINT ( 'NONE',  ( 0.3095370825347233956, -13.73357284481725138, 0.4597470195089733425 ) ) ;
#16197=CARTESIAN_POINT ( 'NONE',  ( 0.4754618798421167414, -7.564402563418384240, -11.68486377711974811 ) ) ;
#16198=CARTESIAN_POINT ( 'NONE',  ( 16.56753206892534891, -0.009369540855502119653, -0.001549402974393242162 ) ) ;
#16199=( BOUNDED_SURFACE ( )  B_SPLINE_SURFACE ( 3, 1, ( 
 ( #1692, #17462 ),
 ( #1794, #7636 ),
 ( #13446, #6186 ),
 ( #16222, #359 ) ),
 .UNSPECIFIED., .F., .F., .T. ) 
 B_SPLINE_SURFACE_WITH_KNOTS ( ( 4, 4 ),
 ( 2, 2 ),
 ( 0.000000000000000000, 1.000000000000000000 ),
 ( 0.000000000000000000, 1.000000000000000000 ),
 .UNSPECIFIED. ) 
 GEOMETRIC_REPRESENTATION_ITEM ( )  RATIONAL_B_SPLINE_SURFACE ( (
 ( 1.000000000000000000, 1.000000000000000000),
 ( 0.9933953342250436691, 0.8357391271907733676),
 ( 0.9933953342250436691, 0.8357391271907733676),
 ( 1.000000000000000000, 1.000000000000000000) ) ) 
 REPRESENTATION_ITEM ( '' )  SURFACE ( )  );
#16202=CARTESIAN_POINT ( 'NONE',  ( 0.3137051932979792457, 4.679953077377485116, 12.91601973349272114 ) ) ;
#16204=CARTESIAN_POINT ( 'NONE',  ( 2.002547531651519996, -7.942910686618100513, -9.778737580845787036 ) ) ;
#16207=DIRECTION ( 'NONE',  ( -0.7635533937278214944, 0.2197766120036462600, 0.6071939193889586139 ) ) ;
#16208=CARTESIAN_POINT ( 'NONE',  ( 16.58200780006414732, -0.0006320991582339893951, -0.01115192838421470191 ) ) ;
#16209=B_SPLINE_CURVE_WITH_KNOTS ( 'NONE', 3,
 ( #9478, #9389, #13777, #15216, #689, #3735 ),
 .UNSPECIFIED., .F., .F.,
 ( 4, 2, 4 ),
 ( 0.000000000000000000, 0.0001828790815886945087, 0.0003657581631773890174 ),
 .UNSPECIFIED. ) ;
#16212=EDGE_LOOP ( 'NONE', ( #12657, #17844, #13047, #11909 ) ) ;
#16214=VERTEX_POINT ( 'NONE', #12746 ) ;
#16222=CARTESIAN_POINT ( 'NONE',  ( 16.56872352241294521, 0.007512283835805451566, 0.007240717549634016065 ) ) ;
#16224=CARTESIAN_POINT ( 'NONE',  ( 0.3720661004400040439, -4.951033743989553315, -12.89739157014198057 ) ) ;
#16226=ADVANCED_FACE ( 'NONE', ( #7214 ), #10221, .F. ) ;
#16239=ORIENTED_EDGE ( 'NONE', *, *, #8715, .F. ) ;
#16240=CARTESIAN_POINT ( 'NONE',  ( 0.4862570985993235340, 8.769551628660890330, -10.79774104611363761 ) ) ;
#16242=CARTESIAN_POINT ( 'NONE',  ( 2.353870697619111940, 10.00946331859664085, 8.216087327472971324 ) ) ;
#16245=EDGE_LOOP ( 'NONE', ( #4722, #9492, #14712, #18709, #7425, #18682, #8110, #3800, #11093, #12541, #5090, #11029, #5188, #5681, #7523, #9821, #7365, #4010, #7011, #17036, #5979, #6220, #445, #2250, #14964, #13904, #5831, #15339, #14871, #16312, #15523, #15194, #12207, #15160, #6871, #13456, #9549, #7064, #4382, #3350, #9918, #17746, #11648, #2898, #10621, #15457, #4520, #4182, #18738, #6874, #2896, #2578, #15627, #4578, #8254, #3772, #14332, #15541, #3731, #9309, #1298, #18730, #2166, #3416 ) ) ;
#16254=CARTESIAN_POINT ( 'NONE',  ( 0.3095370825347224519, -7.700448427571790155, -11.38092634279636961 ) ) ;
#16256=ADVANCED_FACE ( 'NONE', ( #1271 ), #3241, .F. ) ;
#16257=VERTEX_POINT ( 'NONE', #15519 ) ;
#16258=AXIS2_PLACEMENT_3D ( 'NONE', #15233, #18285, #4917 ) ;
#16259=CARTESIAN_POINT ( 'NONE',  ( 3.377929128793397684, -10.50432311212909475, 9.234024516648283054 ) ) ;
#16273=CARTESIAN_POINT ( 'NONE',  ( 16.57210152137263393, -0.008007331252332796495, -0.01214401161737526519 ) ) ;
#16278=CARTESIAN_POINT ( 'NONE',  ( 3.074695600507405757, 7.366518011945858646, 13.70113613813188458 ) ) ;
#16279=ADVANCED_FACE ( 'NONE', ( #8272 ), #5680, .F. ) ;
#16280=( BOUNDED_SURFACE ( )  B_SPLINE_SURFACE ( 3, 1, ( 
 ( #10085, #11253 ),
 ( #2620, #8649 ),
 ( #1008, #8558 ),
 ( #18403, #8469 ) ),
 .UNSPECIFIED., .F., .F., .T. ) 
 B_SPLINE_SURFACE_WITH_KNOTS ( ( 4, 4 ),
 ( 2, 2 ),
 ( 0.000000000000000000, 1.000000000000000000 ),
 ( 0.000000000000000000, 1.000000000000000000 ),
 .UNSPECIFIED. ) 
 GEOMETRIC_REPRESENTATION_ITEM ( )  RATIONAL_B_SPLINE_SURFACE ( (
 ( 1.000000000000000000, 1.000000000000000000),
 ( 0.7792777138730158093, 0.9689936506012928330),
 ( 0.7792777138730158093, 0.9689936506012928330),
 ( 1.000000000000000000, 1.000000000000000000) ) ) 
 REPRESENTATION_ITEM ( '' )  SURFACE ( )  );
#16284=VERTEX_POINT ( 'NONE', #3066 ) ;
#16290=ORIENTED_EDGE ( 'NONE', *, *, #4349, .T. ) ;
#16291=CARTESIAN_POINT ( 'NONE',  ( 1.342453679581834924, 11.38190519890853558, 9.456403821038842139 ) ) ;
#16296=CARTESIAN_POINT ( 'NONE',  ( 2.002547531651519996, 6.845637710436341727, -10.57595306287284842 ) ) ;
#16298=CARTESIAN_POINT ( 'NONE',  ( 1.977228804421385933, 15.33060379559031539, -1.488378900181928532 ) ) ;
#16301=CARTESIAN_POINT ( 'NONE',  ( 16.56782317627811096, 0.009228812961908652857, -0.003357783021327854014 ) ) ;
#16304=CARTESIAN_POINT ( 'NONE',  ( 2.002547531651519996, 4.532360870844327039, 11.75462648437103752 ) ) ;
#16305=CARTESIAN_POINT ( 'NONE',  ( 16.56679352167444819, 0.006526964904752344775, -0.006618561353600113835 ) ) ;
#16311=LINE ( 'NONE', #3490, #5673 ) ;
#16312=ORIENTED_EDGE ( 'NONE', *, *, #12285, .F. ) ;
#16318=( BOUNDED_SURFACE ( )  B_SPLINE_SURFACE ( 3, 1, ( 
 ( #14498, #11359 ),
 ( #15929, #5693 ),
 ( #14314, #5888 ),
 ( #15835, #17464 ) ),
 .UNSPECIFIED., .F., .F., .T. ) 
 B_SPLINE_SURFACE_WITH_KNOTS ( ( 4, 4 ),
 ( 2, 2 ),
 ( 0.000000000000000000, 1.000000000000000000 ),
 ( 0.000000000000000000, 1.000000000000000000 ),
 .UNSPECIFIED. ) 
 GEOMETRIC_REPRESENTATION_ITEM ( )  RATIONAL_B_SPLINE_SURFACE ( (
 ( 1.000000000000000000, 1.000000000000000000),
 ( 0.9933953342250436691, 0.8357391271907733676),
 ( 0.9933953342250436691, 0.8357391271907733676),
 ( 1.000000000000000000, 1.000000000000000000) ) ) 
 REPRESENTATION_ITEM ( '' )  SURFACE ( )  );
#16319=CARTESIAN_POINT ( 'NONE',  ( 1.847412631396504468, -12.44294644888238821, -0.04315047898448168967 ) ) ;
#16320=ORIENTED_EDGE ( 'NONE', *, *, #4987, .T. ) ;
#16321=CARTESIAN_POINT ( 'NONE',  ( 0.3137051932979792457, -10.83767969834809008, 8.442169467526815296 ) ) ;
#16322=CARTESIAN_POINT ( 'NONE',  ( 2.002547531651519996, 9.778737580845815458, -7.942910686618064986 ) ) ;
#16326=CARTESIAN_POINT ( 'NONE',  ( 1.847168016377980670, 12.44137401948661470, -0.1868244120189998803 ) ) ;
#16328=CARTESIAN_POINT ( 'NONE',  ( 1.847421816787903071, 0.02876707915197697710, -12.44300551404155364 ) ) ;
#16334=EDGE_LOOP ( 'NONE', ( #17594, #3681, #18861, #15965 ) ) ;
#16337=VERTEX_POINT ( 'NONE', #1559 ) ;
#16342=CARTESIAN_POINT ( 'NONE',  ( 3.353306896162453477, -10.44017738170049903, -9.252610477110389198 ) ) ;
#16344=CARTESIAN_POINT ( 'NONE',  ( 16.58200780006414732, 0.002844973367391037070, 0.01080144354108989249 ) ) ;
#16345=DIRECTION ( 'NONE',  ( 0.7561779333270775005, -0.2350349629540270657, 0.6106991889125030770 ) ) ;
#16349=CARTESIAN_POINT ( 'NONE',  ( 2.747332970342022840, 2.409922051470680060, 16.17136872824899285 ) ) ;
#16357=CARTESIAN_POINT ( 'NONE',  ( 0.4862570985993235340, 8.769551628660735787, 10.79774104611376373 ) ) ;
#16361=B_SPLINE_CURVE_WITH_KNOTS ( 'NONE', 3,
 ( #7826, #12115, #15067, #6185 ),
 .UNSPECIFIED., .F., .F.,
 ( 4, 4 ),
 ( 0.000000000000000000, 0.002004993803842800969 ),
 .UNSPECIFIED. ) ;
#16362=ORIENTED_EDGE ( 'NONE', *, *, #6620, .T. ) ;
#16370=ADVANCED_FACE ( 'NONE', ( #16384 ), #13013, .T. ) ;
#16375=CARTESIAN_POINT ( 'NONE',  ( 0.4862570985993235340, -10.79774104611366781, -8.769551628660854803 ) ) ;
#16384=FACE_OUTER_BOUND ( 'NONE', #3094, .T. ) ;
#16386=ORIENTED_EDGE ( 'NONE', *, *, #9263, .F. ) ;
#16389=CARTESIAN_POINT ( 'NONE',  ( 1.845755665166726844, 3.386720041070728104, 11.97169564665392727 ) ) ;
#16393=AXIS2_PLACEMENT_3D ( 'NONE', #2423, #6927, #7110 ) ;
#16399=B_SPLINE_CURVE_WITH_KNOTS ( 'NONE', 3,
 ( #7782, #7973, #18184, #2136, #13595, #18091 ),
 .UNSPECIFIED., .F., .F.,
 ( 4, 2, 4 ),
 ( 0.000000000000000000, 0.0001828790815886950779, 0.0003657581631773901558 ),
 .UNSPECIFIED. ) ;
#16400=CIRCLE ( 'NONE', #14855, 14.54644660717763927 ) ;
#16401=CARTESIAN_POINT ( 'NONE',  ( 0.3132642857406554571, 12.89240536501346313, 4.743831191224429311 ) ) ;
#16402=CARTESIAN_POINT ( 'NONE',  ( 0.3058872367615226295, -3.664492643742672584, -13.24582953854928569 ) ) ;
#16403=( BOUNDED_SURFACE ( )  B_SPLINE_SURFACE ( 3, 1, ( 
 ( #5995, #11639 ),
 ( #7642, #7350 ),
 ( #10199, #11833 ),
 ( #8957, #4373 ) ),
 .UNSPECIFIED., .F., .F., .T. ) 
 B_SPLINE_SURFACE_WITH_KNOTS ( ( 4, 4 ),
 ( 2, 2 ),
 ( 0.000000000000000000, 1.000000000000000000 ),
 ( 0.000000000000000000, 1.000000000000000000 ),
 .UNSPECIFIED. ) 
 GEOMETRIC_REPRESENTATION_ITEM ( )  RATIONAL_B_SPLINE_SURFACE ( (
 ( 1.000000000000000000, 1.000000000000000000),
 ( 0.9933953342250438912, 0.8357391271907739227),
 ( 0.9933953342250438912, 0.8357391271907739227),
 ( 1.000000000000000000, 1.000000000000000000) ) ) 
 REPRESENTATION_ITEM ( '' )  SURFACE ( )  );
#16405=CARTESIAN_POINT ( 'NONE',  ( 0.3137051932979757485, 8.442169467526850823, 10.83767969834806166 ) ) ;
#16406=CARTESIAN_POINT ( 'NONE',  ( 0.4862570985993235340, -11.67702470553370553, 7.559321496869385371 ) ) ;
#16407=CIRCLE ( 'NONE', #524, 16.06066017081991149 ) ;
#16408=DIRECTION ( 'NONE',  ( 0.000000000000000000, 0.000000000000000000, -1.000000000000000000 ) ) ;
#16410=CARTESIAN_POINT ( 'NONE',  ( 0.3939822652208094800, -7.545099438011941828, -11.57634296752776137 ) ) ;
#16415=ORIENTED_EDGE ( 'NONE', *, *, #747, .F. ) ;
#16416=ORIENTED_EDGE ( 'NONE', *, *, #8668, .F. ) ;
#16419=CARTESIAN_POINT ( 'NONE',  ( 0.3151926232592474064, 0.07678256780557664307, 13.73922722301401578 ) ) ;
#16420=CARTESIAN_POINT ( 'NONE',  ( 0.3137051932979809665, 10.83767969834803324, 8.442169467526891680 ) ) ;
#16425=FACE_OUTER_BOUND ( 'NONE', #4055, .T. ) ;
#16426=LINE ( 'NONE', #18128, #7989 ) ;
#16432=CARTESIAN_POINT ( 'NONE',  ( 0.3137051932979757485, -8.442169467526770887, -10.83767969834812561 ) ) ;
#16435=ORIENTED_EDGE ( 'NONE', *, *, #1715, .T. ) ;
#16439=CARTESIAN_POINT ( 'NONE',  ( 2.002547531651519996, -9.778737580845639599, -7.942910686618280813 ) ) ;
#16440=B_SPLINE_CURVE_WITH_KNOTS ( 'NONE', 3,
 ( #2793, #7318, #1482, #8550, #18768, #18579 ),
 .UNSPECIFIED., .F., .F.,
 ( 4, 2, 4 ),
 ( 8.131516293641283255E-19, 0.001657017934709845109, 0.003314035869419688484 ),
 .UNSPECIFIED. ) ;
#16448=CARTESIAN_POINT ( 'NONE',  ( 0.3095370825347234511, -7.700448427571787491, -11.38092634279637139 ) ) ;
#16449=EDGE_CURVE ( 'NONE', #137, #11551, #2526, .T. ) ;
#16451=CARTESIAN_POINT ( 'NONE',  ( 2.123976203522053741, -3.347755036806012274, 15.26039569100259108 ) ) ;
#16453=CARTESIAN_POINT ( 'NONE',  ( 0.8740779401508622648, 0.8420120399581700887, 14.27348745891572968 ) ) ;
#16454=CARTESIAN_POINT ( 'NONE',  ( 2.636624412715093513, -14.14563173255330142, 7.605649742761597665 ) ) ;
#16459=DIRECTION ( 'NONE',  ( -0.7635533937278214944, 0.6071939193889607234, -0.2197766120036399873 ) ) ;
#16460=EDGE_CURVE ( 'NONE', #4964, #10109, #16902, .T. ) ;
#16461=CARTESIAN_POINT ( 'NONE',  ( 3.950837973638675393, 10.51028938476217967, 10.05648675950130233 ) ) ;
#16470=ORIENTED_EDGE ( 'NONE', *, *, #13673, .F. ) ;
#16476=B_SPLINE_CURVE_WITH_KNOTS ( 'NONE', 3,
 ( #18325, #1109, #2630, #11348, #15360, #3796 ),
 .UNSPECIFIED., .F., .F.,
 ( 4, 2, 4 ),
 ( 1.939479807224432123E-18, 0.001500839035891553524, 0.003001678071783104879 ),
 .UNSPECIFIED. ) ;
#16477=CARTESIAN_POINT ( 'NONE',  ( 0.4754618798421162973, 0.7484603771384427118, 13.89949764182683012 ) ) ;
#16479=ORIENTED_EDGE ( 'NONE', *, *, #8264, .T. ) ;
#16484=CARTESIAN_POINT ( 'NONE',  ( 0.3145734862173252822, -8.321353293018908914, 10.93207848441430130 ) ) ;
#16485=DIRECTION ( 'NONE',  ( -0.7635533937278216055, 0.1790966170214010056, -0.6204116510013458763 ) ) ;
#16487=ORIENTED_EDGE ( 'NONE', *, *, #6275, .T. ) ;
#16489=CONICAL_SURFACE ( 'NONE', #17375, 14.54644660717763927, 0.8559913436420816257 ) ;
#16490=VERTEX_POINT ( 'NONE', #10940 ) ;
#16493=CARTESIAN_POINT ( 'NONE',  ( 0.3142014840576534684, 3.879477880151442015, 13.17932813834296013 ) ) ;
#16497=CARTESIAN_POINT ( 'NONE',  ( 0.4754618798421171855, -5.007009103465158262, -12.98792082933649716 ) ) ;
#16498=CARTESIAN_POINT ( 'NONE',  ( 2.353870697619110164, -3.268530966681543859, -12.53036919722787879 ) ) ;
#16501=EDGE_CURVE ( 'NONE', #3664, #14019, #10057, .T. ) ;
#16507=ORIENTED_EDGE ( 'NONE', *, *, #3184, .F. ) ;
#16508=ORIENTED_EDGE ( 'NONE', *, *, #9354, .F. ) ;
#16509=EDGE_LOOP ( 'NONE', ( #1585, #11344, #1911, #15752 ) ) ;
#16513=B_SPLINE_CURVE_WITH_KNOTS ( 'NONE', 3,
 ( #2072, #3487, #18207, #18025, #13898, #17938 ),
 .UNSPECIFIED., .F., .F.,
 ( 4, 2, 4 ),
 ( 0.000000000000000000, 0.001656992708822831520, 0.003313985417645663040 ),
 .UNSPECIFIED. ) ;
#16514=CARTESIAN_POINT ( 'NONE',  ( 2.002547531651519996, -10.57595306287287329, -6.845637710436306200 ) ) ;
#16515=EDGE_CURVE ( 'NONE', #17332, #913, #18006, .T. ) ;
#16516=( BOUNDED_SURFACE ( )  B_SPLINE_SURFACE ( 3, 1, ( 
 ( #17776, #4490 ),
 ( #3027, #13557 ),
 ( #185, #6014 ),
 ( #16344, #1709 ) ),
 .UNSPECIFIED., .F., .F., .T. ) 
 B_SPLINE_SURFACE_WITH_KNOTS ( ( 4, 4 ),
 ( 2, 2 ),
 ( 0.000000000000000000, 1.000000000000000000 ),
 ( 0.000000000000000000, 1.000000000000000000 ),
 .UNSPECIFIED. ) 
 GEOMETRIC_REPRESENTATION_ITEM ( )  RATIONAL_B_SPLINE_SURFACE ( (
 ( 1.000000000000000000, 1.000000000000000000),
 ( 0.7792777138730160313, 0.9689936506012927220),
 ( 0.7792777138730160313, 0.9689936506012927220),
 ( 1.000000000000000000, 1.000000000000000000) ) ) 
 REPRESENTATION_ITEM ( '' )  SURFACE ( )  );
#16520=ORIENTED_EDGE ( 'NONE', *, *, #4185, .F. ) ;
#16522=DIRECTION ( 'NONE',  ( -1.000000000000000000, -0.000000000000000000, -0.000000000000000000 ) ) ;
#16526=CARTESIAN_POINT ( 'NONE',  ( 0.3095370825347224519, -0.4597470195091133416, 13.73357284481724605 ) ) ;
#16527=B_SPLINE_CURVE_WITH_KNOTS ( 'NONE', 3,
 ( #16919, #16828, #12608, #11198, #5353, #11290 ),
 .UNSPECIFIED., .F., .F.,
 ( 4, 2, 4 ),
 ( 0.000000000000000000, 0.001656992708824547161, 0.003313985417649093455 ),
 .UNSPECIFIED. ) ;
#16535=CARTESIAN_POINT ( 'NONE',  ( 2.002547531651519996, -6.845637710436110801, -10.57595306287299763 ) ) ;
#16539=DIRECTION ( 'NONE',  ( 0.000000000000000000, 0.000000000000000000, 1.000000000000000000 ) ) ;
#16540=ORIENTED_EDGE ( 'NONE', *, *, #3580, .T. ) ;
#16541=CARTESIAN_POINT ( 'NONE',  ( 0.3137051932979775248, 3.805684345189972895, -13.20008686438101719 ) ) ;
#16543=CARTESIAN_POINT ( 'NONE',  ( 0.3058872367615226295, -7.578326039752520060, -11.46514199369366516 ) ) ;
#16546=CARTESIAN_POINT ( 'NONE',  ( 1.254009781011571567, 1.011465182608068503, 14.64464726212582590 ) ) ;
#16548=CARTESIAN_POINT ( 'NONE',  ( 0.3150686449036065317, 13.01866258978842694, -4.391272911157185099 ) ) ;
#16552=CARTESIAN_POINT ( 'NONE',  ( 0.4862570985993235340, -3.580942890621579444, -13.44146924561384537 ) ) ;
#16553=CARTESIAN_POINT ( 'NONE',  ( 0.3137051932979757485, -8.442169467526770887, -10.83767969834812561 ) ) ;
#16561=CARTESIAN_POINT ( 'NONE',  ( 16.56753206892534891, -0.006669401563384969034, 0.006760771273036147132 ) ) ;
#16564=EDGE_CURVE ( 'NONE', #10137, #2339, #14169, .T. ) ;
#16569=ORIENTED_EDGE ( 'NONE', *, *, #13199, .F. ) ;
#16575=ORIENTED_EDGE ( 'NONE', *, *, #2248, .F. ) ;
#16580=CARTESIAN_POINT ( 'NONE',  ( 16.56872352241294521, -0.004564908236400289435, -0.009382111268606239951 ) ) ;
#16581=EDGE_CURVE ( 'NONE', #9201, #2481, #18734, .T. ) ;
#16587=EDGE_CURVE ( 'NONE', #1103, #306, #9826, .T. ) ;
#16590=CARTESIAN_POINT ( 'NONE',  ( 16.56753206892534891, -0.001549402974394229436, -0.009369540855502527313 ) ) ;
#16591=CARTESIAN_POINT ( 'NONE',  ( 1.846138399168762101, -11.69739621335925328, 4.238866729160359448 ) ) ;
#16595=ORIENTED_EDGE ( 'NONE', *, *, #12807, .T. ) ;
#16599=ORIENTED_EDGE ( 'NONE', *, *, #3458, .T. ) ;
#16600=CARTESIAN_POINT ( 'NONE',  ( 1.959283090834841090, -7.909254450748933962, -9.750336807931228478 ) ) ;
#16601=CARTESIAN_POINT ( 'NONE',  ( 0.3132642857406527370, 4.743831191224565202, -12.89240536501341161 ) ) ;
#16609=CARTESIAN_POINT ( 'NONE',  ( 2.697797270744666243, -11.26906156738832188, 7.053988368581824986 ) ) ;
#16611=CARTESIAN_POINT ( 'NONE',  ( 16.56679352167444819, 0.001518074900130650254, -0.009170718284672547266 ) ) ;
#16618=CARTESIAN_POINT ( 'NONE',  ( 16.56872352241294521, -0.001442253899401880124, -0.01033355228142401362 ) ) ;
#16620=CARTESIAN_POINT ( 'NONE',  ( 2.636624412717140764, -2.862162146982851763, -15.80357026013259514 ) ) ;
#16621=CARTESIAN_POINT ( 'NONE',  ( 2.002547531651519996, -6.845637710436110801, -10.57595306287299763 ) ) ;
#16623=ORIENTED_EDGE ( 'NONE', *, *, #12336, .T. ) ;
#16624=ADVANCED_FACE ( 'NONE', ( #10266 ), #3743, .F. ) ;
#16626=EDGE_CURVE ( 'NONE', #7234, #618, #8924, .T. ) ;
#16627=CARTESIAN_POINT ( 'NONE',  ( 16.56782317627811096, 0.009228812961909594811, 0.003357783021327272015 ) ) ;
#16634=VECTOR ( 'NONE', #6018, 1000.000000000000114 ) ;
#16644=CARTESIAN_POINT ( 'NONE',  ( 2.002547531651519996, -10.57595306287287329, -6.845637710436306200 ) ) ;
#16655=CARTESIAN_POINT ( 'NONE',  ( 0.4862570985993235340, 0.7479633556564388996, -13.89016912371016765 ) ) ;
#16659=EDGE_LOOP ( 'NONE', ( #17473, #12318 ) ) ;
#16660=CARTESIAN_POINT ( 'NONE',  ( 1.845755665166725068, 11.97169564665396280, -3.386720041070604204 ) ) ;
#16664=VERTEX_POINT ( 'NONE', #1962 ) ;
#16667=CARTESIAN_POINT ( 'NONE',  ( 2.353870697619111940, -6.980654702310762794, -10.90705766126227871 ) ) ;
#16670=CARTESIAN_POINT ( 'NONE',  ( 3.950837973638677170, 1.958075594453790869, 14.41405733518061538 ) ) ;
#16674=CARTESIAN_POINT ( 'NONE',  ( 8.522092701127531811, 5.841710761610131364, 3.777034505568545253 ) ) ;
#16676=ADVANCED_FACE ( 'NONE', ( #6259 ), #12137, .T. ) ;
#16677=ADVANCED_FACE ( 'NONE', ( #11896 ), #8376, .F. ) ;
#16683=CARTESIAN_POINT ( 'NONE',  ( 0.3720661004400040439, 7.524064345033631973, -11.58636699658207370 ) ) ;
#16684=CARTESIAN_POINT ( 'NONE',  ( 3.074695600507584281, 13.70113613813179043, -7.366518011945612621 ) ) ;
#16686=CARTESIAN_POINT ( 'NONE',  ( 0.3132635586635975078, 8.495712071659401232, 10.79541209008106861 ) ) ;
#16689=EDGE_CURVE ( 'NONE', #5119, #7915, #15475, .T. ) ;
#16699=DIRECTION ( 'NONE',  ( 0.7561779333270775005, -0.6106991889125055195, -0.2350349629540206264 ) ) ;
#16705=CARTESIAN_POINT ( 'NONE',  ( 2.002547531651519996, 10.57595306287302250, -6.845637710436074386 ) ) ;
#16707=ORIENTED_EDGE ( 'NONE', *, *, #9112, .F. ) ;
#16714=AXIS2_PLACEMENT_3D ( 'NONE', #12928, #1270, #2693 ) ;
#16718=CARTESIAN_POINT ( 'NONE',  ( 0.4754618798421167414, 11.68486377711977298, -7.564402563418342496 ) ) ;
#16719=CARTESIAN_POINT ( 'NONE',  ( 0.3137051932979809665, -13.20008686438108647, 3.805684345189735307 ) ) ;
#16723=CARTESIAN_POINT ( 'NONE',  ( 16.56872352241294521, -0.001821578298043862289, 0.01027347319884366027 ) ) ;
#16724=CARTESIAN_POINT ( 'NONE',  ( 0.3308579732647018989, 11.46737410776364996, -7.595989242675004860 ) ) ;
#16730=CARTESIAN_POINT ( 'NONE',  ( 2.636624412715435462, -15.80357026013316712, -2.862162146983298516 ) ) ;
#16732=CARTESIAN_POINT ( 'NONE',  ( 1.847412631396507798, 11.84727953344288132, -3.804043368582538776 ) ) ;
#16734=CARTESIAN_POINT ( 'NONE',  ( 8.438534575730034959, 6.454982381540319558, -2.341351102130211359 ) ) ;
#16737=AXIS2_PLACEMENT_3D ( 'NONE', #1644, #8720, #7489 ) ;
#16739=DIRECTION ( 'NONE',  ( 0.000000000000000000, 0.000000000000000000, 1.000000000000000000 ) ) ;
#16743=CARTESIAN_POINT ( 'NONE',  ( 0.8740779401510443414, -12.04241618260075164, -7.708543377337893077 ) ) ;
#16744=CARTESIAN_POINT ( 'NONE',  ( 2.002547531651519996, -4.532360870844247991, -11.75462648437106417 ) ) ;
#16748=FACE_OUTER_BOUND ( 'NONE', #16334, .T. ) ;
#16752=ORIENTED_EDGE ( 'NONE', *, *, #14977, .F. ) ;
#16754=CARTESIAN_POINT ( 'NONE',  ( 1.918918678667048683, -11.69059232068581800, 4.466049546133867842 ) ) ;
#16755=ORIENTED_EDGE ( 'NONE', *, *, #8086, .T. ) ;
#16759=DIRECTION ( 'NONE',  ( -1.000000000000000000, -0.000000000000000000, -0.000000000000000000 ) ) ;
#16762=ORIENTED_EDGE ( 'NONE', *, *, #7372, .F. ) ;
#16768=ADVANCED_FACE ( 'NONE', ( #12274, #803 ), #711, .F. ) ;
#16769=CARTESIAN_POINT ( 'NONE',  ( 1.847412631396501803, 7.278870946904251404, 10.09191835241965407 ) ) ;
#16773=CARTESIAN_POINT ( 'NONE',  ( 0.3058872367615230181, -12.87003593440631732, 4.821066432589277362 ) ) ;
#16774=CARTESIAN_POINT ( 'NONE',  ( 8.522092701127531811, -6.489356537178209372, 2.505958102592595882 ) ) ;
#16779=EDGE_LOOP ( 'NONE', ( #11841, #18828, #4226, #7777 ) ) ;
#16784=( BOUNDED_SURFACE ( )  B_SPLINE_SURFACE ( 3, 1, ( 
 ( #2715, #11340 ),
 ( #8468, #15913 ),
 ( #12763, #18586 ),
 ( #14299, #4067 ) ),
 .UNSPECIFIED., .F., .F., .T. ) 
 B_SPLINE_SURFACE_WITH_KNOTS ( ( 4, 4 ),
 ( 2, 2 ),
 ( 0.000000000000000000, 1.000000000000000000 ),
 ( 0.000000000000000000, 1.000000000000000000 ),
 .UNSPECIFIED. ) 
 GEOMETRIC_REPRESENTATION_ITEM ( )  RATIONAL_B_SPLINE_SURFACE ( (
 ( 1.000000000000000000, 1.000000000000000000),
 ( 0.7792777138730158093, 0.9689936506012928330),
 ( 0.7792777138730158093, 0.9689936506012928330),
 ( 1.000000000000000000, 1.000000000000000000) ) ) 
 REPRESENTATION_ITEM ( '' )  SURFACE ( )  );
#16786=B_SPLINE_CURVE_WITH_KNOTS ( 'NONE', 3,
 ( #4832, #16493, #8741, #336, #6069, #7707, #17734, #4438, #4638, #10366, #140, #14659, #10268 ),
 .UNSPECIFIED., .F., .F.,
 ( 4, 3, 3, 3, 4 ),
 ( 2.602085213965210642E-18, 0.0002299780670421064713, 0.0004599561239687913672, 0.0006896788984287877382, 0.0009194956271626401716 ),
 .UNSPECIFIED. ) ;
#16795=CARTESIAN_POINT ( 'NONE',  ( 1.845755665166724624, -7.694641135842892332, 9.776700214453605042 ) ) ;
#16802=CARTESIAN_POINT ( 'NONE',  ( 2.636624412716062071, -11.10302021258080352, -11.60464335004061454 ) ) ;
#16806=CARTESIAN_POINT ( 'NONE',  ( 1.846138399168762101, 11.95493567637855392, -3.446241763652874379 ) ) ;
#16807=ORIENTED_EDGE ( 'NONE', *, *, #18523, .T. ) ;
#16810=CARTESIAN_POINT ( 'NONE',  ( 0.4385251269669942498, 11.63205320541534071, -7.540955776459614235 ) ) ;
#16812=CARTESIAN_POINT ( 'NONE',  ( 1.977436885026782276, -7.806953934146112495, -13.27782258181927233 ) ) ;
#16813=CARTESIAN_POINT ( 'NONE',  ( 1.846138399168762101, -9.815003036200353748, -7.646096044340000120 ) ) ;
#16818=ORIENTED_EDGE ( 'NONE', *, *, #17001, .T. ) ;
#16820=CARTESIAN_POINT ( 'NONE',  ( 0.8740779401510754276, -9.070947476926809472, -11.05257166392059354 ) ) ;
#16821=ORIENTED_EDGE ( 'NONE', *, *, #16964, .T. ) ;
#16822=CARTESIAN_POINT ( 'NONE',  ( 2.636624412715137034, -11.60464335004055947, 11.10302021257951743 ) ) ;
#16823=CARTESIAN_POINT ( 'NONE',  ( 1.847372867223026294, -0.1054171785007356615, 12.44269075185938789 ) ) ;
#16827=ORIENTED_EDGE ( 'NONE', *, *, #5395, .T. ) ;
#16828=CARTESIAN_POINT ( 'NONE',  ( 2.320520222539028232, 15.43440824797023225, -3.126729907237324912 ) ) ;
#16829=CARTESIAN_POINT ( 'NONE',  ( 2.320521194583335500, -13.71278319228129483, -7.743190876766059105 ) ) ;
#16831=CARTESIAN_POINT ( 'NONE',  ( 1.846613052777650976, 9.862487290071108248, -7.585914669018062106 ) ) ;
#16832=EDGE_CURVE ( 'NONE', #17922, #15093, #16917, .T. ) ;
#16834=EDGE_CURVE ( 'NONE', #5002, #3017, #18560, .T. ) ;
#16836=PRESENTATION_STYLE_ASSIGNMENT (( #11109 ) ) ;
#16837=CARTESIAN_POINT ( 'NONE',  ( 16.58200780006414732, -0.002844973367391502410, 0.01080144354108869553 ) ) ;
#16840=ORIENTED_EDGE ( 'NONE', *, *, #9691, .F. ) ;
#16843=CARTESIAN_POINT ( 'NONE',  ( 1.918921323896323194, 12.08297777410669482, -3.258415356426395793 ) ) ;
#16845=ORIENTED_EDGE ( 'NONE', *, *, #10379, .T. ) ;
#16854=EDGE_CURVE ( 'NONE', #17922, #13924, #11311, .T. ) ;
#16856=CARTESIAN_POINT ( 'NONE',  ( 1.847168016377982003, 7.464000291196414061, 9.955470380986653822 ) ) ;
#16858=B_SPLINE_CURVE_WITH_KNOTS ( 'NONE', 3,
 ( #16322, #7922, #9342, #13734, #644, #15168 ),
 .UNSPECIFIED., .F., .F.,
 ( 4, 2, 4 ),
 ( 3.671973638477265170E-17, 0.0001825746017570593200, 0.0003651492035140796086 ),
 .UNSPECIFIED. ) ;
#16862=EDGE_CURVE ( 'NONE', #5180, #4027, #8431, .T. ) ;
#16863=CARTESIAN_POINT ( 'NONE',  ( 1.846613052777651198, 7.035606253495462425, -10.26230975746752350 ) ) ;
#16864=CARTESIAN_POINT ( 'NONE',  ( 2.002547531651520885, -4.532360870844412304, 11.75462648437100377 ) ) ;
#16872=ORIENTED_EDGE ( 'NONE', *, *, #7912, .T. ) ;
#16874=CARTESIAN_POINT ( 'NONE',  ( 0.3137051932979809665, 10.83767969834803324, 8.442169467526891680 ) ) ;
#16878=CARTESIAN_POINT ( 'NONE',  ( 3.950837973638676281, 12.81214529934975310, 6.888253895133341409 ) ) ;
#16879=DIRECTION ( 'NONE',  ( 0.7635533937278214944, -0.5095610256143857653, -0.3966532189476615899 ) ) ;
#16887=ORIENTED_EDGE ( 'NONE', *, *, #18523, .F. ) ;
#16889=ORIENTED_EDGE ( 'NONE', *, *, #2756, .F. ) ;
#16896=ORIENTED_EDGE ( 'NONE', *, *, #9707, .T. ) ;
#16897=CARTESIAN_POINT ( 'NONE',  ( 1.562796894703937678, 0.000000000000000000, -12.15840553252917289 ) ) ;
#16901=CARTESIAN_POINT ( 'NONE',  ( 16.57210152137263393, 0.01453130299868522594, 0.0006600038696346533949 ) ) ;
#16902=B_SPLINE_CURVE_WITH_KNOTS ( 'NONE', 3,
 ( #2044, #15034, #1951, #13602, #3562, #12082 ),
 .UNSPECIFIED., .F., .F.,
 ( 4, 2, 4 ),
 ( 0.000000000000000000, 0.001500839035891551139, 0.003001678071783102277 ),
 .UNSPECIFIED. ) ;
#16905=CARTESIAN_POINT ( 'NONE',  ( 0.3150692679895968906, 13.11337225490258263, -4.099798979280710576 ) ) ;
#16910=CARTESIAN_POINT ( 'NONE',  ( 16.56753206892534891, -0.001421777558676855365, -0.009389754735541546229 ) ) ;
#16917=B_SPLINE_CURVE_WITH_KNOTS ( 'NONE', 3,
 ( #8527, #13111, #1168, #18647, #4324, #14445 ),
 .UNSPECIFIED., .F., .F.,
 ( 4, 2, 4 ),
 ( 4.063025038712889623E-17, 0.0002014099069817291640, 0.0004028198139634176704 ),
 .UNSPECIFIED. ) ;
#16919=CARTESIAN_POINT ( 'NONE',  ( 2.636624412717099908, 15.80357026013547816, -2.862162146981609201 ) ) ;
#16920=ADVANCED_FACE ( 'NONE', ( #7681 ), #589, .F. ) ;
#16924=( BOUNDED_SURFACE ( )  B_SPLINE_SURFACE ( 3, 1, ( 
 ( #6515, #12334 ),
 ( #14051, #5068 ),
 ( #15295, #955 ),
 ( #2208, #8049 ) ),
 .UNSPECIFIED., .F., .F., .F. ) 
 B_SPLINE_SURFACE_WITH_KNOTS ( ( 4, 4 ),
 ( 2, 2 ),
 ( 0.000000000000000000, 1.000000000000000000 ),
 ( 0.000000000000000000, 1.000000000000000000 ),
 .UNSPECIFIED. ) 
 GEOMETRIC_REPRESENTATION_ITEM ( )  RATIONAL_B_SPLINE_SURFACE ( (
 ( 1.000000000000000000, 1.000000000000000000),
 ( 0.9933953342250438912, 0.8357391271907739227),
 ( 0.9933953342250438912, 0.8357391271907739227),
 ( 1.000000000000000000, 1.000000000000000000) ) ) 
 REPRESENTATION_ITEM ( '' )  SURFACE ( )  );
#16925=CARTESIAN_POINT ( 'NONE',  ( 1.846955891736115518, 9.909315188408152508, -7.525208385419853485 ) ) ;
#16935=B_SPLINE_CURVE_WITH_KNOTS ( 'NONE', 3,
 ( #16802, #17145, #4056, #9872 ),
 .UNSPECIFIED., .F., .F.,
 ( 4, 4 ),
 ( 9.204257061898183523E-17, 0.002004993803842712065 ),
 .UNSPECIFIED. ) ;
#16936=CARTESIAN_POINT ( 'NONE',  ( 2.747332970342022840, -2.409922051470567261, -16.17136872824901062 ) ) ;
#16937=CARTESIAN_POINT ( 'NONE',  ( 0.3145729642390375225, -4.535980493005000724, -12.96842777670211611 ) ) ;
#16947=VECTOR ( 'NONE', #2835, 999.9999999999998863 ) ;
#16948=CARTESIAN_POINT ( 'NONE',  ( 2.002547531651520885, 10.57595306287292480, 6.845637710436228929 ) ) ;
#16951=CARTESIAN_POINT ( 'NONE',  ( 1.846524061778018977, 7.023652644192272199, 10.27028962889599484 ) ) ;
#16955=CARTESIAN_POINT ( 'NONE',  ( 0.3150686449036028680, -13.01866258978840030, 4.391272911157273029 ) ) ;
#16964=EDGE_CURVE ( 'NONE', #5602, #2485, #14726, .T. ) ;
#16974=FACE_OUTER_BOUND ( 'NONE', #52, .T. ) ;
#16975=CARTESIAN_POINT ( 'NONE',  ( 0.3058872367615226295, -10.75034008168909416, -8.562166468153835197 ) ) ;
#16977=CARTESIAN_POINT ( 'NONE',  ( 16.57210152137263393, 0.009075239946109033701, 0.01136813053532163831 ) ) ;
#16984=VERTEX_POINT ( 'NONE', #3151 ) ;
#16985=FACE_OUTER_BOUND ( 'NONE', #15843, .T. ) ;
#16986=EDGE_CURVE ( 'NONE', #15892, #14167, #7387, .T. ) ;
#16989=CARTESIAN_POINT ( 'NONE',  ( 2.697797270744667131, -4.970631985779678352, 12.33058466479267778 ) ) ;
#16992=EDGE_CURVE ( 'NONE', #5926, #4785, #18323, .T. ) ;
#16993=VERTEX_POINT ( 'NONE', #4610 ) ;
#17000=CIRCLE ( 'NONE', #4495, 13.42403576283810906 ) ;
#17001=EDGE_CURVE ( 'NONE', #2287, #9336, #11434, .T. ) ;
#17005=( BOUNDED_SURFACE ( )  B_SPLINE_SURFACE ( 3, 1, ( 
 ( #15206, #13947 ),
 ( #4889, #5064 ),
 ( #10911, #2117 ),
 ( #6602, #13764 ) ),
 .UNSPECIFIED., .F., .F., .T. ) 
 B_SPLINE_SURFACE_WITH_KNOTS ( ( 4, 4 ),
 ( 2, 2 ),
 ( 0.000000000000000000, 1.000000000000000000 ),
 ( 0.000000000000000000, 1.000000000000000000 ),
 .UNSPECIFIED. ) 
 GEOMETRIC_REPRESENTATION_ITEM ( )  RATIONAL_B_SPLINE_SURFACE ( (
 ( 1.000000000000000000, 1.000000000000000000),
 ( 0.7792777138730158093, 0.9689936506012928330),
 ( 0.7792777138730158093, 0.9689936506012928330),
 ( 1.000000000000000000, 1.000000000000000000) ) ) 
 REPRESENTATION_ITEM ( '' )  SURFACE ( )  );
#17013=B_SPLINE_CURVE_WITH_KNOTS ( 'NONE', 3,
 ( #13578, #498, #4870, #2552, #1135, #3916 ),
 .UNSPECIFIED., .F., .F.,
 ( 4, 2, 4 ),
 ( 0.000000000000000000, 0.001656992708822042004, 0.003313985417644083140 ),
 .UNSPECIFIED. ) ;
#17017=DIRECTION ( 'NONE',  ( -1.000000000000000000, -0.000000000000000000, -0.000000000000000000 ) ) ;
#17018=EDGE_CURVE ( 'NONE', #4102, #8021, #3684, .T. ) ;
#17019=EDGE_CURVE ( 'NONE', #18802, #10356, #285, .T. ) ;
#17021=CARTESIAN_POINT ( 'NONE',  ( 3.950837973638668288, 0.000000000000000000, 0.000000000000000000 ) ) ;
#17023=CARTESIAN_POINT ( 'NONE',  ( 1.847034903785828019, -7.498375632854680006, 9.929438108952115982 ) ) ;
#17024=CARTESIAN_POINT ( 'NONE',  ( 0.3132642857406535697, -13.21852905223341601, 3.740125687984681591 ) ) ;
#17029=CARTESIAN_POINT ( 'NONE',  ( 1.342453679581834924, -13.74702459364888263, 5.476372339889963747 ) ) ;
#17031=CARTESIAN_POINT ( 'NONE',  ( 0.4862570985993235340, 5.003653737315670647, -12.97920246947874112 ) ) ;
#17032=ORIENTED_EDGE ( 'NONE', *, *, #15576, .T. ) ;
#17036=ORIENTED_EDGE ( 'NONE', *, *, #8834, .T. ) ;
#17051=CARTESIAN_POINT ( 'NONE',  ( 0.3095370825347224519, 11.38092634279639626, -7.700448427571749299 ) ) ;
#17053=CARTESIAN_POINT ( 'NONE',  ( 1.846138399168762101, 12.43476674860266584, -0.4167076046095982700 ) ) ;
#17055=ORIENTED_EDGE ( 'NONE', *, *, #700, .T. ) ;
#17057=VERTEX_POINT ( 'NONE', #602 ) ;
#17061=B_SPLINE_CURVE_WITH_KNOTS ( 'NONE', 3,
 ( #11901, #8642, #5667, #18868, #4348, #14568 ),
 .UNSPECIFIED., .F., .F.,
 ( 4, 2, 4 ),
 ( 0.000000000000000000, 0.001657017934712276541, 0.003314035869424553082 ),
 .UNSPECIFIED. ) ;
#17062=DIRECTION ( 'NONE',  ( -0.7561779333270775005, 0.6322161072786942615, 0.1688126975276577901 ) ) ;
#17068=EDGE_CURVE ( 'NONE', #3117, #14815, #18500, .T. ) ;
#17080=CARTESIAN_POINT ( 'NONE',  ( 3.664313757352971823, -13.97913389346635427, 2.831308606787193316 ) ) ;
#17082=CARTESIAN_POINT ( 'NONE',  ( 0.3137051932979775248, 10.83767969834815581, -8.442169467526731808 ) ) ;
#17086=CARTESIAN_POINT ( 'NONE',  ( 1.847461586945727596, -11.84459954310608332, -3.813310247068566028 ) ) ;
#17093=VERTEX_POINT ( 'NONE', #12521 ) ;
#17094=EDGE_CURVE ( 'NONE', #16055, #3103, #14402, .T. ) ;
#17104=CARTESIAN_POINT ( 'NONE',  ( 16.56753206892534891, -0.008490833999798953410, -0.004253784598196148035 ) ) ;
#17109=DIRECTION ( 'NONE',  ( -1.000000000000000000, -0.000000000000000000, -0.000000000000000000 ) ) ;
#17111=DIRECTION ( 'NONE',  ( -1.000000000000000000, -0.000000000000000000, -0.000000000000000000 ) ) ;
#17121=CARTESIAN_POINT ( 'NONE',  ( 2.320521194583477165, -6.542541239686160637, -14.32454473829993447 ) ) ;
#17123=CARTESIAN_POINT ( 'NONE',  ( 1.959283090834856633, -0.6676170829051342182, -12.53713130127478692 ) ) ;
#17128=CARTESIAN_POINT ( 'NONE',  ( 1.959212340397946450, 7.909199412631302550, -9.750290364083546990 ) ) ;
#17129=CARTESIAN_POINT ( 'NONE',  ( 16.56753206892534891, 0.008432171035096448775, -0.004368917149005366145 ) ) ;
#17136=FACE_OUTER_BOUND ( 'NONE', #2906, .T. ) ;
#17138=VERTEX_POINT ( 'NONE', #16744 ) ;
#17139=CARTESIAN_POINT ( 'NONE',  ( 0.3151926232592440202, 11.07013665200807395, -8.137833541809259330 ) ) ;
#17140=CARTESIAN_POINT ( 'NONE',  ( 2.747332970342022840, -7.289199830147212289, 14.63517873738944708 ) ) ;
#17142=EDGE_CURVE ( 'NONE', #6611, #16284, #13015, .T. ) ;
#17143=VERTEX_POINT ( 'NONE', #11200 ) ;
#17145=CARTESIAN_POINT ( 'NONE',  ( 3.074695600507423521, -10.75417554975728329, -11.23985886659437483 ) ) ;
#17146=CIRCLE ( 'NONE', #4020, 12.15840553252917289 ) ;
#17148=EDGE_CURVE ( 'NONE', #14004, #5097, #16209, .T. ) ;
#17155=CIRCLE ( 'NONE', #4034, 14.54644660717763927 ) ;
#17157=CARTESIAN_POINT ( 'NONE',  ( 1.845756295923360435, -12.43231724724606835, 0.4783934145701590479 ) ) ;
#17162=B_SPLINE_CURVE_WITH_KNOTS ( 'NONE', 3,
 ( #5430, #4194, #5698, #2823, #4090, #8672, #2546, #8395, #11550, #10008, #1412, #1029, #5601 ),
 .UNSPECIFIED., .F., .F.,
 ( 4, 3, 3, 3, 4 ),
 ( 2.168404344971008868E-18, 0.0002299804304191472269, 0.0004599608082120226239, 0.0006467586077647999570, 0.0008336169836825976396 ),
 .UNSPECIFIED. ) ;
#17165=CARTESIAN_POINT ( 'NONE',  ( 2.353870697619111940, -12.53036919722786813, 3.268530966681581607 ) ) ;
#17171=DIRECTION ( 'NONE',  ( -0.7561779333270775005, -0.3559159372837353286, 0.5491072561318327550 ) ) ;
#17175=CARTESIAN_POINT ( 'NONE',  ( 16.58200780006414732, -0.006043560077721775101, 0.009393638146078504489 ) ) ;
#17178=CARTESIAN_POINT ( 'NONE',  ( 3.950837973638668288, 0.000000000000000000, 0.000000000000000000 ) ) ;
#17179=ORIENTED_EDGE ( 'NONE', *, *, #4447, .F. ) ;
#17181=VERTEX_POINT ( 'NONE', #6615 ) ;
#17186=EDGE_CURVE ( 'NONE', #618, #8134, #9138, .T. ) ;
#17188=EDGE_CURVE ( 'NONE', #15164, #14390, #7800, .T. ) ;
#17191=EDGE_CURVE ( 'NONE', #14815, #18903, #4871, .T. ) ;
#17192=CARTESIAN_POINT ( 'NONE',  ( 3.950837973638676281, 13.10350451991840615, 6.316429227969512894 ) ) ;
#17196=ORIENTED_EDGE ( 'NONE', *, *, #11235, .F. ) ;
#17198=LINE ( 'NONE', #8508, #13235 ) ;
#17199=CARTESIAN_POINT ( 'NONE',  ( 0.3145729642390355796, -13.73540280162741212, 0.3065092323350734893 ) ) ;
#17207=ORIENTED_EDGE ( 'NONE', *, *, #9626, .T. ) ;
#17211=CARTESIAN_POINT ( 'NONE',  ( 0.3137051932979792457, 4.679953077377670745, -12.91601973349265720 ) ) ;
#17220=CARTESIAN_POINT ( 'NONE',  ( 0.3150686449036029790, -0.1533607327084788585, -13.73846184595214481 ) ) ;
#17221=DIRECTION ( 'NONE',  ( 0.7635533937278216055, 0.1790966170213880715, 0.6204116510013496510 ) ) ;
#17224=CARTESIAN_POINT ( 'NONE',  ( 0.3137051932979792457, -13.20008686438103140, -3.805684345189927154 ) ) ;
#17230=ORIENTED_EDGE ( 'NONE', *, *, #6617, .F. ) ;
#17232=CARTESIAN_POINT ( 'NONE',  ( 16.56872352241294521, -0.004907101719995745834, -0.009207754980064182873 ) ) ;
#17233=AXIS2_PLACEMENT_3D ( 'NONE', #17390, #17111, #4303 ) ;
#17237=CARTESIAN_POINT ( 'NONE',  ( 0.4754618798421167414, -13.89949764182682124, -0.7484603771385852644 ) ) ;
#17238=ORIENTED_EDGE ( 'NONE', *, *, #16992, .T. ) ;
#17242=EDGE_CURVE ( 'NONE', #5687, #31, #1612, .T. ) ;
#17246=CARTESIAN_POINT ( 'NONE',  ( 0.3720661004400037664, -0.7231997263365766981, 13.79610186261029448 ) ) ;
#17249=DIRECTION ( 'NONE',  ( 1.000000000000000000, 0.000000000000000000, 0.000000000000000000 ) ) ;
#17255=EDGE_CURVE ( 'NONE', #17352, #4785, #18046, .T. ) ;
#17258=ORIENTED_EDGE ( 'NONE', *, *, #15444, .F. ) ;
#17259=DIRECTION ( 'NONE',  ( -1.000000000000000000, -0.000000000000000000, -0.000000000000000000 ) ) ;
#17263=CARTESIAN_POINT ( 'NONE',  ( 2.697797270744667131, 13.26309265156977624, 0.9169917281807724585 ) ) ;
#17276=CARTESIAN_POINT ( 'NONE',  ( 0.3095370825347224519, -13.73357284481725138, 0.4597470195089713441 ) ) ;
#17277=ORIENTED_EDGE ( 'NONE', *, *, #13873, .T. ) ;
#17281=CARTESIAN_POINT ( 'NONE',  ( 1.845755665166724846, -6.920419570228271589, -10.33920510797150882 ) ) ;
#17287=AXIS2_PLACEMENT_3D ( 'NONE', #5551, #2413, #15598 ) ;
#17289=CARTESIAN_POINT ( 'NONE',  ( 3.950837973638676281, -14.41405733518061716, 1.958075594453740687 ) ) ;
#17290=CARTESIAN_POINT ( 'NONE',  ( 1.846138399168762101, -6.971848976710933954, -10.30487220521577818 ) ) ;
#17298=CARTESIAN_POINT ( 'NONE',  ( 0.3170788640506441158, 4.100430649998145327, -13.11595226728153385 ) ) ;
#17301=CARTESIAN_POINT ( 'NONE',  ( 1.977436885026044200, -13.27782258181834685, 7.806953934146225293 ) ) ;
#17302=CARTESIAN_POINT ( 'NONE',  ( 3.950837973638668288, 0.000000000000000000, 0.000000000000000000 ) ) ;
#17303=VERTEX_POINT ( 'NONE', #17289 ) ;
#17305=EDGE_LOOP ( 'NONE', ( #8633, #8637, #18503, #6279 ) ) ;
#17306=CARTESIAN_POINT ( 'NONE',  ( 16.56679352167444819, 0.009190982326619362083, -0.001390132774595485713 ) ) ;
#17307=ORIENTED_EDGE ( 'NONE', *, *, #14597, .T. ) ;
#17308=CARTESIAN_POINT ( 'NONE',  ( 1.846613052777651198, 10.26230975746759810, 7.035606253495352291 ) ) ;
#17312=CARTESIAN_POINT ( 'NONE',  ( 3.950837973638676281, 6.316429227969464932, 13.10350451991842569 ) ) ;
#17315=CARTESIAN_POINT ( 'NONE',  ( 0.8740764193765260259, 3.609949042658226581, 13.83508774435983035 ) ) ;
#17316=CARTESIAN_POINT ( 'NONE',  ( 0.4754618798421162973, -13.89949764182682124, -0.7484603771385882620 ) ) ;
#17319=VECTOR ( 'NONE', #16879, 1000.000000000000227 ) ;
#17322=CARTESIAN_POINT ( 'NONE',  ( 3.512766787570836158, 7.127386085302768848, 13.25664064834467837 ) ) ;
#17332=VERTEX_POINT ( 'NONE', #3032 ) ;
#17342=CARTESIAN_POINT ( 'NONE',  ( 16.56753206892534891, 0.008490833999798002782, -0.004253784598196794220 ) ) ;
#17343=CARTESIAN_POINT ( 'NONE',  ( 16.57210152137263393, -0.009075239946109120437, -0.01136813053532156892 ) ) ;
#17351=ORIENTED_EDGE ( 'NONE', *, *, #8999, .F. ) ;
#17352=VERTEX_POINT ( 'NONE', #2941 ) ;
#17358=ORIENTED_EDGE ( 'NONE', *, *, #8624, .F. ) ;
#17359=DIRECTION ( 'NONE',  ( 0.000000000000000000, 0.000000000000000000, 1.000000000000000000 ) ) ;
#17363=CARTESIAN_POINT ( 'NONE',  ( 0.3058872367615226295, 13.24582953854930345, -3.664492643742625511 ) ) ;
#17364=CARTESIAN_POINT ( 'NONE',  ( 0.3142011359265332593, -10.88514493056448096, 8.382042760265870029 ) ) ;
#17366=CARTESIAN_POINT ( 'NONE',  ( 2.002547531651519996, -7.942910686618100513, -9.778737580845787036 ) ) ;
#17368=CARTESIAN_POINT ( 'NONE',  ( 0.3137051932979792457, 4.679953077377485116, 12.91601973349272114 ) ) ;
#17373=ORIENTED_EDGE ( 'NONE', *, *, #15576, .F. ) ;
#17375=AXIS2_PLACEMENT_3D ( 'NONE', #4006, #2554, #8405 ) ;
#17386=ADVANCED_FACE ( 'NONE', ( #6021 ), #1282, .F. ) ;
#17389=CARTESIAN_POINT ( 'NONE',  ( 0.3142011359265306503, -13.17934269988455576, -3.879426116491829557 ) ) ;
#17390=CARTESIAN_POINT ( 'NONE',  ( 2.636624412714236865, 0.000000000000000000, 0.000000000000000000 ) ) ;
#17397=CARTESIAN_POINT ( 'NONE',  ( 0.3151928476913555821, 8.075547435847115096, -11.11539186930577827 ) ) ;
#17398=ORIENTED_EDGE ( 'NONE', *, *, #14979, .T. ) ;
#17399=CARTESIAN_POINT ( 'NONE',  ( 0.3170788640506440603, -13.11595226728160668, 4.100430649997911736 ) ) ;
#17401=CARTESIAN_POINT ( 'NONE',  ( 1.847380140988739594, 10.13114603776196887, 7.224522571381366554 ) ) ;
#17402=B_SPLINE_CURVE_WITH_KNOTS ( 'NONE', 3,
 ( #4125, #15677, #4227, #111 ),
 .UNSPECIFIED., .F., .F.,
 ( 4, 4 ),
 ( 1.514782153580211930E-17, 0.003005512676784846161 ),
 .UNSPECIFIED. ) ;
#17404=B_SPLINE_CURVE_WITH_KNOTS ( 'NONE', 3,
 ( #3188, #11906, #16410, #9038, #10277, #10177 ),
 .UNSPECIFIED., .F., .F.,
 ( 4, 2, 4 ),
 ( 4.256846838097967453E-17, 0.0002014099069817298958, 0.0004028198139634172367 ),
 .UNSPECIFIED. ) ;
#17413=CARTESIAN_POINT ( 'NONE',  ( 2.320520222536399668, 3.126729907239529815, 15.43440824796666710 ) ) ;
#17416=B_SPLINE_CURVE_WITH_KNOTS ( 'NONE', 3,
 ( #18689, #5592, #17263, #4183, #7825, #1983 ),
 .UNSPECIFIED., .F., .F.,
 ( 4, 2, 4 ),
 ( 0.000000000000000000, 0.001500839035891553090, 0.003001678071783106180 ),
 .UNSPECIFIED. ) ;
#17422=CARTESIAN_POINT ( 'NONE',  ( 2.636624412714236865, 15.91454522070173638, 2.161493821596668585 ) ) ;
#17426=CARTESIAN_POINT ( 'NONE',  ( 16.56753206892534891, -0.006760771273036217388, -0.006669401563384900512 ) ) ;
#17428=ORIENTED_EDGE ( 'NONE', *, *, #18267, .F. ) ;
#17430=CIRCLE ( 'NONE', #4308, 16.06066017081991149 ) ;
#17431=CARTESIAN_POINT ( 'NONE',  ( 1.342453679581834924, -14.76648944001038544, -0.9602753779832271519 ) ) ;
#17432=ORIENTED_EDGE ( 'NONE', *, *, #18238, .F. ) ;
#17440=CARTESIAN_POINT ( 'NONE',  ( 1.254255976358046087, 5.487601330835574664, -13.61551404021248857 ) ) ;
#17446=CARTESIAN_POINT ( 'NONE',  ( 1.959283090834842200, 4.509128209890970851, 11.71721539537256618 ) ) ;
#17448=CARTESIAN_POINT ( 'NONE',  ( 0.3150686449036029790, 13.73846184595214304, -0.1533607327086227434 ) ) ;
#17449=VERTEX_POINT ( 'NONE', #8951 ) ;
#17450=ORIENTED_EDGE ( 'NONE', *, *, #5857, .F. ) ;
#17451=ORIENTED_EDGE ( 'NONE', *, *, #17186, .F. ) ;
#17452=B_SPLINE_CURVE_WITH_KNOTS ( 'NONE', 3,
 ( #12503, #11086, #11177, #14035 ),
 .UNSPECIFIED., .F., .F.,
 ( 4, 4 ),
 ( 0.000000000000000000, 0.002004993803842297466 ),
 .UNSPECIFIED. ) ;
#17455=CARTESIAN_POINT ( 'NONE',  ( 1.847034903785822246, 4.063013886994871982, -11.76058231742741533 ) ) ;
#17460=DIRECTION ( 'NONE',  ( 0.000000000000000000, 0.000000000000000000, 1.000000000000000000 ) ) ;
#17462=CARTESIAN_POINT ( 'NONE',  ( 0.3095370825347234511, 0.4597470195092124290, -13.73357284481724250 ) ) ;
#17464=CARTESIAN_POINT ( 'NONE',  ( 0.4754618798421162973, 3.583352865732667425, 13.45049478164061441 ) ) ;
#17467=CARTESIAN_POINT ( 'NONE',  ( 2.747332970342022840, -16.17136872824900351, 2.409922051470623661 ) ) ;
#17468=CARTESIAN_POINT ( 'NONE',  ( 1.918921323896323639, -9.738309537478938793, -7.860085869556288962 ) ) ;
#17472=ORIENTED_EDGE ( 'NONE', *, *, #14053, .F. ) ;
#17473=ORIENTED_EDGE ( 'NONE', *, *, #6828, .F. ) ;
#17476=VERTEX_POINT ( 'NONE', #6095 ) ;
#17478=CARTESIAN_POINT ( 'NONE',  ( 3.950837973638676281, -10.05648675950133963, 10.51028938476214059 ) ) ;
#17481=ORIENTED_EDGE ( 'NONE', *, *, #16626, .T. ) ;
#17484=CARTESIAN_POINT ( 'NONE',  ( 1.342453679581834924, 0.9602753779830727199, 14.76648944001039787 ) ) ;
#17488=CARTESIAN_POINT ( 'NONE',  ( 16.56679352167444819, -0.001390132774594504727, 0.009190982326619714232 ) ) ;
#17490=DIRECTION ( 'NONE',  ( -1.000000000000000000, -0.000000000000000000, -0.000000000000000000 ) ) ;
#17493=CARTESIAN_POINT ( 'NONE',  ( 16.56782317627811096, -0.007739510688078479403, 0.006045301465876602373 ) ) ;
#17494=B_SPLINE_CURVE_WITH_KNOTS ( 'NONE', 3,
 ( #15196, #3714, #11269, #13935, #12588, #10903 ),
 .UNSPECIFIED., .F., .F.,
 ( 4, 2, 4 ),
 ( 0.000000000000000000, 0.001656992708822040920, 0.003313985417644081839 ),
 .UNSPECIFIED. ) ;
#17500=EDGE_CURVE ( 'NONE', #1614, #5120, #15249, .T. ) ;
#17501=CARTESIAN_POINT ( 'NONE',  ( 0.3151930723728413319, 4.318364831037771800, -13.04315954105010533 ) ) ;
#17509=AXIS2_PLACEMENT_3D ( 'NONE', #4296, #2658, #2834 ) ;
#17512=DIRECTION ( 'NONE',  ( 0.000000000000000000, 0.000000000000000000, -1.000000000000000000 ) ) ;
#17515=ADVANCED_FACE ( 'NONE', ( #16425 ), #16199, .F. ) ;
#17517=CARTESIAN_POINT ( 'NONE',  ( 0.3142014840576516921, 11.33546131209473806, -7.762239086932731347 ) ) ;
#17521=CARTESIAN_POINT ( 'NONE',  ( 0.3132635586635976188, -4.743936529203153007, -12.89236642382226172 ) ) ;
#17522=ORIENTED_EDGE ( 'NONE', *, *, #10868, .F. ) ;
#17524=B_SPLINE_CURVE_WITH_KNOTS ( 'NONE', 3,
 ( #5965, #1667, #7227, #243, #13040, #14662 ),
 .UNSPECIFIED., .F., .F.,
 ( 4, 2, 4 ),
 ( 0.000000000000000000, 0.001656992708824380845, 0.003313985417648761689 ),
 .UNSPECIFIED. ) ;
#17526=FACE_OUTER_BOUND ( 'NONE', #13676, .T. ) ;
#17528=CARTESIAN_POINT ( 'NONE',  ( 3.950837973638668288, 0.000000000000000000, 0.000000000000000000 ) ) ;
#17530=B_SPLINE_CURVE_WITH_KNOTS ( 'NONE', 3,
 ( #7597, #13118, #10444, #3163, #9011, #25 ),
 .UNSPECIFIED., .F., .F.,
 ( 4, 2, 4 ),
 ( 2.474737474518078493E-18, 0.0002017457492448081235, 0.0004034914984896138075 ),
 .UNSPECIFIED. ) ;
#17531=FACE_OUTER_BOUND ( 'NONE', #5728, .T. ) ;
#17533=FACE_OUTER_BOUND ( 'NONE', #8424, .T. ) ;
#17537=CARTESIAN_POINT ( 'NONE',  ( 2.747332970342022840, -11.45495994260726214, 11.66639548242803492 ) ) ;
#17539=FACE_OUTER_BOUND ( 'NONE', #7504, .T. ) ;
#17541=CARTESIAN_POINT ( 'NONE',  ( 0.3145729642390356351, 13.73540280162741034, -0.3065092323351694126 ) ) ;
#17545=AXIS2_PLACEMENT_3D ( 'NONE', #2007, #9069, #1906 ) ;
#17549=ORIENTED_EDGE ( 'NONE', *, *, #2756, .T. ) ;
#17553=CARTESIAN_POINT ( 'NONE',  ( 3.512766787570801519, 6.535475144496956545, 13.55823433651946175 ) ) ;
#17554=VECTOR ( 'NONE', #17062, 1000.000000000000114 ) ;
#17556=ORIENTED_EDGE ( 'NONE', *, *, #10097, .F. ) ;
#17560=CARTESIAN_POINT ( 'NONE',  ( 2.705023505549867924, -0.8488853074252048492, -13.27418276223637150 ) ) ;
#17562=CARTESIAN_POINT ( 'NONE',  ( 1.846822687350021974, 0.2922081769261886675, -12.43915556955403190 ) ) ;
#17565=CARTESIAN_POINT ( 'NONE',  ( 0.3148213771069321987, -7.888490156175138601, -11.24846294176320960 ) ) ;
#17567=AXIS2_PLACEMENT_3D ( 'NONE', #6820, #6647, #12639 ) ;
#17569=ORIENTED_EDGE ( 'NONE', *, *, #17611, .F. ) ;
#17570=EDGE_CURVE ( 'NONE', #3103, #7378, #16021, .T. ) ;
#17571=ORIENTED_EDGE ( 'NONE', *, *, #3323, .T. ) ;
#17572=CARTESIAN_POINT ( 'NONE',  ( 0.3095370825347233956, -3.806662003783505277, 13.20347358821913275 ) ) ;
#17573=EDGE_CURVE ( 'NONE', #16490, #5397, #14588, .T. ) ;
#17582=CARTESIAN_POINT ( 'NONE',  ( 2.002547531651519996, 10.57595306287302250, -6.845637710436074386 ) ) ;
#17583=CONICAL_SURFACE ( 'NONE', #11485, 14.54644660717763927, 0.8559913436420816257 ) ;
#17584=CARTESIAN_POINT ( 'NONE',  ( 16.57210152137263393, 0.01402404281922921964, -0.003862718596009325888 ) ) ;
#17588=SURFACE_SIDE_STYLE ('',( #13566 ) ) ;
#17590=VERTEX_POINT ( 'NONE', #1987 ) ;
#17594=ORIENTED_EDGE ( 'NONE', *, *, #926, .F. ) ;
#17600=CARTESIAN_POINT ( 'NONE',  ( 3.950837973638675393, -10.51028938476210328, -10.05648675950137871 ) ) ;
#17602=B_SPLINE_CURVE_WITH_KNOTS ( 'NONE', 3,
 ( #247, #11525, #12374, #9417, #13621, #2157 ),
 .UNSPECIFIED., .F., .F.,
 ( 4, 2, 4 ),
 ( 3.551420023959826846E-17, 0.0001825746017570578021, 0.0003651492035140800965 ),
 .UNSPECIFIED. ) ;
#17608=CARTESIAN_POINT ( 'NONE',  ( 0.3132635586635980074, -10.79541209008109703, 8.495712071659360376 ) ) ;
#17609=CARTESIAN_POINT ( 'NONE',  ( 0.3939875929385656117, -13.80036004410495210, 0.7003304234512695015 ) ) ;
#17611=EDGE_CURVE ( 'NONE', #13213, #4341, #9711, .T. ) ;
#17612=VECTOR ( 'NONE', #1571, 1000.000000000000114 ) ;
#17615=B_SPLINE_CURVE_WITH_KNOTS ( 'NONE', 3,
 ( #4244, #16087, #13119, #18853, #7398, #5745 ),
 .UNSPECIFIED., .F., .F.,
 ( 4, 2, 4 ),
 ( 2.168404344971008868E-19, 0.0001828790815886944003, 0.0003657581631773885837 ),
 .UNSPECIFIED. ) ;
#17616=( BOUNDED_SURFACE ( )  B_SPLINE_SURFACE ( 3, 1, ( 
 ( #13044, #8931 ),
 ( #7519, #1579 ),
 ( #16305, #5971 ),
 ( #14760, #17834 ) ),
 .UNSPECIFIED., .F., .F., .T. ) 
 B_SPLINE_SURFACE_WITH_KNOTS ( ( 4, 4 ),
 ( 2, 2 ),
 ( 0.000000000000000000, 1.000000000000000000 ),
 ( 0.000000000000000000, 1.000000000000000000 ),
 .UNSPECIFIED. ) 
 GEOMETRIC_REPRESENTATION_ITEM ( )  RATIONAL_B_SPLINE_SURFACE ( (
 ( 1.000000000000000000, 1.000000000000000000),
 ( 0.9593108457356467333, 0.9995965569486454649),
 ( 0.9593108457356467333, 0.9995965569486454649),
 ( 1.000000000000000000, 1.000000000000000000) ) ) 
 REPRESENTATION_ITEM ( '' )  SURFACE ( )  );
#17617=CARTESIAN_POINT ( 'NONE',  ( 16.56872352241294521, -0.007512283835804365630, 0.007240717549633862542 ) ) ;
#17620=VERTEX_POINT ( 'NONE', #18223 ) ;
#17623=ORIENTED_EDGE ( 'NONE', *, *, #11617, .T. ) ;
#17624=VECTOR ( 'NONE', #8610, 1000.000000000000227 ) ;
#17625=ORIENTED_EDGE ( 'NONE', *, *, #18263, .F. ) ;
#17626=CARTESIAN_POINT ( 'NONE',  ( 2.123976203522053297, -15.54801196254785722, -1.531817366691915483 ) ) ;
#17628=B_SPLINE_CURVE_WITH_KNOTS ( 'NONE', 3,
 ( #5483, #4160, #14189, #17440, #7224, #15906 ),
 .UNSPECIFIED., .F., .F.,
 ( 4, 2, 4 ),
 ( 0.000000000000000000, 0.001656992708823640335, 0.003313985417647279802 ),
 .UNSPECIFIED. ) ;
#17633=CARTESIAN_POINT ( 'NONE',  ( 16.56872352241294521, -0.009382111268606286789, 0.004564908236400187953 ) ) ;
#17634=CARTESIAN_POINT ( 'NONE',  ( 0.3137051932979792457, 4.679953077377670745, -12.91601973349265720 ) ) ;
#17635=CIRCLE ( 'NONE', #5122, 2.500000000000000000 ) ;
#17638=CARTESIAN_POINT ( 'NONE',  ( 0.3058872367615230181, 12.87003593440634930, -4.821066432589193873 ) ) ;
#17639=CARTESIAN_POINT ( 'NONE',  ( 16.56822296793089322, 0.009847136207495308519, -0.002414375228568875487 ) ) ;
#17641=CARTESIAN_POINT ( 'NONE',  ( 2.123976203522053297, -10.37815841598499667, 11.67822624909921814 ) ) ;
#17644=CARTESIAN_POINT ( 'NONE',  ( 3.950837973638675393, -6.888253895133384930, 12.81214529934972823 ) ) ;
#17646=CARTESIAN_POINT ( 'NONE',  ( 0.3095370825347224519, -13.73357284481724427, -0.4597470195091612477 ) ) ;
#17652=CARTESIAN_POINT ( 'NONE',  ( 0.3151928476913555821, 0.0002082997483780314805, 13.73922860838472104 ) ) ;
#17656=B_SPLINE_CURVE_WITH_KNOTS ( 'NONE', 3,
 ( #4952, #18137, #6671, #2094, #5037, #8016 ),
 .UNSPECIFIED., .F., .F.,
 ( 4, 2, 4 ),
 ( 0.000000000000000000, 0.001500839035891551572, 0.003001678071783103145 ),
 .UNSPECIFIED. ) ;
#17659=VERTEX_POINT ( 'NONE', #457 ) ;
#17666=CARTESIAN_POINT ( 'NONE',  ( 16.56872352241294521, -0.004907101719994693724, 0.009207754980063731845 ) ) ;
#17669=CARTESIAN_POINT ( 'NONE',  ( 1.847426409206450959, 1.966388007708274189E-11, -12.44303504652081038 ) ) ;
#17673=CARTESIAN_POINT ( 'NONE',  ( 0.3150686449036065317, -8.199336701264455129, -11.02450593298027570 ) ) ;
#17676=VERTEX_POINT ( 'NONE', #6386 ) ;
#17678=ORIENTED_EDGE ( 'NONE', *, *, #5449, .F. ) ;
#17680=CARTESIAN_POINT ( 'NONE',  ( 1.861628059977118888, 9.751736252960505169, 7.751680370224894645 ) ) ;
#17681=ORIENTED_EDGE ( 'NONE', *, *, #10761, .T. ) ;
#17682=CARTESIAN_POINT ( 'NONE',  ( 2.320520222538116961, 10.64885284335071169, -11.60169517779341852 ) ) ;
#17683=CARTESIAN_POINT ( 'NONE',  ( 16.56679352167444819, 0.008252760440870499439, 0.004277682826582289259 ) ) ;
#17688=CARTESIAN_POINT ( 'NONE',  ( 16.56753206892534891, 0.008490833999798923920, 0.004253784598196209618 ) ) ;
#17689=CARTESIAN_POINT ( 'NONE',  ( 1.846822687350018644, -10.23524390843944687, 7.075150813727085541 ) ) ;
#17691=CARTESIAN_POINT ( 'NONE',  ( 2.320521194582547242, 1.795798718313595055, 15.64520804578271118 ) ) ;
#17693=EDGE_CURVE ( 'NONE', #17138, #6541, #8100, .T. ) ;
#17696=B_SPLINE_CURVE_WITH_KNOTS ( 'NONE', 3,
 ( #14621, #10232, #7, #14716, #13477, #392 ),
 .UNSPECIFIED., .F., .F.,
 ( 4, 2, 4 ),
 ( 7.047314121155778821E-19, 0.001657017934710171237, 0.003314035869420342041 ),
 .UNSPECIFIED. ) ;
#17704=CARTESIAN_POINT ( 'NONE',  ( 0.3170788640506440603, 8.200855617524691610, -11.02668139258432944 ) ) ;
#17710=CARTESIAN_POINT ( 'NONE',  ( 0.3095370825347224519, 12.91933430393614302, -4.681152801286025955 ) ) ;
#17712=CARTESIAN_POINT ( 'NONE',  ( 2.636624412714756005, -2.161493821597335607, 15.91454522070219113 ) ) ;
#17715=VERTEX_POINT ( 'NONE', #6756 ) ;
#17722=CARTESIAN_POINT ( 'NONE',  ( 2.123976203522053741, -7.899625852120303549, 13.47898556379310087 ) ) ;
#17724=ORIENTED_EDGE ( 'NONE', *, *, #13421, .F. ) ;
#17725=ADVANCED_FACE ( 'NONE', ( #5403 ), #18157, .F. ) ;
#17728=ORIENTED_EDGE ( 'NONE', *, *, #14818, .F. ) ;
#17729=CARTESIAN_POINT ( 'NONE',  ( 2.002547531651519996, -12.17374746633580784, 3.242439124566603326 ) ) ;
#17730=ORIENTED_EDGE ( 'NONE', *, *, #15789, .T. ) ;
#17731=CARTESIAN_POINT ( 'NONE',  ( 0.3058872367615226295, 13.72992299905060065, 0.6080468242581433813 ) ) ;
#17732=CARTESIAN_POINT ( 'NONE',  ( 16.56753206892534891, 0.008432171035096382855, 0.004368917149004273269 ) ) ;
#17734=CARTESIAN_POINT ( 'NONE',  ( 0.3151928476913582466, 4.245853234426384404, 13.06671852871090778 ) ) ;
#17737=( BOUNDED_SURFACE ( )  B_SPLINE_SURFACE ( 3, 1, ( 
 ( #14470, #8840 ),
 ( #1383, #5767 ),
 ( #10370, #2796 ),
 ( #11611, #1283 ) ),
 .UNSPECIFIED., .F., .F., .T. ) 
 B_SPLINE_SURFACE_WITH_KNOTS ( ( 4, 4 ),
 ( 2, 2 ),
 ( 0.000000000000000000, 1.000000000000000000 ),
 ( 0.000000000000000000, 1.000000000000000000 ),
 .UNSPECIFIED. ) 
 GEOMETRIC_REPRESENTATION_ITEM ( )  RATIONAL_B_SPLINE_SURFACE ( (
 ( 1.000000000000000000, 1.000000000000000000),
 ( 0.9593108457356467333, 0.9995965569486454649),
 ( 0.9593108457356467333, 0.9995965569486454649),
 ( 1.000000000000000000, 1.000000000000000000) ) ) 
 REPRESENTATION_ITEM ( '' )  SURFACE ( )  );
#17740=CARTESIAN_POINT ( 'NONE',  ( 1.846138399168762101, 6.971848976711159551, -10.30487220521562541 ) ) ;
#17741=CARTESIAN_POINT ( 'NONE',  ( 3.512766787570759330, -7.127386085302901186, 13.25664064834469968 ) ) ;
#17742=EDGE_CURVE ( 'NONE', #5687, #4624, #18396, .T. ) ;
#17746=ORIENTED_EDGE ( 'NONE', *, *, #3927, .F. ) ;
#17747=B_SPLINE_CURVE_WITH_KNOTS ( 'NONE', 3,
 ( #6407, #10616, #4683, #3228, #17781, #7564, #3129, #12043, #4967, #9264, #12236, #3331, #18062 ),
 .UNSPECIFIED., .F., .F.,
 ( 4, 3, 3, 3, 4 ),
 ( 1.734723475976807094E-18, 0.0002299780670421060647, 0.0004599561239687893072, 0.0006896788984287890393, 0.0009194956271626404968 ),
 .UNSPECIFIED. ) ;
#17748=ORIENTED_EDGE ( 'NONE', *, *, #664, .T. ) ;
#17753=CARTESIAN_POINT ( 'NONE',  ( 1.918918678667046684, -7.860057224348774518, -9.738328798462466906 ) ) ;
#17754=ORIENTED_EDGE ( 'NONE', *, *, #14925, .T. ) ;
#17759=CARTESIAN_POINT ( 'NONE',  ( 0.3095370825347233956, -4.681152801286073917, -12.91933430393612525 ) ) ;
#17760=CARTESIAN_POINT ( 'NONE',  ( 1.846955891736114852, 12.44001089941741611, -0.2634721419535633880 ) ) ;
#17766=ORIENTED_EDGE ( 'NONE', *, *, #6998, .T. ) ;
#17771=ORIENTED_EDGE ( 'NONE', *, *, #16834, .T. ) ;
#17773=VERTEX_POINT ( 'NONE', #5304 ) ;
#17774=CARTESIAN_POINT ( 'NONE',  ( 1.959212340397945562, -6.829000156128106624, -10.53510106265289359 ) ) ;
#17775=CARTESIAN_POINT ( 'NONE',  ( 1.846822687350018422, 11.74004266906804617, 4.121816957446238661 ) ) ;
#17776=CARTESIAN_POINT ( 'NONE',  ( 16.56872352241294521, -0.009207754980064163791, 0.004907101719995779661 ) ) ;
#17778=CARTESIAN_POINT ( 'NONE',  ( 8.522092701127531811, 2.505958102592713121, -6.489356537178164075 ) ) ;
#17781=CARTESIAN_POINT ( 'NONE',  ( 0.3150692679895996107, 13.01874238516610482, 4.391039771493711719 ) ) ;
#17783=CARTESIAN_POINT ( 'NONE',  ( 0.3095370825347234511, 12.91933430393608084, 4.681152801286207144 ) ) ;
#17785=LINE ( 'NONE', #7758, #3157 ) ;
#17787=ORIENTED_EDGE ( 'NONE', *, *, #434, .F. ) ;
#17788=B_SPLINE_CURVE_WITH_KNOTS ( 'NONE', 3,
 ( #13322, #2985, #6363, #430, #7801, #534 ),
 .UNSPECIFIED., .F., .F.,
 ( 4, 2, 4 ),
 ( 2.622335209753013447E-18, 0.0002017457492448088824, 0.0004034914984896151085 ),
 .UNSPECIFIED. ) ;
#17789=VECTOR ( 'NONE', #1376, 1000.000000000000000 ) ;
#17794=CARTESIAN_POINT ( 'NONE',  ( 3.377929128793395908, -13.92579934231096495, 1.296196549818894539 ) ) ;
#17800=CARTESIAN_POINT ( 'NONE',  ( 0.4385251269669958596, -12.93791070501030660, -4.978066129061825329 ) ) ;
#17803=CARTESIAN_POINT ( 'NONE',  ( 0.4754618798421171855, 7.564402563418640035, -11.68486377711958291 ) ) ;
#17806=CARTESIAN_POINT ( 'NONE',  ( 1.342453679581834924, 13.74702459364891993, -5.476372339889874041 ) ) ;
#17807=VERTEX_POINT ( 'NONE', #11151 ) ;
#17809=CARTESIAN_POINT ( 'NONE',  ( 2.123976203522053297, -13.47898556379318435, 7.899625852120161440 ) ) ;
#17811=CARTESIAN_POINT ( 'NONE',  ( 16.56753206892534891, 0.006669401563385194548, 0.006760771273035138390 ) ) ;
#17815=CARTESIAN_POINT ( 'NONE',  ( 0.3137051932979809665, -3.805684345189881856, 13.20008686438104739 ) ) ;
#17820=EDGE_CURVE ( 'NONE', #11554, #14601, #3780, .T. ) ;
#17827=CARTESIAN_POINT ( 'NONE',  ( 0.4754618798421162973, -13.89949764182683190, 0.7484603771383941950 ) ) ;
#17829=CARTESIAN_POINT ( 'NONE',  ( 1.977228804423231345, 7.806978995470744032, -13.27756617201399969 ) ) ;
#17831=DIRECTION ( 'NONE',  ( 0.000000000000000000, 0.000000000000000000, -1.000000000000000000 ) ) ;
#17832=CARTESIAN_POINT ( 'NONE',  ( 0.3095370825347234511, -4.681152801286254217, 12.91933430393606486 ) ) ;
#17833=DIRECTION ( 'NONE',  ( 1.000000000000000000, 0.000000000000000000, 0.000000000000000000 ) ) ;
#17834=CARTESIAN_POINT ( 'NONE',  ( 0.3095370825347224519, -11.38092634279633941, 7.700448427571837229 ) ) ;
#17839=ADVANCED_FACE ( 'NONE', ( #1281 ), #7045, .F. ) ;
#17843=ORIENTED_EDGE ( 'NONE', *, *, #14672, .F. ) ;
#17844=ORIENTED_EDGE ( 'NONE', *, *, #9482, .F. ) ;
#17847=CARTESIAN_POINT ( 'NONE',  ( 3.950837973638675393, -13.10350451991835818, -6.316429227969608817 ) ) ;
#17850=DIRECTION ( 'NONE',  ( 0.000000000000000000, 0.000000000000000000, 1.000000000000000000 ) ) ;
#17853=CARTESIAN_POINT ( 'NONE',  ( 1.847034903785822690, 12.44051878787773191, 0.2299360331934612034 ) ) ;
#17862=ORIENTED_EDGE ( 'NONE', *, *, #9133, .F. ) ;
#17867=EDGE_LOOP ( 'NONE', ( #17358, #16569, #15364, #4093 ) ) ;
#17871=CARTESIAN_POINT ( 'NONE',  ( 1.254255976357838698, 9.426444230097315469, -11.25336128106935973 ) ) ;
#17874=LINE ( 'NONE', #6403, #7811 ) ;
#17879=CARTESIAN_POINT ( 'NONE',  ( 16.57778382496167424, 0.01354073047775767452, 0.006312874906843726416 ) ) ;
#17884=CIRCLE ( 'NONE', #488, 14.54644660717763927 ) ;
#17887=CARTESIAN_POINT ( 'NONE',  ( 1.977228804422057395, -11.52787183731166820, 10.21522664410399095 ) ) ;
#17888=CARTESIAN_POINT ( 'NONE',  ( 2.002547531651519996, -9.778737580845755062, 7.942910686618138705 ) ) ;
#17889=ORIENTED_EDGE ( 'NONE', *, *, #8543, .F. ) ;
#17898=CARTESIAN_POINT ( 'NONE',  ( 0.3058872367615230181, 13.72992299905060065, -0.6080468242581438254 ) ) ;
#17899=CARTESIAN_POINT ( 'NONE',  ( 16.56753206892534891, -0.004253784598196824578, -0.008490833999797990639 ) ) ;
#17900=CARTESIAN_POINT ( 'NONE',  ( 16.57778382496167424, -0.002851818597093308278, -0.01466529584256674387 ) ) ;
#17905=CARTESIAN_POINT ( 'NONE',  ( 0.4862570985993235340, 7.559321496869593204, -11.67702470553357053 ) ) ;
#17906=B_SPLINE_CURVE_WITH_KNOTS ( 'NONE', 3,
 ( #12963, #8484, #13062, #7251, #4190, #10103 ),
 .UNSPECIFIED., .F., .F.,
 ( 4, 2, 4 ),
 ( 2.438852479171459636E-18, 0.001657017934711444091, 0.003314035869422886013 ),
 .UNSPECIFIED. ) ;
#17907=VECTOR ( 'NONE', #7223, 1000.000000000000114 ) ;
#17912=ORIENTED_EDGE ( 'NONE', *, *, #3209, .F. ) ;
#17913=CARTESIAN_POINT ( 'NONE',  ( 0.3145729642390363567, -7.825496023201391260, 11.29233589755989797 ) ) ;
#17916=ORIENTED_EDGE ( 'NONE', *, *, #12774, .T. ) ;
#17921=CARTESIAN_POINT ( 'NONE',  ( 2.002547531651519996, 3.242439124566649511, 12.17374746633579541 ) ) ;
#17922=VERTEX_POINT ( 'NONE', #9032 ) ;
#17923=VECTOR ( 'NONE', #2852, 1000.000000000000227 ) ;
#17930=CARTESIAN_POINT ( 'NONE',  ( 0.3720661004400037664, -3.575426119359092159, -13.34435358167256247 ) ) ;
#17932=LINE ( 'NONE', #6455, #8936 ) ;
#17933=CARTESIAN_POINT ( 'NONE',  ( 1.846138399168762101, -11.69739621335919111, -4.238866729160527314 ) ) ;
#17938=CARTESIAN_POINT ( 'NONE',  ( 0.4862570985993235340, -13.89016912371016943, -0.7479633556563904939 ) ) ;
#17944=ORIENTED_EDGE ( 'NONE', *, *, #3443, .T. ) ;
#17948=B_SPLINE_CURVE_WITH_KNOTS ( 'NONE', 3,
 ( #7802, #7992, #2324, #5283, #11129, #3378 ),
 .UNSPECIFIED., .F., .F.,
 ( 4, 2, 4 ),
 ( 1.951563910473907981E-18, 0.0002017457492448081235, 0.0004034914984896142954 ),
 .UNSPECIFIED. ) ;
#17949=CARTESIAN_POINT ( 'NONE',  ( 0.4862570985993235340, -13.89016912371016943, -0.7479633556563904939 ) ) ;
#17950=CARTESIAN_POINT ( 'NONE',  ( 2.002547531651519996, -3.242439124566566910, -12.17374746633581495 ) ) ;
#17951=CARTESIAN_POINT ( 'NONE',  ( 0.4385251269669948049, 13.84299131624729817, 0.7363879510385874516 ) ) ;
#17952=CARTESIAN_POINT ( 'NONE',  ( 3.950837973638677170, -14.31366178983255466, 2.591948120961746760 ) ) ;
#17958=CARTESIAN_POINT ( 'NONE',  ( 2.636624412714237309, 15.80357026013209953, 2.862162146984226663 ) ) ;
#17959=CARTESIAN_POINT ( 'NONE',  ( 16.56679352167444819, -0.001518074900131792136, -0.009170718284672557674 ) ) ;
#17963=ADVANCED_FACE ( 'NONE', ( #17531 ), #18867, .F. ) ;
#17964=VERTEX_POINT ( 'NONE', #8927 ) ;
#17965=ORIENTED_EDGE ( 'NONE', *, *, #10100, .F. ) ;
#17968=EDGE_CURVE ( 'NONE', #17143, #14747, #10465, .T. ) ;
#17969=CARTESIAN_POINT ( 'NONE',  ( 2.697797270744666687, -10.19107313879051269, -8.537712152180978009 ) ) ;
#17970=CARTESIAN_POINT ( 'NONE',  ( 3.512766787570692273, -2.682019731918297012, -14.81029789862167867 ) ) ;
#17971=CARTESIAN_POINT ( 'NONE',  ( 2.002547531651519996, -12.57989064830759141, -0.6781519942173057647 ) ) ;
#17977=CARTESIAN_POINT ( 'NONE',  ( 3.950837973638677170, -1.958075594453692503, -14.41405733518062959 ) ) ;
#17979=CARTESIAN_POINT ( 'NONE',  ( 0.3145734862173233393, 13.15783074029284272, -3.953068532979860272 ) ) ;
#17980=EDGE_LOOP ( 'NONE', ( #4656, #3419, #10261, #4845 ) ) ;
#17981=CARTESIAN_POINT ( 'NONE',  ( 1.254255976357308233, 13.61551404021196277, 5.487601330834896096 ) ) ;
#17982=CARTESIAN_POINT ( 'NONE',  ( 1.847461586945734702, 11.82388984758123840, -3.877048136045254001 ) ) ;
#17986=CARTESIAN_POINT ( 'NONE',  ( 0.4384471787762801442, 10.76632603192799742, -8.732395932355569101 ) ) ;
#17991=ORIENTED_EDGE ( 'NONE', *, *, #2623, .F. ) ;
#17992=CARTESIAN_POINT ( 'NONE',  ( 0.3170788640506440603, 13.11595226728163510, -4.100430649997826471 ) ) ;
#17994=DIRECTION ( 'NONE',  ( -1.000000000000000000, 0.000000000000000000, 0.000000000000000000 ) ) ;
#17995=CARTESIAN_POINT ( 'NONE',  ( 3.950837973638676281, -6.316429227969562632, 13.10350451991838128 ) ) ;
#17996=EDGE_LOOP ( 'NONE', ( #7046, #397, #14136, #11739 ) ) ;
#18002=VERTEX_POINT ( 'NONE', #12194 ) ;
#18005=CARTESIAN_POINT ( 'NONE',  ( 0.3151928476913556376, -8.075547435847033384, 11.11539186930584044 ) ) ;
#18006=LINE ( 'NONE', #616, #8769 ) ;
#18013=CARTESIAN_POINT ( 'NONE',  ( 2.636624412714236865, 0.000000000000000000, 0.000000000000000000 ) ) ;
#18015=CARTESIAN_POINT ( 'NONE',  ( 0.3095370825347224519, 7.700448427571875420, 11.38092634279631099 ) ) ;
#18017=DIRECTION ( 'NONE',  ( 0.000000000000000000, 0.000000000000000000, 1.000000000000000000 ) ) ;
#18018=CARTESIAN_POINT ( 'NONE',  ( 2.320521194581854907, 15.64520804578206281, -1.795798718312993758 ) ) ;
#18020=CARTESIAN_POINT ( 'NONE',  ( 0.3151928479966097374, 1.775918418904422640E-15, 13.73922861026898623 ) ) ;
#18022=CARTESIAN_POINT ( 'NONE',  ( 1.342453679581834924, -5.476372339889922003, -13.74702459364890039 ) ) ;
#18023=CARTESIAN_POINT ( 'NONE',  ( 0.3308579732647004001, 0.5950689966506276241, -13.74211098745268345 ) ) ;
#18024=CARTESIAN_POINT ( 'NONE',  ( 0.3148213771069364175, 7.888490156175222090, 11.24846294176314387 ) ) ;
#18025=CARTESIAN_POINT ( 'NONE',  ( 1.254255976357675717, -14.64488542023465101, -1.011593778944541278 ) ) ;
#18027=CARTESIAN_POINT ( 'NONE',  ( 16.56872352241294521, 0.001442253899401802278, 0.01033355228142402403 ) ) ;
#18032=ORIENTED_EDGE ( 'NONE', *, *, #9379, .T. ) ;
#18034=ORIENTED_EDGE ( 'NONE', *, *, #8059, .T. ) ;
#18035=EDGE_CURVE ( 'NONE', #3873, #13478, #10640, .T. ) ;
#18037=CARTESIAN_POINT ( 'NONE',  ( 0.4385251269669978580, 4.978066129061869738, -12.93791070501029239 ) ) ;
#18039=PRODUCT_DEFINITION_CONTEXT ( 'detailed design', #826, 'design' ) ;
#18040=ORIENTED_EDGE ( 'NONE', *, *, #950, .F. ) ;
#18044=DIRECTION ( 'NONE',  ( 0.7635533937278216055, -0.6453904417649387604, -0.02138673900302107828 ) ) ;
#18046=B_SPLINE_CURVE_WITH_KNOTS ( 'NONE', 3,
 ( #1148, #8509, #9748, #15572 ),
 .UNSPECIFIED., .F., .F.,
 ( 4, 4 ),
 ( 0.000000000000000000, 0.002004993803842713366 ),
 .UNSPECIFIED. ) ;
#18049=SHAPE_REPRESENTATION ( 'straight miter gear_iso_ISO - Straight miter gear 1.5M20T 20PA 2FW ---20O5H16.576MD5.0N', ( #2030 ), #15178 ) ;
#18056=EDGE_CURVE ( 'NONE', #9556, #17715, #3554, .T. ) ;
#18059=DIRECTION ( 'NONE',  ( -1.000000000000000000, -0.000000000000000000, -0.000000000000000000 ) ) ;
#18062=CARTESIAN_POINT ( 'NONE',  ( 0.3137051932979792457, 13.20008686438105983, 3.805684345189833451 ) ) ;
#18064=CARTESIAN_POINT ( 'NONE',  ( 1.846138399168762101, -10.30487220521574976, 6.971848976710974810 ) ) ;
#18068=CARTESIAN_POINT ( 'NONE',  ( 0.3145734862173240054, 0.3064017202077272128, -13.73540602248380971 ) ) ;
#18070=EDGE_LOOP ( 'NONE', ( #7857, #8400, #5063, #15682 ) ) ;
#18073=ORIENTED_EDGE ( 'NONE', *, *, #13966, .T. ) ;
#18075=CIRCLE ( 'NONE', #6788, 2.500000000000000000 ) ;
#18076=EDGE_CURVE ( 'NONE', #6766, #181, #8331, .T. ) ;
#18085=CARTESIAN_POINT ( 'NONE',  ( 1.861706995891670546, -12.00328602385077659, -3.332865258614104320 ) ) ;
#18091=CARTESIAN_POINT ( 'NONE',  ( 2.002547531651519996, 10.57595306287302250, -6.845637710436074386 ) ) ;
#18092=EDGE_LOOP ( 'NONE', ( #9486, #9699, #12785, #16507 ) ) ;
#18097=CARTESIAN_POINT ( 'NONE',  ( 0.8740764193768466583, -11.05257066464528748, -9.070946295054149289 ) ) ;
#18104=CARTESIAN_POINT ( 'NONE',  ( 3.074695600507308946, 2.093687500611960850, 15.41438262616221522 ) ) ;
#18109=DIRECTION ( 'NONE',  ( -1.000000000000000000, -0.000000000000000000, -0.000000000000000000 ) ) ;
#18111=CARTESIAN_POINT ( 'NONE',  ( 16.56872352241294521, -0.01033355228142402750, 0.001442253899401767583 ) ) ;
#18125=CARTESIAN_POINT ( 'NONE',  ( 0.3151926232592466848, 11.16039997398654116, 8.013596737356428079 ) ) ;
#18128=CARTESIAN_POINT ( 'NONE',  ( 8.438534575730034959, -5.688336279099072357, 3.845978796786017284 ) ) ;
#18131=EDGE_CURVE ( 'NONE', #381, #9516, #11078, .T. ) ;
#18132=CARTESIAN_POINT ( 'NONE',  ( 3.950837973638676281, -12.81214529934979929, 6.888253895133251703 ) ) ;
#18134=VECTOR ( 'NONE', #6966, 1000.000000000000227 ) ;
#18135=CARTESIAN_POINT ( 'NONE',  ( 2.636624412716062515, -6.973567714909003179, -14.46769361191335790 ) ) ;
#18137=CARTESIAN_POINT ( 'NONE',  ( 2.353870697619111496, 3.268530966681629568, 12.53036919722785925 ) ) ;
#18142=VERTEX_POINT ( 'NONE', #5718 ) ;
#18144=CARTESIAN_POINT ( 'NONE',  ( 16.57210152137263393, 0.009075239946108201033, -0.01136813053532078656 ) ) ;
#18150=EDGE_LOOP ( 'NONE', ( #9698, #3347, #18233, #5300 ) ) ;
#18154=FACE_OUTER_BOUND ( 'NONE', #1823, .T. ) ;
#18155=CARTESIAN_POINT ( 'NONE',  ( 3.950837973638668288, 0.000000000000000000, 0.000000000000000000 ) ) ;
#18156=CARTESIAN_POINT ( 'NONE',  ( 0.3151926232592466293, 13.04305446098362253, -4.318679262939488339 ) ) ;
#18157=( BOUNDED_SURFACE ( )  B_SPLINE_SURFACE ( 3, 1, ( 
 ( #15528, #14095 ),
 ( #2614, #11426 ),
 ( #9704, #17246 ),
 ( #5573, #9980 ) ),
 .UNSPECIFIED., .F., .F., .T. ) 
 B_SPLINE_SURFACE_WITH_KNOTS ( ( 4, 4 ),
 ( 2, 2 ),
 ( 0.000000000000000000, 1.000000000000000000 ),
 ( 0.000000000000000000, 1.000000000000000000 ),
 .UNSPECIFIED. ) 
 GEOMETRIC_REPRESENTATION_ITEM ( )  RATIONAL_B_SPLINE_SURFACE ( (
 ( 1.000000000000000000, 1.000000000000000000),
 ( 0.9933953342250436691, 0.8357391271907733676),
 ( 0.9933953342250436691, 0.8357391271907733676),
 ( 1.000000000000000000, 1.000000000000000000) ) ) 
 REPRESENTATION_ITEM ( '' )  SURFACE ( )  );
#18159=CIRCLE ( 'NONE', #1045, 16.06066017081991149 ) ;
#18160=ORIENTED_EDGE ( 'NONE', *, *, #4504, .F. ) ;
#18164=ORIENTED_EDGE ( 'NONE', *, *, #5885, .T. ) ;
#18165=CARTESIAN_POINT ( 'NONE',  ( 2.002547531651519996, 11.75462648437108015, -4.532360870844206246 ) ) ;
#18167=B_SPLINE_CURVE_WITH_KNOTS ( 'NONE', 3,
 ( #5271, #8251, #12352, #792, #11025, #3745, #18188, #11115, #9399, #3842, #9671, #15228, #2398 ),
 .UNSPECIFIED., .F., .F.,
 ( 4, 3, 3, 3, 4 ),
 ( 4.906538933386797396E-18, 0.0002299780670421066068, 0.0004599561239687925598, 0.0006896788984287864372, 0.0009194956271626387621 ),
 .UNSPECIFIED. ) ;
#18170=CARTESIAN_POINT ( 'NONE',  ( 2.002547531651519996, -4.532360870844247991, -11.75462648437106417 ) ) ;
#18172=EDGE_LOOP ( 'NONE', ( #18231, #1063, #15853, #2720 ) ) ;
#18174=CARTESIAN_POINT ( 'NONE',  ( 8.438534575730034959, -5.688336279099016402, -3.845978796786099885 ) ) ;
#18180=CARTESIAN_POINT ( 'NONE',  ( 1.846138399168762989, -3.446241763653083101, 11.95493567637849530 ) ) ;
#18181=EDGE_CURVE ( 'NONE', #13031, #8021, #6568, .T. ) ;
#18183=CARTESIAN_POINT ( 'NONE',  ( 0.4754618798421162973, -10.80499583390518836, 8.775436892861078420 ) ) ;
#18184=CARTESIAN_POINT ( 'NONE',  ( 1.861628059977342042, 10.38573835516722355, -6.879051339207178373 ) ) ;
#18188=CARTESIAN_POINT ( 'NONE',  ( 0.3151928476913571364, -11.11539186930580669, -8.075547435847068911 ) ) ;
#18191=ORIENTED_EDGE ( 'NONE', *, *, #4468, .T. ) ;
#18197=DIRECTION ( 'NONE',  ( -0.000000000000000000, 0.000000000000000000, 1.000000000000000000 ) ) ;
#18198=DIRECTION ( 'NONE',  ( 0.7561779333270775005, -0.4122479608995778255, 0.5081796452863200919 ) ) ;
#18200=FACE_BOUND ( 'NONE', #3120, .T. ) ;
#18206=CARTESIAN_POINT ( 'NONE',  ( 0.3720661004400040439, -12.89739157014196635, 4.951033743989591507 ) ) ;
#18207=CARTESIAN_POINT ( 'NONE',  ( 1.977436885026099711, -15.33079650480437550, -1.488549889122204650 ) ) ;
#18210=EDGE_LOOP ( 'NONE', ( #7257, #7428, #4887, #15114 ) ) ;
#18213=ORIENTED_EDGE ( 'NONE', *, *, #1779, .T. ) ;
#18220=B_SPLINE_CURVE_WITH_KNOTS ( 'NONE', 3,
 ( #6452, #2411, #8172, #3479, #894, #3575 ),
 .UNSPECIFIED., .F., .F.,
 ( 4, 2, 4 ),
 ( 0.000000000000000000, 0.0001828790815886942919, 0.0003657581631773885837 ),
 .UNSPECIFIED. ) ;
#18223=CARTESIAN_POINT ( 'NONE',  ( 1.846138399168762101, -9.815003036200465658, 7.646096044339859787 ) ) ;
#18231=ORIENTED_EDGE ( 'NONE', *, *, #351, .F. ) ;
#18233=ORIENTED_EDGE ( 'NONE', *, *, #1262, .T. ) ;
#18238=EDGE_CURVE ( 'NONE', #11022, #13051, #10353, .T. ) ;
#18242=CARTESIAN_POINT ( 'NONE',  ( 3.074695600507125981, -2.772091048739183439, -15.30693405987811673 ) ) ;
#18243=CARTESIAN_POINT ( 'NONE',  ( 2.353870697619111496, -4.720869121224215093, 12.05847592522641953 ) ) ;
#18247=CARTESIAN_POINT ( 'NONE',  ( 1.847412631396500693, -11.82061107079961992, -3.886120457021520647 ) ) ;
#18255=ORIENTED_EDGE ( 'NONE', *, *, #6047, .T. ) ;
#18257=VERTEX_POINT ( 'NONE', #17977 ) ;
#18261=CARTESIAN_POINT ( 'NONE',  ( 1.846138399168762101, -3.446241763652916124, -11.95493567637853971 ) ) ;
#18263=EDGE_CURVE ( 'NONE', #1860, #349, #6026, .T. ) ;
#18264=ORIENTED_EDGE ( 'NONE', *, *, #491, .F. ) ;
#18267=EDGE_CURVE ( 'NONE', #1614, #4817, #3056, .T. ) ;
#18268=DIRECTION ( 'NONE',  ( -1.000000000000000000, -0.000000000000000000, -0.000000000000000000 ) ) ;
#18272=( NAMED_UNIT ( * ) PLANE_ANGLE_UNIT ( ) SI_UNIT ( $, .RADIAN. ) );
#18279=CARTESIAN_POINT ( 'NONE',  ( 0.3137051932979792457, -13.73004976592202375, 0.4596302728639276580 ) ) ;
#18280=CARTESIAN_POINT ( 'NONE',  ( 0.4754618798421171855, -0.7484603771383426807, -13.89949764182683545 ) ) ;
#18282=EDGE_LOOP ( 'NONE', ( #17787, #12978, #10604, #13453 ) ) ;
#18283=ORIENTED_EDGE ( 'NONE', *, *, #12187, .T. ) ;
#18284=DIRECTION ( 'NONE',  ( 0.7635533937278214944, -0.6071939193889578368, -0.2197766120036483140 ) ) ;
#18285=DIRECTION ( 'NONE',  ( -1.000000000000000000, -0.000000000000000000, -0.000000000000000000 ) ) ;
#18286=ORIENTED_EDGE ( 'NONE', *, *, #3323, .F. ) ;
#18295=CARTESIAN_POINT ( 'NONE',  ( 0.3151928476913565258, -13.06671852871092199, 4.245853234426333778 ) ) ;
#18296=CARTESIAN_POINT ( 'NONE',  ( 0.3095370825347233956, -12.91933430393611104, 4.681152801286112997 ) ) ;
#18298=ADVANCED_FACE ( 'NONE', ( #3431 ), #3115, .F. ) ;
#18300=DIRECTION ( 'NONE',  ( 0.7561779333270775005, 0.3559159372837274460, 0.5491072561318377510 ) ) ;
#18301=CARTESIAN_POINT ( 'NONE',  ( 8.438534575730034959, 5.415535776177581972, -4.221456476902606170 ) ) ;
#18311=CARTESIAN_POINT ( 'NONE',  ( 0.4862570985993235340, -7.559321496869506163, 11.67702470553362559 ) ) ;
#18314=CARTESIAN_POINT ( 'NONE',  ( 3.074695600508143833, 13.70113613813285269, 7.366518011945069055 ) ) ;
#18315=CARTESIAN_POINT ( 'NONE',  ( 2.002547531651519996, -7.942910686618240845, 9.778737580845669797 ) ) ;
#18323=CIRCLE ( 'NONE', #326, 16.06066017081991149 ) ;
#18324=CARTESIAN_POINT ( 'NONE',  ( 16.56872352241294521, -0.001442253899401298341, 0.01033355228142499027 ) ) ;
#18325=CARTESIAN_POINT ( 'NONE',  ( 2.002547531651519996, 12.17374746633582561, -3.242439124566524278 ) ) ;
#18327=CARTESIAN_POINT ( 'NONE',  ( 0.4384471787762835859, 13.39294437382618419, 3.577367180593594043 ) ) ;
#18329=CARTESIAN_POINT ( 'NONE',  ( 0.3720661004400040439, -8.694226082900513575, -10.73619472937711983 ) ) ;
#18336=CARTESIAN_POINT ( 'NONE',  ( 0.3151928479966099039, 0.07658992383256929548, -13.73922861026898623 ) ) ;
#18337=( BOUNDED_SURFACE ( )  B_SPLINE_SURFACE ( 3, 1, ( 
 ( #2258, #4949 ),
 ( #4858, #2092 ),
 ( #3605, #832 ),
 ( #737, #8105 ) ),
 .UNSPECIFIED., .F., .F., .T. ) 
 B_SPLINE_SURFACE_WITH_KNOTS ( ( 4, 4 ),
 ( 2, 2 ),
 ( 0.000000000000000000, 1.000000000000000000 ),
 ( 0.000000000000000000, 1.000000000000000000 ),
 .UNSPECIFIED. ) 
 GEOMETRIC_REPRESENTATION_ITEM ( )  RATIONAL_B_SPLINE_SURFACE ( (
 ( 1.000000000000000000, 1.000000000000000000),
 ( 0.9933953342250438912, 0.8357391271907739227),
 ( 0.9933953342250438912, 0.8357391271907739227),
 ( 1.000000000000000000, 1.000000000000000000) ) ) 
 REPRESENTATION_ITEM ( '' )  SURFACE ( )  );
#18344=ORIENTED_EDGE ( 'NONE', *, *, #10868, .T. ) ;
#18347=CARTESIAN_POINT ( 'NONE',  ( 1.847426409206450959, -2.029922383240494730E-11, 12.44303504652081038 ) ) ;
#18349=CARTESIAN_POINT ( 'NONE',  ( 2.002547531651519996, 4.532360870844494016, -11.75462648437097180 ) ) ;
#18352=CARTESIAN_POINT ( 'NONE',  ( 3.664313757352975376, 9.645155442698909454, -10.50730552161222597 ) ) ;
#18353=CARTESIAN_POINT ( 'NONE',  ( 0.3939822652208125331, -13.34132036472939831, 3.598529276937210142 ) ) ;
#18356=CARTESIAN_POINT ( 'NONE',  ( 0.3151928479966097929, -0.07658992383253612757, 13.73922861026898623 ) ) ;
#18358=CIRCLE ( 'NONE', #7698, 12.15840553252917289 ) ;
#18360=CARTESIAN_POINT ( 'NONE',  ( 2.636624412716062960, 2.862162146982868194, -15.80357026013419564 ) ) ;
#18361=EDGE_CURVE ( 'NONE', #8605, #17143, #11045, .T. ) ;
#18364=ORIENTED_EDGE ( 'NONE', *, *, #4338, .T. ) ;
#18367=CARTESIAN_POINT ( 'NONE',  ( 0.3150686449036048664, -4.391272911157235725, -13.01866258978841628 ) ) ;
#18368=EDGE_LOOP ( 'NONE', ( #958, #11423, #6198, #2080 ) ) ;
#18371=CARTESIAN_POINT ( 'NONE',  ( 2.002547531651519996, -6.845637710436110801, -10.57595306287299763 ) ) ;
#18380=CARTESIAN_POINT ( 'NONE',  ( 1.846138399168762101, 7.646096044339892650, 9.815003036200437236 ) ) ;
#18386=EDGE_CURVE ( 'NONE', #17057, #12585, #9449, .T. ) ;
#18390=B_SPLINE_CURVE_WITH_KNOTS ( 'NONE', 3,
 ( #18347, #15751, #7068, #11283, #16823, #15652, #12882, #5161, #3726, #2291 ),
 .UNSPECIFIED., .F., .F.,
 ( 4, 3, 3, 4 ),
 ( 0.0004168119862255878537, 0.0004599608082120251176, 0.0006467586077648016917, 0.0008336169836825990491 ),
 .UNSPECIFIED. ) ;
#18396=LINE ( 'NONE', #14008, #15714 ) ;
#18403=CARTESIAN_POINT ( 'NONE',  ( 16.56872352241294521, 0.004907101719994633009, -0.009207754980063766539 ) ) ;
#18425=EDGE_LOOP ( 'NONE', ( #18160, #14909, #2379, #14574 ) ) ;
#18428=CARTESIAN_POINT ( 'NONE',  ( 0.3720661004400040439, 8.694226082900595287, 10.73619472937705233 ) ) ;
#18429=CIRCLE ( 'NONE', #10193, 16.06066017081991149 ) ;
#18434=CARTESIAN_POINT ( 'NONE',  ( 1.918918678667044686, -4.466049546133833203, -11.69059232068582865 ) ) ;
#18435=CARTESIAN_POINT ( 'NONE',  ( 8.438534575730034959, 2.341351102130369011, -6.454982381540262715 ) ) ;
#18439=B_SPLINE_CURVE_WITH_KNOTS ( 'NONE', 3,
 ( #10407, #16242, #7655, #14899, #14991, #15090 ),
 .UNSPECIFIED., .F., .F.,
 ( 4, 2, 4 ),
 ( 8.673617379884035472E-19, 0.001500839035891548753, 0.003001678071783096639 ),
 .UNSPECIFIED. ) ;
#18441=DIRECTION ( 'NONE',  ( -0.7635533937278216055, -0.5347026451755912957, -0.3620487483322542555 ) ) ;
#18443=CARTESIAN_POINT ( 'NONE',  ( 2.123976203522053741, 15.26039569100260174, 3.347755036805956763 ) ) ;
#18447=CARTESIAN_POINT ( 'NONE',  ( 3.074695600507260984, -14.01296402267893448, 6.754521329824735076 ) ) ;
#18449=CARTESIAN_POINT ( 'NONE',  ( 1.846138399168762101, 11.69739621335927815, -4.238866729160283064 ) ) ;
#18452=CARTESIAN_POINT ( 'NONE',  ( 0.3170788640506440603, -11.02668139258435787, -8.200855617524654306 ) ) ;
#18463=EDGE_CURVE ( 'NONE', #9556, #12864, #3907, .T. ) ;
#18470=PRODUCT_CONTEXT ( 'NONE', #14862, 'mechanical' ) ;
#18474=VECTOR ( 'NONE', #2517, 1000.000000000000114 ) ;
#18483=EDGE_LOOP ( 'NONE', ( #12152, #13392, #6534, #14388 ) ) ;
#18492=CARTESIAN_POINT ( 'NONE',  ( 2.002547531651519996, 6.845637710436190737, 10.57595306287294612 ) ) ;
#18495=CARTESIAN_POINT ( 'NONE',  ( 16.58200780006414732, 0.01115192838421568376, 0.0006320991582350033409 ) ) ;
#18496=CARTESIAN_POINT ( 'NONE',  ( 2.636624412714236865, 0.000000000000000000, 0.000000000000000000 ) ) ;
#18497=EDGE_CURVE ( 'NONE', #14481, #4102, #17884, .T. ) ;
#18500=B_SPLINE_CURVE_WITH_KNOTS ( 'NONE', 3,
 ( #8055, #7876, #13863, #12255, #15301, #13688 ),
 .UNSPECIFIED., .F., .F.,
 ( 4, 2, 4 ),
 ( 0.000000000000000000, 0.001657017934710632240, 0.003314035869421264480 ),
 .UNSPECIFIED. ) ;
#18503=ORIENTED_EDGE ( 'NONE', *, *, #2782, .T. ) ;
#18508=CARTESIAN_POINT ( 'NONE',  ( 16.56822296793089322, -0.0007467251401297892322, -0.01011126603341077311 ) ) ;
#18514=CARTESIAN_POINT ( 'NONE',  ( 0.3137051932979792457, -11.37800749014136592, 7.698472063774431717 ) ) ;
#18517=VECTOR ( 'NONE', #17221, 1000.000000000000114 ) ;
#18523=EDGE_CURVE ( 'NONE', #17807, #16214, #5636, .T. ) ;
#18524=DIRECTION ( 'NONE',  ( -0.7561779333270775005, -0.6534392409364822019, 0.03481510524964565034 ) ) ;
#18526=CONICAL_SURFACE ( 'NONE', #16714, 14.54644660717763927, 0.8559913436420816257 ) ;
#18529=FACE_OUTER_BOUND ( 'NONE', #12535, .T. ) ;
#18536=CARTESIAN_POINT ( 'NONE',  ( 0.3095370825347233956, 13.20347358821914519, 3.806662003783457315 ) ) ;
#18537=VERTEX_POINT ( 'NONE', #16813 ) ;
#18540=CARTESIAN_POINT ( 'NONE',  ( 0.4862570985993235340, -11.67702470553359539, -7.559321496869553236 ) ) ;
#18544=( NAMED_UNIT ( * ) SI_UNIT ( $, .STERADIAN. ) SOLID_ANGLE_UNIT ( ) );
#18549=VERTEX_POINT ( 'NONE', #9545 ) ;
#18560=LINE ( 'NONE', #2682, #10672 ) ;
#18561=CARTESIAN_POINT ( 'NONE',  ( 1.845755665166724180, 7.694641135842960722, -9.776700214453546423 ) ) ;
#18562=LINE ( 'NONE', #12736, #18517 ) ;
#18568=EDGE_LOOP ( 'NONE', ( #7406, #1602, #15011, #8630 ) ) ;
#18570=CARTESIAN_POINT ( 'NONE',  ( 1.847461586945732925, 3.877048136045379234, 11.82388984758120287 ) ) ;
#18577=ORIENTED_EDGE ( 'NONE', *, *, #10379, .F. ) ;
#18579=CARTESIAN_POINT ( 'NONE',  ( 2.636624412714237309, 11.10302021257826866, 11.60464335004050973 ) ) ;
#18582=CARTESIAN_POINT ( 'NONE',  ( 0.3137051932979792457, -10.83767969834796929, -8.442169467526971616 ) ) ;
#18586=CARTESIAN_POINT ( 'NONE',  ( 1.342453679581834924, -9.456403821038714241, -11.38190519890864039 ) ) ;
#18588=CARTESIAN_POINT ( 'NONE',  ( 1.918918678667072442, -12.49849921341423276, 0.6348738215464800883 ) ) ;
#18594=B_SPLINE_CURVE_WITH_KNOTS ( 'NONE', 3,
 ( #584, #9366, #10515, #8978, #13376, #6209 ),
 .UNSPECIFIED., .F., .F.,
 ( 4, 2, 4 ),
 ( 8.673617379884035472E-19, 0.0001828790815886939666, 0.0003657581631773870658 ),
 .UNSPECIFIED. ) ;
#18597=FACE_OUTER_BOUND ( 'NONE', #18425, .T. ) ;
#18601=ORIENTED_EDGE ( 'NONE', *, *, #2524, .T. ) ;
#18602=CARTESIAN_POINT ( 'NONE',  ( 2.636624412714236865, 0.000000000000000000, 0.000000000000000000 ) ) ;
#18608=CARTESIAN_POINT ( 'NONE',  ( 0.4862570985993252548, 5.003653737315486794, 12.97920246947881395 ) ) ;
#18612=VERTEX_POINT ( 'NONE', #11273 ) ;
#18613=FACE_OUTER_BOUND ( 'NONE', #3593, .T. ) ;
#18614=EDGE_CURVE ( 'NONE', #492, #10356, #9900, .T. ) ;
#18615=ORIENTED_EDGE ( 'NONE', *, *, #10655, .T. ) ;
#18616=ADVANCED_FACE ( 'NONE', ( #11638 ), #11567, .F. ) ;
#18618=VERTEX_POINT ( 'NONE', #17366 ) ;
#18619=DIRECTION ( 'NONE',  ( 0.7561779333270775005, 0.5491072561318364187, -0.3559159372837296664 ) ) ;
#18621=FACE_OUTER_BOUND ( 'NONE', #6638, .T. ) ;
#18630=( LENGTH_UNIT ( ) NAMED_UNIT ( * ) SI_UNIT ( .MILLI., .METRE. ) );
#18637=ORIENTED_EDGE ( 'NONE', *, *, #16564, .T. ) ;
#18642=ORIENTED_EDGE ( 'NONE', *, *, #12615, .T. ) ;
#18647=CARTESIAN_POINT ( 'NONE',  ( 0.3308579732647051186, 3.680601586799872482, 13.25341063505876882 ) ) ;
#18650=EDGE_CURVE ( 'NONE', #17449, #2783, #9916, .T. ) ;
#18655=CARTESIAN_POINT ( 'NONE',  ( 3.512766787570772653, -2.682019731918489303, 14.81029789862156143 ) ) ;
#18657=CARTESIAN_POINT ( 'NONE',  ( 1.846138399168762989, 3.446241763652997836, 11.95493567637851839 ) ) ;
#18660=CARTESIAN_POINT ( 'NONE',  ( 0.3151930723728382788, 11.16020735774779027, -8.013866567350774517 ) ) ;
#18662=ORIENTED_EDGE ( 'NONE', *, *, #17019, .F. ) ;
#18663=ORIENTED_EDGE ( 'NONE', *, *, #1715, .F. ) ;
#18674=CARTESIAN_POINT ( 'NONE',  ( 16.56872352241294521, 0.01027347319884441834, -0.001821578298044677175 ) ) ;
#18682=ORIENTED_EDGE ( 'NONE', *, *, #18497, .F. ) ;
#18689=CARTESIAN_POINT ( 'NONE',  ( 2.002547531651519996, 12.57989064830759496, 0.6781519942172178350 ) ) ;
#18693=EDGE_CURVE ( 'NONE', #11053, #13313, #8103, .T. ) ;
#18695=CARTESIAN_POINT ( 'NONE',  ( 1.918921323896323639, -10.48468902844557071, 6.832782632379341692 ) ) ;
#18701=ORIENTED_EDGE ( 'NONE', *, *, #6047, .F. ) ;
#18703=CARTESIAN_POINT ( 'NONE',  ( 0.4754618798421171855, 10.80499583390525764, -8.775436892860993154 ) ) ;
#18709=ORIENTED_EDGE ( 'NONE', *, *, #2079, .T. ) ;
#18711=DIRECTION ( 'NONE',  ( -1.000000000000000000, -0.000000000000000000, -0.000000000000000000 ) ) ;
#18712=FACE_OUTER_BOUND ( 'NONE', #4536, .T. ) ;
#18713=( BOUNDED_SURFACE ( )  B_SPLINE_SURFACE ( 3, 1, ( 
 ( #6349, #14935 ),
 ( #3463, #9297 ),
 ( #6532, #416 ),
 ( #10936, #13597 ) ),
 .UNSPECIFIED., .F., .F., .T. ) 
 B_SPLINE_SURFACE_WITH_KNOTS ( ( 4, 4 ),
 ( 2, 2 ),
 ( 0.000000000000000000, 1.000000000000000000 ),
 ( 0.000000000000000000, 1.000000000000000000 ),
 .UNSPECIFIED. ) 
 GEOMETRIC_REPRESENTATION_ITEM ( )  RATIONAL_B_SPLINE_SURFACE ( (
 ( 1.000000000000000000, 1.000000000000000000),
 ( 0.7792777138730160313, 0.9689936506012927220),
 ( 0.7792777138730160313, 0.9689936506012927220),
 ( 1.000000000000000000, 1.000000000000000000) ) ) 
 REPRESENTATION_ITEM ( '' )  SURFACE ( )  );
#18716=CARTESIAN_POINT ( 'NONE',  ( 16.56679352167444819, -0.009190982326619729845, -0.001390132774594407148 ) ) ;
#18719=CARTESIAN_POINT ( 'NONE',  ( 0.3150692679895995552, -13.01874238516607285, -4.391039771493804089 ) ) ;
#18721=CARTESIAN_POINT ( 'NONE',  ( 1.846138399168762101, 6.971848976711011225, 10.30487220521572667 ) ) ;
#18724=DIRECTION ( 'NONE',  ( -0.7635533937278216055, -0.5095610256143884298, 0.3966532189476580372 ) ) ;
#18729=CARTESIAN_POINT ( 'NONE',  ( 2.636624412714236865, 0.000000000000000000, 0.000000000000000000 ) ) ;
#18730=ORIENTED_EDGE ( 'NONE', *, *, #1532, .T. ) ;
#18731=LINE ( 'NONE', #7187, #17624 ) ;
#18733=DIRECTION ( 'NONE',  ( -1.000000000000000000, -0.000000000000000000, -0.000000000000000000 ) ) ;
#18734=B_SPLINE_CURVE_WITH_KNOTS ( 'NONE', 3,
 ( #2484, #8159, #3843, #12623, #8339, #8252, #1058, #2314, #18367, #13974, #16937, #883, #6724 ),
 .UNSPECIFIED., .F., .F.,
 ( 4, 3, 3, 3, 4 ),
 ( 3.878959614448864246E-18, 0.0002299780670421054142, 0.0004599561239687919093, 0.0006896788984287899067, 0.0009194956271626406052 ),
 .UNSPECIFIED. ) ;
#18735=ORIENTED_EDGE ( 'NONE', *, *, #1264, .F. ) ;
#18737=CARTESIAN_POINT ( 'NONE',  ( 0.4862570985993235340, -5.003653737315397976, -12.97920246947884770 ) ) ;
#18738=ORIENTED_EDGE ( 'NONE', *, *, #14977, .T. ) ;
#18744=ORIENTED_EDGE ( 'NONE', *, *, #10780, .F. ) ;
#18745=ADVANCED_FACE ( 'NONE', ( #10393 ), #13294, .F. ) ;
#18750=CARTESIAN_POINT ( 'NONE',  ( 2.636624412714237309, 7.605649742761960042, 14.14563173255213613 ) ) ;
#18751=CARTESIAN_POINT ( 'NONE',  ( 1.846613052777651198, 4.166957398589849149, 11.72395935470500028 ) ) ;
#18756=CARTESIAN_POINT ( 'NONE',  ( 0.4862570985993235340, -13.44146924561378498, -3.580942890621813923 ) ) ;
#18759=B_SPLINE_CURVE_WITH_KNOTS ( 'NONE', 3,
 ( #2089, #7925, #5031, #857, #6504, #7956 ),
 .UNSPECIFIED., .F., .F.,
 ( 4, 2, 4 ),
 ( 0.000000000000000000, 0.001656992708823243950, 0.003313985417646487033 ),
 .UNSPECIFIED. ) ;
#18763=ORIENTED_EDGE ( 'NONE', *, *, #1420, .T. ) ;
#18764=CARTESIAN_POINT ( 'NONE',  ( 0.3939875929385635578, -4.930599594904470528, -12.90850834464105645 ) ) ;
#18768=CARTESIAN_POINT ( 'NONE',  ( 2.320521194581854907, 10.64885423995017355, 11.60169518685927059 ) ) ;
#18769=CARTESIAN_POINT ( 'NONE',  ( 1.847247051441587518, -9.967131402978145260, -7.448813758297282206 ) ) ;
#18774=CARTESIAN_POINT ( 'NONE',  ( 3.950837973638676281, -6.316429227969383220, -13.10350451991847009 ) ) ;
#18776=CARTESIAN_POINT ( 'NONE',  ( 0.4754618798421167414, 8.775436892861268490, -10.80499583390503560 ) ) ;
#18781=EDGE_CURVE ( 'NONE', #2339, #8095, #1940, .T. ) ;
#18782=ORIENTED_EDGE ( 'NONE', *, *, #10596, .F. ) ;
#18787=CARTESIAN_POINT ( 'NONE',  ( 8.522092701127531811, 3.777034505568523048, 5.841710761610143798 ) ) ;
#18789=CARTESIAN_POINT ( 'NONE',  ( 0.3058872367615226295, 10.75034008168916166, 8.562166468153757037 ) ) ;
#18790=EDGE_LOOP ( 'NONE', ( #10730, #9041, #6497, #8313 ) ) ;
#18791=FACE_OUTER_BOUND ( 'NONE', #8561, .T. ) ;
#18794=CARTESIAN_POINT ( 'NONE',  ( 1.845755665166725290, -10.33920510797148395, 6.920419570228313333 ) ) ;
#18798=CARTESIAN_POINT ( 'NONE',  ( 2.636624412716062071, -11.10302021258080352, -11.60464335004061454 ) ) ;
#18800=B_SPLINE_CURVE_WITH_KNOTS ( 'NONE', 3,
 ( #7939, #2362, #6681, #660, #9534, #13749 ),
 .UNSPECIFIED., .F., .F.,
 ( 4, 2, 4 ),
 ( 9.263427422397552964E-19, 0.001500839035891552656, 0.003001678071783104446 ),
 .UNSPECIFIED. ) ;
#18802=VERTEX_POINT ( 'NONE', #736 ) ;
#18807=EDGE_LOOP ( 'NONE', ( #8766, #6379, #18663, #15899 ) ) ;
#18814=CARTESIAN_POINT ( 'NONE',  ( 16.56679352167444819, 0.001390132774595458174, 0.009190982326619367287 ) ) ;
#18815=ORIENTED_EDGE ( 'NONE', *, *, #18872, .F. ) ;
#18816=CARTESIAN_POINT ( 'NONE',  ( 0.3170788640506440603, 13.02120094575828269, 4.392045232375855868 ) ) ;
#18819=CARTESIAN_POINT ( 'NONE',  ( 0.3137051932979792457, -13.73004976592201842, -0.4596302728641207813 ) ) ;
#18820=CARTESIAN_POINT ( 'NONE',  ( 0.3151928476913548050, -13.06684726503523919, -4.245457024760359133 ) ) ;
#18828=ORIENTED_EDGE ( 'NONE', *, *, #11354, .F. ) ;
#18833=CARTESIAN_POINT ( 'NONE',  ( 0.3142011359265349801, 7.762194356530932815, -11.33549115679415031 ) ) ;
#18839=CARTESIAN_POINT ( 'NONE',  ( 3.950837973638676281, -14.41405733518059229, -1.958075594453940971 ) ) ;
#18844=CARTESIAN_POINT ( 'NONE',  ( 0.3148208552358917611, -0.2299193288886511033, -13.73693263646119078 ) ) ;
#18851=CARTESIAN_POINT ( 'NONE',  ( 2.705023505549867924, 12.36217802824812573, -4.909285963183943835 ) ) ;
#18853=CARTESIAN_POINT ( 'NONE',  ( 1.918921323896322750, -12.49850046818174398, -0.6349083173281465653 ) ) ;
#18854=VERTEX_POINT ( 'NONE', #6571 ) ;
#18857=ORIENTED_EDGE ( 'NONE', *, *, #7528, .T. ) ;
#18861=ORIENTED_EDGE ( 'NONE', *, *, #18614, .F. ) ;
#18863=ORIENTED_EDGE ( 'NONE', *, *, #18872, .T. ) ;
#18865=CARTESIAN_POINT ( 'NONE',  ( 1.847168016377985111, -10.17509564929253507, -7.161712042621569019 ) ) ;
#18867=( BOUNDED_SURFACE ( )  B_SPLINE_SURFACE ( 3, 1, ( 
 ( #16107, #2987 ),
 ( #7415, #5964 ),
 ( #14857, #17638 ),
 ( #16198, #6071 ) ),
 .UNSPECIFIED., .F., .F., .T. ) 
 B_SPLINE_SURFACE_WITH_KNOTS ( ( 4, 4 ),
 ( 2, 2 ),
 ( 0.000000000000000000, 1.000000000000000000 ),
 ( 0.000000000000000000, 1.000000000000000000 ),
 .UNSPECIFIED. ) 
 GEOMETRIC_REPRESENTATION_ITEM ( )  RATIONAL_B_SPLINE_SURFACE ( (
 ( 1.000000000000000000, 1.000000000000000000),
 ( 0.9933953342250438912, 0.8357391271907739227),
 ( 0.9933953342250438912, 0.8357391271907739227),
 ( 1.000000000000000000, 1.000000000000000000) ) ) 
 REPRESENTATION_ITEM ( '' )  SURFACE ( )  );
#18868=CARTESIAN_POINT ( 'NONE',  ( 1.977228804423455610, 11.52787183731216381, -10.21522664410554881 ) ) ;
#18869=( BOUNDED_SURFACE ( )  B_SPLINE_SURFACE ( 3, 1, ( 
 ( #6770, #12580 ),
 ( #6490, #6585 ),
 ( #18144, #5045 ),
 ( #10897, #3795 ) ),
 .UNSPECIFIED., .F., .F., .T. ) 
 B_SPLINE_SURFACE_WITH_KNOTS ( ( 4, 4 ),
 ( 2, 2 ),
 ( 0.000000000000000000, 1.000000000000000000 ),
 ( 0.000000000000000000, 1.000000000000000000 ),
 .UNSPECIFIED. ) 
 GEOMETRIC_REPRESENTATION_ITEM ( )  RATIONAL_B_SPLINE_SURFACE ( (
 ( 1.000000000000000000, 1.000000000000000000),
 ( 0.7792777138730158093, 0.9689936506012928330),
 ( 0.7792777138730158093, 0.9689936506012928330),
 ( 1.000000000000000000, 1.000000000000000000) ) ) 
 REPRESENTATION_ITEM ( '' )  SURFACE ( )  );
#18871=DIRECTION ( 'NONE',  ( -1.000000000000000000, -0.000000000000000000, -0.000000000000000000 ) ) ;
#18872=EDGE_CURVE ( 'NONE', #11553, #7697, #563, .T. ) ;
#18874=CARTESIAN_POINT ( 'NONE',  ( 0.3142014840576500267, 13.73311050063163918, 0.3830336514509360413 ) ) ;
#18883=CARTESIAN_POINT ( 'NONE',  ( 0.3720661004400037664, 10.73619472937702213, 8.694226082900630814 ) ) ;
#18887=CARTESIAN_POINT ( 'NONE',  ( 3.950837973638675393, 10.05648675950126325, 10.51028938476221342 ) ) ;
#18889=CARTESIAN_POINT ( 'NONE',  ( 2.636624412714292376, 11.60464335004048309, 11.10302021257707850 ) ) ;
#18890=CARTESIAN_POINT ( 'NONE',  ( 0.3142014840576535795, -11.33546131209467767, 7.762239086932820165 ) ) ;
#18895=CARTESIAN_POINT ( 'NONE',  ( 3.950837973638675393, 2.591948120961804936, 14.31366178983254578 ) ) ;
#18903=VERTEX_POINT ( 'NONE', #1095 ) ;
#18904=CARTESIAN_POINT ( 'NONE',  ( 1.847380140988739594, 7.402792205949101145, 10.00162556679653214 ) ) ;
ENDSEC;
END-ISO-10303-21;
